ISO-10303-21;
HEADER;
FILE_DESCRIPTION (('STEP AP214'),
    '1' );
FILE_NAME ('Latch Return Spring.step',
    '2026-10-06T13:23:30',
    ( '' ),
    ( '' ),
    'SwSTEP 2.0',
    'SolidWorks 2020',
    '' );
FILE_SCHEMA (( 'AUTOMOTIVE_DESIGN' ));
ENDSEC;

DATA;
#5=CARTESIAN_POINT ( 'NONE',  ( -17.23399296970191941, 39.75881394383647915, -140.1956667236787553 ) ) ;
#24=CARTESIAN_POINT ( 'NONE',  ( -5.972224716186543603, 40.79464204718496489, -141.7656025440738006 ) ) ;
#36=CARTESIAN_POINT ( 'NONE',  ( -30.18072937777062492, 41.58839647259347316, -144.3146225325547505 ) ) ;
#40=CARTESIAN_POINT ( 'NONE',  ( -11.30159772195502299, 34.40649072814353815, -140.3533750429825773 ) ) ;
#41=CARTESIAN_POINT ( 'NONE',  ( -19.36238656785138090, 32.32519816855536732, -144.8017779651653427 ) ) ;
#48=CARTESIAN_POINT ( 'NONE',  ( -8.100541861814468447, 36.99062475582145737, -140.7379126119401178 ) ) ;
#56=CARTESIAN_POINT ( 'NONE',  ( -17.71126569040000120, 40.30718541979999969, -145.9389846960000057 ) ) ;
#61=CLOSED_SHELL ( 'NONE', ( #2527, #3162, #21913, #12259, #23509, #6478, #21323, #18404, #11266, #1129, #5411, #9358, #21072, #12421, #16618, #19421, #14593, #11107, #12865, #16221, #14697, #10087, #8870, #20532, #21101, #11720, #17202, #7335, #11973, #7291, #21318, #13553, #10889, #7699, #12447, #10834 ) ) ;
#62=FACE_OUTER_BOUND ( 'NONE', #19920, .T. ) ;
#71=ORIENTED_EDGE ( 'NONE', *, *, #16428, .T. ) ;
#84=CARTESIAN_POINT ( 'NONE',  ( -19.91646121121569735, 34.85517757522313076, -141.3256718703773629 ) ) ;
#85=CARTESIAN_POINT ( 'NONE',  ( -30.02199999990000023, 40.03108891319999429, -145.8052959529999839 ) ) ;
#108=CARTESIAN_POINT ( 'NONE',  ( -21.95493828276233472, 34.13232134794248651, -147.9325040407576353 ) ) ;
#113=ORIENTED_EDGE ( 'NONE', *, *, #15897, .T. ) ;
#114=CARTESIAN_POINT ( 'NONE',  ( -26.86882954950000268, 40.29793777999999804, -142.0811670120000088 ) ) ;
#128=CARTESIAN_POINT ( 'NONE',  ( -17.11288009319332915, 40.89466944836319584, -143.6359263498834196 ) ) ;
#141=CARTESIAN_POINT ( 'NONE',  ( -7.010349702009219364, 37.05829245175948472, -148.1453878979395995 ) ) ;
#151=CARTESIAN_POINT ( 'NONE',  ( -29.72253042784264210, 40.43424528537140361, -140.6915255650335723 ) ) ;
#155=CARTESIAN_POINT ( 'NONE',  ( -10.36638211085415584, 32.95473824138212393, -141.4495653476137704 ) ) ;
#156=CARTESIAN_POINT ( 'NONE',  ( -18.21358191688009498, 34.41669922854067920, -147.7040578527177388 ) ) ;
#159=CARTESIAN_POINT ( 'NONE',  ( -22.66750349916592810, 37.99877533998466816, -139.6205617058595294 ) ) ;
#166=CARTESIAN_POINT ( 'NONE',  ( -5.932764524189999555, 37.76833845600000217, -147.9772051180000005 ) ) ;
#185=CARTESIAN_POINT ( 'NONE',  ( -16.74070468267852618, 33.96681352825373779, -142.1712902011884978 ) ) ;
#191=CARTESIAN_POINT ( 'NONE',  ( -19.09494877074376262, 33.54410563133428269, -142.1858765932176141 ) ) ;
#195=EDGE_CURVE ( 'NONE', #7827, #16530, #20002, .T. ) ;
#206=CARTESIAN_POINT ( 'NONE',  ( -26.46126365530976443, 39.05410761395327057, -141.1838645948565443 ) ) ;
#208=CARTESIAN_POINT ( 'NONE',  ( -23.51619327739999932, 36.94101002280000046, -140.1031831869999849 ) ) ;
#221=CARTESIAN_POINT ( 'NONE',  ( -11.29029698198118048, 36.23043332044583309, -140.4049246345721826 ) ) ;
#223=CARTESIAN_POINT ( 'NONE',  ( -9.052249647940781685, 41.71831906193862949, -143.4732298663905965 ) ) ;
#235=CARTESIAN_POINT ( 'NONE',  ( -17.12614424251881573, 38.90004930153931895, -139.7093083313472448 ) ) ;
#236=CARTESIAN_POINT ( 'NONE',  ( -29.46750132911070352, 41.44936499793962525, -145.0977680319627439 ) ) ;
#242=CARTESIAN_POINT ( 'NONE',  ( -18.09080689940000397, 41.54765954780000214, -144.4256796519999853 ) ) ;
#252=CARTESIAN_POINT ( 'NONE',  ( -10.92854443050000057, 33.70908472050000171, -142.0058283510000194 ) ) ;
#255=CARTESIAN_POINT ( 'NONE',  ( -27.13199227600000185, 40.71900643419999710, -144.3906906950000177 ) ) ;
#266=CARTESIAN_POINT ( 'NONE',  ( -19.59255166828732087, 37.05126161859348599, -140.3061871182880225 ) ) ;
#269=CARTESIAN_POINT ( 'NONE',  ( -22.77297780190586707, 38.93970885093763457, -139.8786318329592291 ) ) ;
#285=CARTESIAN_POINT ( 'NONE',  ( -13.05114220192597507, 34.48316525647341990, -140.6280605682619864 ) ) ;
#307=EDGE_CURVE ( 'NONE', #18180, #4474, #17692, .T. ) ;
#310=CARTESIAN_POINT ( 'NONE',  ( -20.84115054893410601, 39.15569877547226696, -141.0545280455379782 ) ) ;
#321=CARTESIAN_POINT ( 'NONE',  ( -26.41333858494015630, 40.49754993825023064, -143.6922548833833559 ) ) ;
#329=CARTESIAN_POINT ( 'NONE',  ( -29.13601448249999848, 36.98639052360000079, -140.5419328609999923 ) ) ;
#330=CARTESIAN_POINT ( 'NONE',  ( -23.51619327739999932, 36.94101002280000046, -140.1031831869999849 ) ) ;
#344=EDGE_CURVE ( 'NONE', #6561, #14370, #10508, .T. ) ;
#347=CARTESIAN_POINT ( 'NONE',  ( -12.26329284728311997, 39.72411301547229101, -147.9408354451884122 ) ) ;
#348=CARTESIAN_POINT ( 'NONE',  ( -16.81794493329665841, 37.02435727937783838, -140.5111119823167769 ) ) ;
#349=CARTESIAN_POINT ( 'NONE',  ( -29.33124862419971635, 40.50047896906287548, -145.5019065615213663 ) ) ;
#360=CARTESIAN_POINT ( 'NONE',  ( -20.38718376954965450, 37.93371258244203403, -139.5095340218612137 ) ) ;
#374=EDGE_CURVE ( 'NONE', #19550, #16183, #12819, .T. ) ;
#386=CARTESIAN_POINT ( 'NONE',  ( -19.44179523432628898, 36.07285822990824897, -139.5501647635505265 ) ) ;
#387=EDGE_CURVE ( 'NONE', #598, #15229, #5528, .T. ) ;
#389=CARTESIAN_POINT ( 'NONE',  ( -9.032885736824702860, 36.94161628544370046, -147.5965110586934941 ) ) ;
#390=CARTESIAN_POINT ( 'NONE',  ( -24.12417792002877803, 37.90708835554210765, -148.6276364009957547 ) ) ;
#399=( BOUNDED_CURVE ( )  B_SPLINE_CURVE ( 5, ( #9681, #664, #13385, #7895, #20653, #2571 ),
 .UNSPECIFIED., .F., .F. ) 
 B_SPLINE_CURVE_WITH_KNOTS ( ( 6, 6 ),
 ( 1.570796326503991924, 3.141592653590000062 ),
 .UNSPECIFIED. ) 
 CURVE ( )  GEOMETRIC_REPRESENTATION_ITEM ( )  RATIONAL_B_SPLINE_CURVE ( ( 0.2500000000000000555, 0.2499999999629477221, 0.2999999999444215582, 0.3999999999258954109, 0.5999999999258953665, 1.000000000000000000 ) ) 
 REPRESENTATION_ITEM ( '' )  );
#403=CARTESIAN_POINT ( 'NONE',  ( -5.935706415042687034, 40.05508565971382495, -145.7977461092045530 ) ) ;
#406=CARTESIAN_POINT ( 'NONE',  ( -22.02234931426594144, 33.75799147763578389, -142.0591516048408778 ) ) ;
#409=CARTESIAN_POINT ( 'NONE',  ( -13.09722452613436516, 33.49976389652860576, -143.7852608042046256 ) ) ;
#422=CARTESIAN_POINT ( 'NONE',  ( -13.71246964740000074, 35.06639867129999999, -139.8243480419999685 ) ) ;
#423=CARTESIAN_POINT ( 'NONE',  ( -9.285539185979999388, 35.09287230280000358, -147.9937876190000168 ) ) ;
#432=CARTESIAN_POINT ( 'NONE',  ( -20.83898962464882842, 39.06148406400365758, -147.0165715935449953 ) ) ;
#445=CARTESIAN_POINT ( 'NONE',  ( -26.83129905141586846, 39.07913712597448352, -146.9590705472632521 ) ) ;
#447=CARTESIAN_POINT ( 'NONE',  ( -23.44935120326739764, 36.05472785596497687, -139.7839751993253685 ) ) ;
#448=B_SPLINE_CURVE_WITH_KNOTS ( 'NONE', 5,
 ( #16535, #590, #18437, #5588, #12836, #20113, #242, #2960, #2732, #6397, #21052, #13899 ),
 .UNSPECIFIED., .F., .F.,
 ( 6, 3, 3, 6 ),
 ( 0.000000000000000000, 4.124045064660000648, 8.344666563069999654, 12.67057240369999782 ),
 .UNSPECIFIED. ) ;
#454=CARTESIAN_POINT ( 'NONE',  ( -27.67795712710000089, 37.78351609900000341, -147.6208067679999942 ) ) ;
#459=CARTESIAN_POINT ( 'NONE',  ( -8.767025672889793952, 38.73734267217074034, -139.9349420084332962 ) ) ;
#466=CARTESIAN_POINT ( 'NONE',  ( -25.90907760989737341, 37.01347911741230945, -139.4251635482864913 ) ) ;
#469=CARTESIAN_POINT ( 'NONE',  ( -11.91401949022731799, 39.67431894273512683, -140.4170659721649486 ) ) ;
#471=CARTESIAN_POINT ( 'NONE',  ( -17.79289316922850617, 37.75490432960187803, -147.9677353736447571 ) ) ;
#474=CARTESIAN_POINT ( 'NONE',  ( -7.572469997240619755, 37.05365869150052305, -139.6601318952005215 ) ) ;
#476=CARTESIAN_POINT ( 'NONE',  ( -30.64259443220337786, 40.28463426600031028, -145.8661425198801567 ) ) ;
#482=CARTESIAN_POINT ( 'NONE',  ( -20.97542662470000252, 40.85881720449999932, -141.8340754020000247 ) ) ;
#509=CARTESIAN_POINT ( 'NONE',  ( -9.072898850179999641, 36.94639249900000522, -148.2684494029999769 ) ) ;
#510=CARTESIAN_POINT ( 'NONE',  ( -22.88190335430070377, 39.79040966463082185, -140.3815034252083365 ) ) ;
#511=CARTESIAN_POINT ( 'NONE',  ( -15.46613156833100078, 36.99333119719623397, -147.5584717933785726 ) ) ;
#519=CARTESIAN_POINT ( 'NONE',  ( -7.081915218180248495, 37.06683495600064759, -147.7519347211647585 ) ) ;
#525=CARTESIAN_POINT ( 'NONE',  ( -22.51542269368358617, 35.01159793962629863, -141.2271873608204373 ) ) ;
#528=CARTESIAN_POINT ( 'NONE',  ( -12.51319725274692374, 36.30635479524141829, -147.4212986608875156 ) ) ;
#535=CARTESIAN_POINT ( 'NONE',  ( -13.59981317924083655, 37.05039483956776536, -139.6306434366684925 ) ) ;
#539=CARTESIAN_POINT ( 'NONE',  ( -27.92684401174140163, 34.15387849089756145, -147.9120013265362559 ) ) ;
#540=ORIENTED_EDGE ( 'NONE', *, *, #741, .F. ) ;
#543=CARTESIAN_POINT ( 'NONE',  ( -13.13790626639999992, 32.38985286280000508, -143.7114742199999853 ) ) ;
#545=DIRECTION ( 'NONE',  ( 0.000000000000000000, -0.8660254037841379482, 0.5000000000005210277 ) ) ;
#550=CARTESIAN_POINT ( 'NONE',  ( -19.79317654000728055, 38.64314174751988418, -140.5356700201026001 ) ) ;
#562=CARTESIAN_POINT ( 'NONE',  ( -25.64792992871999999, 37.04465132566515706, -139.7265440085297996 ) ) ;
#573=CARTESIAN_POINT ( 'NONE',  ( -6.366122344970272628, 35.09376510157478180, -148.3726825278031640 ) ) ;
#582=CARTESIAN_POINT ( 'NONE',  ( -12.41748666345656282, 41.11124952250558096, -146.5209369397300918 ) ) ;
#583=CARTESIAN_POINT ( 'NONE',  ( -18.01836706189362758, 38.92693601672081627, -148.4107366658697913 ) ) ;
#584=CARTESIAN_POINT ( 'NONE',  ( -29.86462848822639771, 41.46897301220559484, -145.0541174283626162 ) ) ;
#586=CARTESIAN_POINT ( 'NONE',  ( -6.518232409689999507, 33.41592120480000006, -146.1606736330000160 ) ) ;
#590=CARTESIAN_POINT ( 'NONE',  ( -17.32451618079999633, 37.89224186959999940, -139.5945780149999962 ) ) ;
#594=CARTESIAN_POINT ( 'NONE',  ( -19.90747643769189423, 40.84829927215759682, -141.9758135236385783 ) ) ;
#596=CARTESIAN_POINT ( 'NONE',  ( -27.80359210614968291, 32.89696731216636039, -146.3345487532903917 ) ) ;
#598=VERTEX_POINT ( 'NONE', #7861 ) ;
#606=CARTESIAN_POINT ( 'NONE',  ( -19.79184979336555017, 37.02747215728111740, -140.6521846888478819 ) ) ;
#625=CARTESIAN_POINT ( 'NONE',  ( -16.48779918059999616, 32.42295671489999620, -143.3618442240000093 ) ) ;
#630=CARTESIAN_POINT ( 'NONE',  ( -5.700500667576763547, 40.41662643729544868, -143.6588243170081682 ) ) ;
#635=CARTESIAN_POINT ( 'NONE',  ( -21.59125871610556402, 33.71934651132892924, -145.8354015992185850 ) ) ;
#638=CARTESIAN_POINT ( 'NONE',  ( -12.69103652210661615, 35.00128951864121518, -146.9022827771903223 ) ) ;
#650=CARTESIAN_POINT ( 'NONE',  ( -12.79720822650000045, 32.99715178900000012, -146.4964997610000239 ) ) ;
#651=CARTESIAN_POINT ( 'NONE',  ( -10.56415788819999868, 36.18163687389999694, -139.7056672729999889 ) ) ;
#658=CARTESIAN_POINT ( 'NONE',  ( -20.74716465872499427, 38.46557005212173408, -140.6515328043094826 ) ) ;
#664=CARTESIAN_POINT ( 'NONE',  ( -22.48976697757458254, 37.06353063726728436, -140.4055699430356015 ) ) ;
#669=( BOUNDED_CURVE ( )  B_SPLINE_CURVE ( 5, ( #13319, #6186, #2623, #22370, #18688, #13085, #2509, #252, #11633, #18446, #20701, #12969 ),
 .UNSPECIFIED., .F., .F. ) 
 B_SPLINE_CURVE_WITH_KNOTS ( ( 6, 3, 3, 6 ),
 ( 0.000000000000000000, 4.570086947620000117, 8.869210483019999813, 12.91901055009999943 ),
 .UNSPECIFIED. ) 
 CURVE ( )  GEOMETRIC_REPRESENTATION_ITEM ( )  RATIONAL_B_SPLINE_CURVE ( ( 0.2500000000000000000, 0.2500000000000000000, 0.2500000000000000000, 0.2500000000000000000, 0.2500000000000000000, 0.2500000000000000000, 0.2500000000000000000, 0.2500000000000000000, 0.2500000000000000000, 0.2500000000000000000, 0.2500000000000000000, 0.2500000000000000000 ) ) 
 REPRESENTATION_ITEM ( '' )  );
#675=CARTESIAN_POINT ( 'NONE',  ( -27.01837854179119702, 37.68189902554408377, -147.5283965130139734 ) ) ;
#678=CARTESIAN_POINT ( 'NONE',  ( -22.55322464622646805, 32.24327928621291051, -143.4921094554972854 ) ) ;
#686=CARTESIAN_POINT ( 'NONE',  ( -27.30725598840000146, 40.30964169850000189, -145.9048855949999961 ) ) ;
#690=CARTESIAN_POINT ( 'NONE',  ( -6.875342432574099050, 34.21798895325673584, -148.0105455186688914 ) ) ;
#699=CARTESIAN_POINT ( 'NONE',  ( -12.76385253868072134, 37.02886902027827887, -147.6186336933980101 ) ) ;
#700=CARTESIAN_POINT ( 'NONE',  ( -17.81786398825392581, 37.84862138750237648, -148.3932271983275086 ) ) ;
#711=CARTESIAN_POINT ( 'NONE',  ( -21.83774898087361649, 37.96346924979418702, -148.4776379419676857 ) ) ;
#741=EDGE_CURVE ( 'NONE', #598, #16477, #15266, .T. ) ;
#743=CARTESIAN_POINT ( 'NONE',  ( -24.79382848429712638, 38.90154695920348615, -148.2729990965086699 ) ) ;
#745=CARTESIAN_POINT ( 'NONE',  ( -15.70784696974144801, 32.45430872951681778, -144.2620499800023879 ) ) ;
#746=CARTESIAN_POINT ( 'NONE',  ( -16.93132238861308281, 33.26380838982603194, -143.5428277902702803 ) ) ;
#758=CARTESIAN_POINT ( 'NONE',  ( -22.07763076357180054, 37.06632353693598247, -147.8362371613994242 ) ) ;
#761=CARTESIAN_POINT ( 'NONE',  ( -13.64404366366992072, 33.71937897316467314, -142.3027892629986013 ) ) ;
#765=CARTESIAN_POINT ( 'NONE',  ( -27.26567793380000282, 36.96940380710000085, -148.4835048639999968 ) ) ;
#767=CARTESIAN_POINT ( 'NONE',  ( -7.682760800853645655, 38.61178422963649837, -140.5440265716989359 ) ) ;
#778=CARTESIAN_POINT ( 'NONE',  ( -14.49707537166952598, 35.20425844453338726, -140.3484218534934485 ) ) ;
#779=CARTESIAN_POINT ( 'NONE',  ( -9.394775000179999225, 34.25903911019999981, -147.4808749560000081 ) ) ;
#787=CARTESIAN_POINT ( 'NONE',  ( -20.26899604970972035, 40.93030953072783973, -143.7497896408596034 ) ) ;
#788=CARTESIAN_POINT ( 'NONE',  ( -18.53945141080000170, 39.74065879090000664, -147.6687609889999919 ) ) ;
#794=CARTESIAN_POINT ( 'NONE',  ( -24.98993381957792792, 33.76017858760970825, -142.1401211143833621 ) ) ;
#801=CARTESIAN_POINT ( 'NONE',  ( -27.26567793390747596, 36.96940380712532459, -148.4835048638151989 ) ) ;
#804=ORIENTED_EDGE ( 'NONE', *, *, #23482, .F. ) ;
#812=CARTESIAN_POINT ( 'NONE',  ( -10.90809651384244461, 40.52503132629866656, -142.2168021453966276 ) ) ;
#815=CARTESIAN_POINT ( 'NONE',  ( -9.483015687148979467, 40.53201449227000097, -146.0034198470924025 ) ) ;
#818=( BOUNDED_SURFACE ( )  B_SPLINE_SURFACE ( 5, 5, ( 
 ( #14854, #2244, #20790, #18525, #4481, #22111 ),
 ( #9469, #16623, #20557, #16863, #16745, #5914 ),
 ( #13169, #4131, #5800, #573, #11374, #15078 ),
 ( #6031, #4256, #690, #2591, #6153, #18768 ),
 ( #2479, #4366, #7920, #15202, #15677, #928 ),
 ( #10414, #10302, #6619, #12209, #12321, #19485 ),
 ( #8274, #22940, #17688, #15426, #19230, #6508 ),
 ( #17329, #14123, #20918, #15546, #3181, #2943 ),
 ( #10052, #1396, #8622, #21268, #21033, #15896 ),
 ( #8403, #17577, #8154, #13994, #23161, #4840 ),
 ( #6858, #3069, #21391, #5077, #22685, #1293 ),
 ( #2714, #13881, #21152, #6380, #23048, #9941 ) ),
 .UNSPECIFIED., .F., .F., .F. ) 
 B_SPLINE_SURFACE_WITH_KNOTS ( ( 6, 3, 3, 6 ),
 ( 6, 6 ),
 ( 0.000000000000000000, 4.346865784160000246, 8.778337911509998648, 13.29702284770000098 ),
 ( 1.570796326505564888, 3.141592653590000062 ),
 .UNSPECIFIED. ) 
 GEOMETRIC_REPRESENTATION_ITEM ( )  RATIONAL_B_SPLINE_SURFACE ( (
 ( 0.2500000000000000000, 0.2499999999631480063, 0.2999999999447220400, 0.3999999999262959793, 0.5999999999262960459, 1.000000000000000000),
 ( 0.2500000000000000000, 0.2499999999631480063, 0.2999999999447220400, 0.3999999999262959793, 0.5999999999262960459, 1.000000000000000000),
 ( 0.2500000000000000000, 0.2499999999631480063, 0.2999999999447220400, 0.3999999999262959793, 0.5999999999262960459, 1.000000000000000000),
 ( 0.2500000000000000000, 0.2499999999631480063, 0.2999999999447220400, 0.3999999999262959793, 0.5999999999262960459, 1.000000000000000000),
 ( 0.2500000000000000000, 0.2499999999631480063, 0.2999999999447220400, 0.3999999999262959793, 0.5999999999262960459, 1.000000000000000000),
 ( 0.2500000000000000000, 0.2499999999631480063, 0.2999999999447220400, 0.3999999999262959793, 0.5999999999262960459, 1.000000000000000000),
 ( 0.2500000000000000000, 0.2499999999631480063, 0.2999999999447220400, 0.3999999999262959793, 0.5999999999262960459, 1.000000000000000000),
 ( 0.2500000000000000000, 0.2499999999631480063, 0.2999999999447220400, 0.3999999999262959793, 0.5999999999262960459, 1.000000000000000000),
 ( 0.2500000000000000000, 0.2499999999631480063, 0.2999999999447220400, 0.3999999999262959793, 0.5999999999262960459, 1.000000000000000000),
 ( 0.2500000000000000000, 0.2499999999631480063, 0.2999999999447220400, 0.3999999999262959793, 0.5999999999262960459, 1.000000000000000000),
 ( 0.2500000000000000000, 0.2499999999631480063, 0.2999999999447220400, 0.3999999999262959793, 0.5999999999262960459, 1.000000000000000000),
 ( 0.2500000000000000000, 0.2499999999631480063, 0.2999999999447220400, 0.3999999999262959793, 0.5999999999262960459, 1.000000000000000000) ) ) 
 REPRESENTATION_ITEM ( '' )  SURFACE ( )  );
#820=CARTESIAN_POINT ( 'NONE',  ( -14.24884431172416832, 36.97292245485109419, -139.4994906131685184 ) ) ;
#826=EDGE_CURVE ( 'NONE', #15229, #14150, #20135, .T. ) ;
#838=CARTESIAN_POINT ( 'NONE',  ( -24.90252082140812107, 32.60880315529160356, -143.5690609613828030 ) ) ;
#849=EDGE_CURVE ( 'NONE', #8868, #17995, #10312, .T. ) ;
#857=CARTESIAN_POINT ( 'NONE',  ( -30.60952439866935748, 40.96074107050382906, -145.5181652820941167 ) ) ;
#858=CARTESIAN_POINT ( 'NONE',  ( -14.11967125442052051, 36.98834135278355717, -140.5455248811183822 ) ) ;
#868=CARTESIAN_POINT ( 'NONE',  ( -24.23404356110848568, 41.65913112518386185, -144.5746520422516994 ) ) ;
#869=CARTESIAN_POINT ( 'NONE',  ( -16.92867099909999595, 34.38083942290000294, -140.2753207150000208 ) ) ;
#870=CARTESIAN_POINT ( 'NONE',  ( -16.69209583599786484, 32.46303108206343069, -144.3722252073379764 ) ) ;
#875=CARTESIAN_POINT ( 'NONE',  ( -10.09730733349775100, 33.57364382018241855, -143.4697625029285746 ) ) ;
#876=CARTESIAN_POINT ( 'NONE',  ( -29.36003260551135341, 40.56893091377379079, -146.2070596149844448 ) ) ;
#882=CARTESIAN_POINT ( 'NONE',  ( -22.09472268147270668, 35.57605554356849353, -147.3183388289436948 ) ) ;
#885=CARTESIAN_POINT ( 'NONE',  ( -22.68921981444905356, 38.61093386690951945, -140.6331873800498613 ) ) ;
#889=CARTESIAN_POINT ( 'NONE',  ( -9.953901651018769670, 37.05155446198870095, -148.5872971971928962 ) ) ;
#891=CARTESIAN_POINT ( 'NONE',  ( -8.547556706628435919, 40.01242579642496366, -142.2846414162569317 ) ) ;
#906=CARTESIAN_POINT ( 'NONE',  ( -18.36556700629002492, 41.35841174322762015, -144.3779443069900026 ) ) ;
#911=CARTESIAN_POINT ( 'NONE',  ( -24.30183382816920812, 35.51482525056968598, -147.3052200786065669 ) ) ;
#928=CARTESIAN_POINT ( 'NONE',  ( -6.518232409689999507, 33.41592120480000006, -146.1606736330000160 ) ) ;
#933=CARTESIAN_POINT ( 'NONE',  ( -9.971101149720000834, 37.05360750090000721, -147.8421425029999909 ) ) ;
#937=CARTESIAN_POINT ( 'NONE',  ( -17.71320442848650956, 38.77266098830207142, -148.1578736811549959 ) ) ;
#945=CARTESIAN_POINT ( 'NONE',  ( -14.80303414763277914, 37.74518406597707099, -140.0709723763587249 ) ) ;
#946=CARTESIAN_POINT ( 'NONE',  ( -26.23154108612487789, 35.99110338347298921, -139.4510183337245621 ) ) ;
#979=CARTESIAN_POINT ( 'NONE',  ( -16.20147620251679754, 33.40528963976247923, -143.4816615022228063 ) ) ;
#983=DIRECTION ( 'NONE',  ( -0.1185248058630065937, 0.9929510916430560608, 2.679939603570147632E-13 ) ) ;
#986=CARTESIAN_POINT ( 'NONE',  ( -9.685596112079144504, 34.85788159552594578, -146.7686248962264983 ) ) ;
#989=CARTESIAN_POINT ( 'NONE',  ( -24.97797643630000053, 37.05442817780000553, -147.8575004449999994 ) ) ;
#993=CARTESIAN_POINT ( 'NONE',  ( -28.80902675595255857, 36.08666534566612683, -139.5659208846137744 ) ) ;
#996=ORIENTED_EDGE ( 'NONE', *, *, #10115, .F. ) ;
#997=CARTESIAN_POINT ( 'NONE',  ( -13.92432874550000044, 37.01165864720000087, -139.5650670249999905 ) ) ;
#1001=CARTESIAN_POINT ( 'NONE',  ( -9.897232795978197828, 34.02093318812835321, -147.8794181089841118 ) ) ;
#1005=( NAMED_UNIT ( * ) PLANE_ANGLE_UNIT ( ) SI_UNIT ( $, .RADIAN. ) );
#1011=CARTESIAN_POINT ( 'NONE',  ( -6.990747311370722805, 33.54994435292839938, -144.4888610368732600 ) ) ;
#1020=CARTESIAN_POINT ( 'NONE',  ( -18.46720449282527454, 40.97819876959629681, -144.3328547432334119 ) ) ;
#1025=CARTESIAN_POINT ( 'NONE',  ( -24.57863953957676273, 33.12365565967444070, -146.2648171790582126 ) ) ;
#1046=CARTESIAN_POINT ( 'NONE',  ( -9.172004967711496093, 41.72460712644299008, -144.4785182484624784 ) ) ;
#1063=CARTESIAN_POINT ( 'NONE',  ( -14.58163105942842641, 36.93319896293559168, -139.6872257168839440 ) ) ;
#1064=CARTESIAN_POINT ( 'NONE',  ( -24.79371418826683993, 32.62011804915596258, -144.5039952333266058 ) ) ;
#1084=EDGE_CURVE ( 'NONE', #13908, #20921, #22689, .T. ) ;
#1099=CARTESIAN_POINT ( 'NONE',  ( -15.66251200267681831, 32.89188227335794323, -143.3406170289139254 ) ) ;
#1110=EDGE_CURVE ( 'NONE', #2371, #10397, #1593, .T. ) ;
#1114=CARTESIAN_POINT ( 'NONE',  ( -29.10972917886757116, 33.01395076712321952, -141.7686278616081950 ) ) ;
#1118=CARTESIAN_POINT ( 'NONE',  ( -13.30230152915278197, 36.27094684673078717, -140.3343369752782621 ) ) ;
#1122=EDGE_CURVE ( 'NONE', #14150, #6123, #4001, .T. ) ;
#1125=CARTESIAN_POINT ( 'NONE',  ( -9.667609713899818047, 35.97527138268016245, -148.7282639817501035 ) ) ;
#1129=ADVANCED_FACE ( 'NONE', ( #19115 ), #12963, .F. ) ;
#1133=FILL_AREA_STYLE ('',( #8586 ) ) ;
#1136=CARTESIAN_POINT ( 'NONE',  ( -6.728963506639928482, 33.26001575821830158, -144.4977132839956653 ) ) ;
#1146=CARTESIAN_POINT ( 'NONE',  ( -17.68978131337266291, 36.92028947728029920, -140.0842674916291628 ) ) ;
#1152=CARTESIAN_POINT ( 'NONE',  ( -24.16551117144435779, 36.07182940189623821, -148.2420083174796162 ) ) ;
#1155=CARTESIAN_POINT ( 'NONE',  ( -11.75883488016316214, 37.77601231981555685, -140.0882460024616876 ) ) ;
#1161=DIRECTION ( 'NONE',  ( 1.000000000000000000, 0.000000000000000000, 0.000000000000000000 ) ) ;
#1170=CARTESIAN_POINT ( 'NONE',  ( -19.14899212252498728, 37.07484167171551093, -147.8220480108043375 ) ) ;
#1171=FACE_OUTER_BOUND ( 'NONE', #10638, .T. ) ;
#1174=( BOUNDED_SURFACE ( )  B_SPLINE_SURFACE ( 5, 5, ( 
 ( #6524, #10195, #17596, #1063, #13791, #11624 ),
 ( #3087, #6399, #945, #22834, #18898, #8059 ),
 ( #19022, #2841, #15444, #6639, #20936, #17119 ),
 ( #22594, #23067, #8423, #21171, #6752, #21054 ),
 ( #13538, #11870, #17349, #13660, #20810, #22706 ),
 ( #4501, #11741, #2734, #9961, #17232, #17470 ),
 ( #15693, #10071, #22955, #4859, #12104, #19381 ),
 ( #10321, #10543, #21764, #12454, #12336, #4980 ),
 ( #19733, #10665, #21408, #14256, #7234, #12227 ),
 ( #5450, #15916, #3428, #1418, #18062, #3196 ),
 ( #14499, #12696, #19852, #16162, #23301, #10899 ),
 ( #19502, #16398, #8995, #16042, #19613, #1660 ) ),
 .UNSPECIFIED., .F., .F., .F. ) 
 B_SPLINE_SURFACE_WITH_KNOTS ( ( 6, 3, 3, 6 ),
 ( 6, 6 ),
 ( 0.000000000000000000, 4.151671928079999851, 8.316542232069998875, 12.50501063799999990 ),
 ( 1.570796326769924978, 3.141592653590000062 ),
 .UNSPECIFIED. ) 
 GEOMETRIC_REPRESENTATION_ITEM ( )  RATIONAL_B_SPLINE_SURFACE ( (
 ( 0.2500000000000000000, 0.2499999999968069986, 0.2999999999952105423, 0.3999999999936145190, 0.5999999999936139750, 1.000000000000000000),
 ( 0.2500000000000000000, 0.2499999999968069986, 0.2999999999952105423, 0.3999999999936145190, 0.5999999999936139750, 1.000000000000000000),
 ( 0.2500000000000000000, 0.2499999999968069986, 0.2999999999952105423, 0.3999999999936145190, 0.5999999999936139750, 1.000000000000000000),
 ( 0.2500000000000000000, 0.2499999999968069986, 0.2999999999952105423, 0.3999999999936145190, 0.5999999999936139750, 1.000000000000000000),
 ( 0.2500000000000000000, 0.2499999999968069986, 0.2999999999952105423, 0.3999999999936145190, 0.5999999999936139750, 1.000000000000000000),
 ( 0.2500000000000000000, 0.2499999999968069986, 0.2999999999952105423, 0.3999999999936145190, 0.5999999999936139750, 1.000000000000000000),
 ( 0.2500000000000000000, 0.2499999999968069986, 0.2999999999952105423, 0.3999999999936145190, 0.5999999999936139750, 1.000000000000000000),
 ( 0.2500000000000000000, 0.2499999999968069986, 0.2999999999952105423, 0.3999999999936145190, 0.5999999999936139750, 1.000000000000000000),
 ( 0.2500000000000000000, 0.2499999999968069986, 0.2999999999952105423, 0.3999999999936145190, 0.5999999999936139750, 1.000000000000000000),
 ( 0.2500000000000000000, 0.2499999999968069986, 0.2999999999952105423, 0.3999999999936145190, 0.5999999999936139750, 1.000000000000000000),
 ( 0.2500000000000000000, 0.2499999999968069986, 0.2999999999952105423, 0.3999999999936145190, 0.5999999999936139750, 1.000000000000000000),
 ( 0.2500000000000000000, 0.2499999999968069986, 0.2999999999952105423, 0.3999999999936145190, 0.5999999999936139750, 1.000000000000000000) ) ) 
 REPRESENTATION_ITEM ( '' )  SURFACE ( )  );
#1179=CARTESIAN_POINT ( 'NONE',  ( -28.80902675589999973, 36.08666534569999840, -139.5659208849999970 ) ) ;
#1196=CARTESIAN_POINT ( 'NONE',  ( -25.59027027610704508, 34.17788759730120063, -140.1904131873745314 ) ) ;
#1215=CARTESIAN_POINT ( 'NONE',  ( -15.17828643429606039, 39.13746915041387808, -146.9793796816204008 ) ) ;
#1220=CARTESIAN_POINT ( 'NONE',  ( -28.47499893025936046, 37.06529344306884610, -140.4421442387223635 ) ) ;
#1233=CARTESIAN_POINT ( 'NONE',  ( -9.244908380075797183, 34.43529505381081890, -147.2272989846510427 ) ) ;
#1237=CARTESIAN_POINT ( 'NONE',  ( -29.52942110880598037, 36.03607219280863916, -139.7545453072953023 ) ) ;
#1244=CARTESIAN_POINT ( 'NONE',  ( -23.41273968116292892, 40.49448598672354649, -143.7690349874483218 ) ) ;
#1248=VERTEX_POINT ( 'NONE', #15169 ) ;
#1249=CARTESIAN_POINT ( 'NONE',  ( -4.780317782130000914, 38.61135856239999953, -140.5115181619999873 ) ) ;
#1255=CARTESIAN_POINT ( 'NONE',  ( -8.208807763381100742, 34.49436158464779822, -140.8229124830248224 ) ) ;
#1264=EDGE_LOOP ( 'NONE', ( #18506, #9337, #16865, #8986 ) ) ;
#1268=CARTESIAN_POINT ( 'NONE',  ( -17.78691755432707566, 40.45100730230187480, -143.6151573293873298 ) ) ;
#1271=CARTESIAN_POINT ( 'NONE',  ( -6.093288228365017822, 36.94882630176448401, -147.6373263597673713 ) ) ;
#1272=CARTESIAN_POINT ( 'NONE',  ( -25.64408091310000160, 33.16124342930000068, -144.5387451670000019 ) ) ;
#1288=CARTESIAN_POINT ( 'NONE',  ( -9.483015687270000882, 40.53201449259999833, -146.0034198470000035 ) ) ;
#1290=CARTESIAN_POINT ( 'NONE',  ( -11.40498010996960332, 39.09966106399821228, -141.2721109090012419 ) ) ;
#1293=CARTESIAN_POINT ( 'NONE',  ( -7.427142538590000065, 36.18616221519999954, -139.9783837409999876 ) ) ;
#1294=CARTESIAN_POINT ( 'NONE',  ( -9.241517523749537943, 39.86784999477015390, -147.9446264559352926 ) ) ;
#1296=CARTESIAN_POINT ( 'NONE',  ( -28.14969746239999893, 32.41805236249999922, -143.4814202869999917 ) ) ;
#1299=ORIENTED_EDGE ( 'NONE', *, *, #1110, .F. ) ;
#1310=CARTESIAN_POINT ( 'NONE',  ( -25.30868096333427175, 35.35627366547125661, -147.9647939034089461 ) ) ;
#1312=( BOUNDED_SURFACE ( )  B_SPLINE_SURFACE ( 5, 5, ( 
 ( #12886, #22177, #2194, #2543, #11555, #18728 ),
 ( #16816, #2437, #9546, #22289, #528, #17042 ),
 ( #18602, #5978, #3972, #20511, #9765, #7761 ),
 ( #15026, #9654, #18833, #16929, #638, #20167 ),
 ( #4325, #7647, #9417, #7871, #3860, #2083 ),
 ( #20279, #4083, #16694, #15146, #5861, #18372 ),
 ( #22409, #6105, #20391, #7991, #409, #13360 ),
 ( #9301, #11095, #11321, #20630, #14918, #761 ),
 ( #15275, #16577, #285, #7527, #13120, #14802 ),
 ( #22063, #5751, #13009, #11205, #18479, #10125 ),
 ( #4556, #15845, #17399, #1118, #11918, #22888 ),
 ( #997, #3133, #11794, #19073, #17639, #1348 ) ),
 .UNSPECIFIED., .F., .F., .F. ) 
 B_SPLINE_SURFACE_WITH_KNOTS ( ( 6, 3, 3, 6 ),
 ( 6, 6 ),
 ( 0.000000000000000000, 4.066159495680000013, 8.252146144990000209, 12.56898909050000057 ),
 ( 0.000000000000000000, 1.570796326821630062 ),
 .UNSPECIFIED. ) 
 GEOMETRIC_REPRESENTATION_ITEM ( )  RATIONAL_B_SPLINE_SURFACE ( (
 ( 1.000000000000000000, 0.5999999999932189576, 0.3999999999932190020, 0.2999999999949140017, 0.2499999999966094899, 0.2500000000000000000),
 ( 1.000000000000000000, 0.5999999999932189576, 0.3999999999932190020, 0.2999999999949140017, 0.2499999999966094899, 0.2500000000000000000),
 ( 1.000000000000000000, 0.5999999999932189576, 0.3999999999932190020, 0.2999999999949140017, 0.2499999999966094899, 0.2500000000000000000),
 ( 1.000000000000000000, 0.5999999999932189576, 0.3999999999932190020, 0.2999999999949140017, 0.2499999999966094899, 0.2500000000000000000),
 ( 1.000000000000000000, 0.5999999999932189576, 0.3999999999932190020, 0.2999999999949140017, 0.2499999999966094899, 0.2500000000000000000),
 ( 1.000000000000000000, 0.5999999999932189576, 0.3999999999932190020, 0.2999999999949140017, 0.2499999999966094899, 0.2500000000000000000),
 ( 1.000000000000000000, 0.5999999999932189576, 0.3999999999932190020, 0.2999999999949140017, 0.2499999999966094899, 0.2500000000000000000),
 ( 1.000000000000000000, 0.5999999999932189576, 0.3999999999932190020, 0.2999999999949140017, 0.2499999999966094899, 0.2500000000000000000),
 ( 1.000000000000000000, 0.5999999999932189576, 0.3999999999932190020, 0.2999999999949140017, 0.2499999999966094899, 0.2500000000000000000),
 ( 1.000000000000000000, 0.5999999999932189576, 0.3999999999932190020, 0.2999999999949140017, 0.2499999999966094899, 0.2500000000000000000),
 ( 1.000000000000000000, 0.5999999999932189576, 0.3999999999932190020, 0.2999999999949140017, 0.2499999999966094899, 0.2500000000000000000),
 ( 1.000000000000000000, 0.5999999999932189576, 0.3999999999932190020, 0.2999999999949140017, 0.2499999999966094899, 0.2500000000000000000) ) ) 
 REPRESENTATION_ITEM ( '' )  SURFACE ( )  );
#1319=B_SPLINE_CURVE_WITH_KNOTS ( 'NONE', 5,
 ( #12966, #8913, #20244, #3936, #8801, #16196, #16078, #23448, #7144, #14409, #11403, #22487 ),
 .UNSPECIFIED., .F., .F.,
 ( 6, 3, 3, 6 ),
 ( 0.000000000000000000, 4.066159495680000013, 8.252146144990000209, 12.56898909049999880 ),
 .UNSPECIFIED. ) ;
#1325=CARTESIAN_POINT ( 'NONE',  ( -14.01363760658083457, 39.11235265668859995, -141.1958727404175136 ) ) ;
#1331=CARTESIAN_POINT ( 'NONE',  ( -10.88504013565279216, 37.01634837951832679, -139.4704149078483226 ) ) ;
#1334=CARTESIAN_POINT ( 'NONE',  ( -16.17668464575115195, 34.89952366001249828, -140.8770501902727119 ) ) ;
#1343=CARTESIAN_POINT ( 'NONE',  ( -25.17490547269999723, 35.46855981759999565, -147.6699473629999773 ) ) ;
#1345=CARTESIAN_POINT ( 'NONE',  ( -29.68301555210662102, 36.92109708053965988, -140.1550845752753105 ) ) ;
#1348=CARTESIAN_POINT ( 'NONE',  ( -14.11967125442052051, 36.98834135278355717, -140.5455248811183822 ) ) ;
#1354=CARTESIAN_POINT ( 'NONE',  ( -5.251527070960000820, 40.93408815870000694, -143.6492421949999994 ) ) ;
#1356=CARTESIAN_POINT ( 'NONE',  ( -8.564938780319947043, 40.19157471905271706, -145.9271927685878154 ) ) ;
#1360=CARTESIAN_POINT ( 'NONE',  ( -7.902404225063866861, 35.56594207916549522, -140.9322834864426852 ) ) ;
#1361=CARTESIAN_POINT ( 'NONE',  ( -5.459597139290000456, 36.94776568910000236, -139.8191173760000083 ) ) ;
#1372=CARTESIAN_POINT ( 'NONE',  ( -18.90246017567791270, 37.04541408822704796, -147.4848489022495528 ) ) ;
#1376=CARTESIAN_POINT ( 'NONE',  ( -16.92867099909999595, 34.38083942290000294, -140.2753207150000208 ) ) ;
#1382=CARTESIAN_POINT ( 'NONE',  ( -22.52780672251092042, 37.05898997718767873, -140.0074087193914067 ) ) ;
#1394=CARTESIAN_POINT ( 'NONE',  ( -12.13467478890487961, 40.69160539512103725, -144.5327625259997717 ) ) ;
#1396=CARTESIAN_POINT ( 'NONE',  ( -8.249050749313617814, 34.24288854963995732, -140.4966857150371595 ) ) ;
#1410=CARTESIAN_POINT ( 'NONE',  ( -19.69393976310000127, 37.84845892290000080, -140.3168504270000199 ) ) ;
#1415=CARTESIAN_POINT ( 'NONE',  ( -20.45144833149999997, 36.94873838139999833, -139.8044047869999815 ) ) ;
#1418=CARTESIAN_POINT ( 'NONE',  ( -15.96393590121257233, 38.83090064245826056, -147.9761310711117801 ) ) ;
#1421=CARTESIAN_POINT ( 'NONE',  ( -27.77832206610000298, 37.03059619289999915, -147.6270870419999710 ) ) ;
#1431=CARTESIAN_POINT ( 'NONE',  ( -25.54709891120000265, 36.13246793440000459, -139.7173810940000180 ) ) ;
#1440=CARTESIAN_POINT ( 'NONE',  ( -15.03885004549999849, 41.12207116019999376, -146.4108951270000034 ) ) ;
#1441=CARTESIAN_POINT ( 'NONE',  ( -28.71215957428060506, 38.99550079887305287, -140.7731748223484090 ) ) ;
#1448=ORIENTED_EDGE ( 'NONE', *, *, #5211, .F. ) ;
#1456=DIRECTION ( 'NONE',  ( 2.261079091466875261E-12, 0.000000000000000000, 1.000000000000000000 ) ) ;
#1473=CARTESIAN_POINT ( 'NONE',  ( -11.46682130719020876, 35.35929522821826509, -140.3232393995872087 ) ) ;
#1474=EDGE_CURVE ( 'NONE', #12438, #20510, #5173, .T. ) ;
#1475=CARTESIAN_POINT ( 'NONE',  ( -18.60901166350398483, 37.01038625230250290, -148.6497975989814506 ) ) ;
#1476=CARTESIAN_POINT ( 'NONE',  ( -8.764836022000000781, 39.53398178709999655, -147.5842891229999907 ) ) ;
#1480=ORIENTED_EDGE ( 'NONE', *, *, #5903, .T. ) ;
#1481=CARTESIAN_POINT ( 'NONE',  ( -6.901241125868466497, 36.34453081637710881, -147.4362978685941528 ) ) ;
#1487=CARTESIAN_POINT ( 'NONE',  ( -5.480550747686820046, 36.94526453639213059, -140.5641745855346301 ) ) ;
#1508=CARTESIAN_POINT ( 'NONE',  ( -23.43027330800707730, 37.94004033882730198, -139.4495095434923826 ) ) ;
#1514=CARTESIAN_POINT ( 'NONE',  ( -15.57786843150000067, 37.00666880280000726, -148.5521201120000114 ) ) ;
#1519=CARTESIAN_POINT ( 'NONE',  ( -9.771488485180000794, 38.65068379619999916, -147.6127673909999771 ) ) ;
#1520=CARTESIAN_POINT ( 'NONE',  ( -11.27392315527871602, 41.29449409377051694, -144.7140135096667848 ) ) ;
#1542=CARTESIAN_POINT ( 'NONE',  ( -21.54058924440989742, 34.11652205135742832, -147.8735334098300029 ) ) ;
#1551=CARTESIAN_POINT ( 'NONE',  ( -26.59168384020000175, 38.48554521319999822, -140.5676127940000129 ) ) ;
#1559=CARTESIAN_POINT ( 'NONE',  ( -12.95309207270000051, 35.58606224190000233, -147.4460499719999689 ) ) ;
#1567=CARTESIAN_POINT ( 'NONE',  ( -13.69605334181871115, 39.31347921127435541, -140.9805954651069158 ) ) ;
#1568=CARTESIAN_POINT ( 'NONE',  ( -29.25462571399999590, 37.92445966660000778, -140.5403777589999947 ) ) ;
#1580=CARTESIAN_POINT ( 'NONE',  ( -4.712143453930511150, 38.89658459788447686, -139.8814980668870760 ) ) ;
#1582=CARTESIAN_POINT ( 'NONE',  ( -23.71856152630000025, 38.62313066519999438, -140.3058339320000130 ) ) ;
#1593=( BOUNDED_CURVE ( )  B_SPLINE_CURVE ( 5, ( #12206, #14120, #17685, #2938, #22936, #10410, #4719, #3176, #10299, #21388, #5074, #8514 ),
 .UNSPECIFIED., .F., .F. ) 
 B_SPLINE_CURVE_WITH_KNOTS ( ( 6, 3, 3, 6 ),
 ( 0.000000000000000000, 4.059123295939999210, 8.340116530639999581, 12.86134770560000007 ),
 .UNSPECIFIED. ) 
 CURVE ( )  GEOMETRIC_REPRESENTATION_ITEM ( )  RATIONAL_B_SPLINE_CURVE ( ( 0.2500000000000000000, 0.2500000000000000000, 0.2500000000000000000, 0.2500000000000000000, 0.2500000000000000000, 0.2500000000000000000, 0.2500000000000000000, 0.2500000000000000000, 0.2500000000000000000, 0.2500000000000000000, 0.2500000000000000000, 0.2500000000000000000 ) ) 
 REPRESENTATION_ITEM ( '' )  );
#1595=CARTESIAN_POINT ( 'NONE',  ( -29.25462571399999590, 37.92445966660000778, -140.5403777589999947 ) ) ;
#1599=CARTESIAN_POINT ( 'NONE',  ( -10.46662683120000104, 35.31824366040000029, -139.9138328150000063 ) ) ;
#1601=CARTESIAN_POINT ( 'NONE',  ( -18.32340570184511463, 36.04493404334465367, -148.6528109212497952 ) ) ;
#1607=SHAPE_REPRESENTATION_RELATIONSHIP ( 'NONE' , 'NONE' ,  #2821, #19731 ) ;
#1625=CARTESIAN_POINT ( 'NONE',  ( -15.90559286389999905, 34.15404988380000617, -147.7469703310000000 ) ) ;
#1635=CARTESIAN_POINT ( 'NONE',  ( -28.04360111912153286, 34.66455527868549069, -140.6572026283309640 ) ) ;
#1641=CARTESIAN_POINT ( 'NONE',  ( -20.21101409811915772, 36.97743810397759745, -140.7155889590012237 ) ) ;
#1655=CARTESIAN_POINT ( 'NONE',  ( -18.48412402389261544, 36.99547888839300214, -147.4161207264765778 ) ) ;
#1660=CARTESIAN_POINT ( 'NONE',  ( -15.57786843150000067, 37.00666880280000726, -148.5521201120000114 ) ) ;
#1666=CARTESIAN_POINT ( 'NONE',  ( -27.04496201379999931, 40.71797592360000095, -143.5957174049999878 ) ) ;
#1668=ORIENTED_EDGE ( 'NONE', *, *, #14006, .F. ) ;
#1673=ORIENTED_EDGE ( 'NONE', *, *, #5958, .F. ) ;
#1676=CARTESIAN_POINT ( 'NONE',  ( -13.21931118290000029, 33.83281470429999871, -146.0365350580000268 ) ) ;
#1679=CARTESIAN_POINT ( 'NONE',  ( -11.26413364438170106, 36.97109742516077802, -139.4278719022366317 ) ) ;
#1680=CARTESIAN_POINT ( 'NONE',  ( -14.35287446704815473, 40.57630474357829797, -143.6962090187504373 ) ) ;
#1696=CARTESIAN_POINT ( 'NONE',  ( -5.475508280718690557, 38.87484624601071914, -139.7033240574601223 ) ) ;
#1701=CARTESIAN_POINT ( 'NONE',  ( -15.46613156839999981, 36.99333119719999985, -147.5584717940000132 ) ) ;
#1704=CARTESIAN_POINT ( 'NONE',  ( -24.06602356359999817, 36.94557182220000158, -148.2530914610000252 ) ) ;
#1706=CARTESIAN_POINT ( 'NONE',  ( -24.87949572109999963, 37.83967983510000010, -147.8465544160000036 ) ) ;
#1707=CARTESIAN_POINT ( 'NONE',  ( -29.64895016830000429, 40.48034887659999725, -142.7934167989999992 ) ) ;
#1711=PRESENTATION_STYLE_ASSIGNMENT (( #1825 ) ) ;
#1712=CARTESIAN_POINT ( 'NONE',  ( -19.70924662384209824, 34.96809591615225088, -139.6648745877703846 ) ) ;
#1714=CARTESIAN_POINT ( 'NONE',  ( -9.483015687316079578, 40.53201449268256340, -146.0034198473055937 ) ) ;
#1727=CARTESIAN_POINT ( 'NONE',  ( -5.459597139462840865, 36.94776568914183912, -139.8191173758248169 ) ) ;
#1747=CARTESIAN_POINT ( 'NONE',  ( -13.30167158631291358, 35.54685148874143863, -147.6446058646477013 ) ) ;
#1754=CARTESIAN_POINT ( 'NONE',  ( -11.99109128264890423, 36.93662743998119424, -148.3295785879899427 ) ) ;
#1769=CARTESIAN_POINT ( 'NONE',  ( -20.08037650829999876, 40.50744741009999927, -142.1449807700000179 ) ) ;
#1775=CARTESIAN_POINT ( 'NONE',  ( -21.73420140653708543, 36.02043114307134175, -148.7219678492595278 ) ) ;
#1809=CARTESIAN_POINT ( 'NONE',  ( -6.397971003482101793, 41.16484389488864792, -146.3678220594143795 ) ) ;
#1818=CARTESIAN_POINT ( 'NONE',  ( -24.97797643630000053, 37.05442817780000553, -147.8575004449999994 ) ) ;
#1820=CARTESIAN_POINT ( 'NONE',  ( -23.86695901012427967, 38.68196870791431508, -148.0474502905817928 ) ) ;
#1821=CARTESIAN_POINT ( 'NONE',  ( -30.15470591354345586, 40.57106738518383082, -144.2503661066654956 ) ) ;
#1825=SURFACE_STYLE_USAGE ( .BOTH. , #20020 ) ;
#1827=CARTESIAN_POINT ( 'NONE',  ( -18.86860405549940012, 33.24829707042102456, -142.0020245836044239 ) ) ;
#1829=CARTESIAN_POINT ( 'NONE',  ( -9.971101149792001905, 37.05360750094371980, -147.8421425034861727 ) ) ;
#1865=CARTESIAN_POINT ( 'NONE',  ( -12.86016529610566117, 36.30837334279895146, -147.6243440205185777 ) ) ;
#1870=CARTESIAN_POINT ( 'NONE',  ( -19.50275481447760484, 33.54643882699141244, -144.6274805566119426 ) ) ;
#1871=CARTESIAN_POINT ( 'NONE',  ( -11.57042140271139985, 39.24233794802490394, -147.3928844070919126 ) ) ;
#1891=CARTESIAN_POINT ( 'NONE',  ( -26.16983372450180312, 40.98399646778832306, -141.7700373849442030 ) ) ;
#1893=CARTESIAN_POINT ( 'NONE',  ( -22.14393879224838813, 35.16037992174653937, -148.2535502083404140 ) ) ;
#1899=CARTESIAN_POINT ( 'NONE',  ( -27.10979229004369628, 41.68302333980914653, -143.4785537008253868 ) ) ;
#1905=CARTESIAN_POINT ( 'NONE',  ( -10.50683292394248092, 35.68768245788039906, -140.8109541216290950 ) ) ;
#1910=ORIENTED_EDGE ( 'NONE', *, *, #5021, .F. ) ;
#1916=CARTESIAN_POINT ( 'NONE',  ( -15.07147389518837954, 36.94622240756218901, -147.6034838242705973 ) ) ;
#1917=CARTESIAN_POINT ( 'NONE',  ( -29.82391180389999619, 40.55477172079999804, -144.2881336360000262 ) ) ;
#1934=CARTESIAN_POINT ( 'NONE',  ( -5.762834418027599881, 39.50865942494267813, -140.4825946863184072 ) ) ;
#1943=( BOUNDED_CURVE ( )  B_SPLINE_CURVE ( 5, ( #12719, #14395, #20233, #11160, #7016, #3926 ),
 .UNSPECIFIED., .F., .F. ) 
 B_SPLINE_CURVE_WITH_KNOTS ( ( 6, 6 ),
 ( 1.570796327036584783, 3.141592653590000062 ),
 .UNSPECIFIED. ) 
 CURVE ( )  GEOMETRIC_REPRESENTATION_ITEM ( )  RATIONAL_B_SPLINE_CURVE ( ( 0.2500000000000000000, 0.2500000000307595616, 0.3000000000461393035, 0.4000000000615190898, 0.6000000000615191009, 1.000000000000000000 ) ) 
 REPRESENTATION_ITEM ( '' )  );
#1946=CARTESIAN_POINT ( 'NONE',  ( -24.31357332192622778, 38.37299497772424672, -147.2056731264148084 ) ) ;
#1952=CARTESIAN_POINT ( 'NONE',  ( -19.18314309878111956, 35.27735355289885177, -140.1794542500113039 ) ) ;
#1962=CARTESIAN_POINT ( 'NONE',  ( -6.608289563844804704, 38.45937946434654009, -147.2295807508219525 ) ) ;
#1976=CARTESIAN_POINT ( 'NONE',  ( -17.22605506639999717, 36.97564272059999979, -139.5994799229999899 ) ) ;
#1985=CARTESIAN_POINT ( 'NONE',  ( -17.37032063983712860, 35.50980293810385291, -140.6805347145502196 ) ) ;
#1996=CARTESIAN_POINT ( 'NONE',  ( -19.79103853767445287, 33.24264095657647999, -144.7076267160936140 ) ) ;
#2003=CARTESIAN_POINT ( 'NONE',  ( -28.00347998534502736, 37.05747243975537231, -148.5422211674043353 ) ) ;
#2012=CARTESIAN_POINT ( 'NONE',  ( -25.58569844857837339, 38.74756584344044796, -140.2713792647305411 ) ) ;
#2015=CARTESIAN_POINT ( 'NONE',  ( -22.71761275429354754, 35.08418826686737901, -139.6199258849947000 ) ) ;
#2026=CARTESIAN_POINT ( 'NONE',  ( -10.46662683120000104, 35.31824366040000029, -139.9138328150000063 ) ) ;
#2029=CARTESIAN_POINT ( 'NONE',  ( -12.86016529629999994, 36.30837334279999595, -147.6243440209999847 ) ) ;
#2049=CARTESIAN_POINT ( 'NONE',  ( -5.584341313528829787, 39.74112841659670892, -140.1950701786490185 ) ) ;
#2059=FACE_OUTER_BOUND ( 'NONE', #23094, .T. ) ;
#2060=CARTESIAN_POINT ( 'NONE',  ( -22.33063748469999865, 35.38828378200000202, -140.2025093959999822 ) ) ;
#2064=CARTESIAN_POINT ( 'NONE',  ( -18.36995524497817200, 33.45442790097475694, -146.2078216622589366 ) ) ;
#2071=CARTESIAN_POINT ( 'NONE',  ( -16.05159040817519056, 32.28373075711905926, -144.3107489965007062 ) ) ;
#2077=CARTESIAN_POINT ( 'NONE',  ( -7.010349701995939320, 37.05829245175783626, -148.1453878980124159 ) ) ;
#2083=CARTESIAN_POINT ( 'NONE',  ( -13.21931118294300056, 33.83281470423892046, -146.0365350582607959 ) ) ;
#2092=UNCERTAINTY_MEASURE_WITH_UNIT (LENGTH_MEASURE( 1.000000000000000082E-05 ), #8479, 'distance_accuracy_value', 'NONE');
#2103=CARTESIAN_POINT ( 'NONE',  ( -20.31217984471907556, 37.68760996765858806, -140.7108956903404362 ) ) ;
#2107=CARTESIAN_POINT ( 'NONE',  ( -23.90890255115609264, 36.92681688280359964, -147.8857207495020418 ) ) ;
#2115=CARTESIAN_POINT ( 'NONE',  ( -26.09271177668468056, 41.23383702271284790, -143.6447300367354671 ) ) ;
#2117=CARTESIAN_POINT ( 'NONE',  ( -22.25912899098128861, 34.38362928960210496, -140.2961181449622643 ) ) ;
#2118=VERTEX_POINT ( 'NONE', #18682 ) ;
#2123=CARTESIAN_POINT ( 'NONE',  ( -27.48801997220000004, 39.21796412529999998, -147.0196846460000017 ) ) ;
#2130=CARTESIAN_POINT ( 'NONE',  ( -10.24284460795958474, 35.44041190389086182, -140.1367555553470083 ) ) ;
#2131=CARTESIAN_POINT ( 'NONE',  ( -8.325889011996979505, 41.57695941999546108, -143.5717776959861567 ) ) ;
#2142=CARTESIAN_POINT ( 'NONE',  ( -11.69788097216356171, 37.87433970954386098, -139.6673822189363818 ) ) ;
#2144=CARTESIAN_POINT ( 'NONE',  ( -17.53224077489999999, 39.64394931100000008, -140.2973660050000149 ) ) ;
#2145=CARTESIAN_POINT ( 'NONE',  ( -30.02199999990000023, 40.03108891319999429, -145.8052959529999839 ) ) ;
#2154=CARTESIAN_POINT ( 'NONE',  ( -21.06565549771221413, 41.62781742176859723, -143.5964485135013433 ) ) ;
#2156=CARTESIAN_POINT ( 'NONE',  ( -28.03429568402808059, 32.40695676816267934, -144.4586890253928004 ) ) ;
#2165=( BOUNDED_CURVE ( )  B_SPLINE_CURVE ( 5, ( #19574, #19333, #8956, #3044, #23260, #3161 ),
 .UNSPECIFIED., .F., .F. ) 
 B_SPLINE_CURVE_WITH_KNOTS ( ( 6, 6 ),
 ( 1.570796326630344186, 3.141592653590000062 ),
 .UNSPECIFIED. ) 
 CURVE ( )  GEOMETRIC_REPRESENTATION_ITEM ( )  RATIONAL_B_SPLINE_CURVE ( ( 0.2500000000000000555, 0.2499999999790353811, 0.2999999999685530883, 0.3999999999580707288, 0.5999999999580707399, 1.000000000000000000 ) ) 
 REPRESENTATION_ITEM ( '' )  );
#2169=CARTESIAN_POINT ( 'NONE',  ( -23.22224815339999893, 34.57381638260000045, -140.7548632179999970 ) ) ;
#2175=CARTESIAN_POINT ( 'NONE',  ( -20.13043194029999938, 34.25277599949999541, -140.5881547479999938 ) ) ;
#2178=CARTESIAN_POINT ( 'NONE',  ( -24.21201708719999957, 40.99356323119999956, -143.6328343570000072 ) ) ;
#2179=CARTESIAN_POINT ( 'NONE',  ( -14.84561440076392458, 36.91926241633398575, -147.9647079511927927 ) ) ;
#2186=CARTESIAN_POINT ( 'NONE',  ( -5.941327522415615903, 39.27619043351264594, -140.7701191936981218 ) ) ;
#2187=ORIENTED_EDGE ( 'NONE', *, *, #11432, .F. ) ;
#2192=CARTESIAN_POINT ( 'NONE',  ( -24.32282749495824703, 36.01414085272633514, -148.6131980735590901 ) ) ;
#2194=CARTESIAN_POINT ( 'NONE',  ( -11.85909339608079094, 36.92087135288664967, -147.9691652862316857 ) ) ;
#2204=( BOUNDED_CURVE ( )  B_SPLINE_CURVE ( 5, ( #23313, #2029, #1559, #7362, #1676, #14622, #19626, #7006, #14156, #5465, #12823, #16294 ),
 .UNSPECIFIED., .F., .F. ) 
 B_SPLINE_CURVE_WITH_KNOTS ( ( 6, 3, 3, 6 ),
 ( 0.000000000000000000, 4.066159495680000013, 8.252146144990000209, 12.56898909049999880 ),
 .UNSPECIFIED. ) 
 CURVE ( )  GEOMETRIC_REPRESENTATION_ITEM ( )  RATIONAL_B_SPLINE_CURVE ( ( 0.2500000000000000000, 0.2500000000000000000, 0.2500000000000000000, 0.2500000000000000000, 0.2500000000000000000, 0.2500000000000000000, 0.2500000000000000000, 0.2500000000000000000, 0.2500000000000000000, 0.2500000000000000000, 0.2500000000000000000, 0.2500000000000000000 ) ) 
 REPRESENTATION_ITEM ( '' )  );
#2209=CARTESIAN_POINT ( 'NONE',  ( -13.80638726114959169, 32.41177233165633709, -143.7882581758906611 ) ) ;
#2219=CARTESIAN_POINT ( 'NONE',  ( -21.50444101780000139, 40.78041997809999941, -146.2395182369999986 ) ) ;
#2224=FACE_OUTER_BOUND ( 'NONE', #14982, .T. ) ;
#2232=CARTESIAN_POINT ( 'NONE',  ( -26.20001943430085589, 40.80945677298473129, -144.5049606645992242 ) ) ;
#2234=CARTESIAN_POINT ( 'NONE',  ( -22.43192306081355269, 32.22142746413794612, -144.5072135593746623 ) ) ;
#2240=CARTESIAN_POINT ( 'NONE',  ( -29.29455083643873436, 36.96746664034499474, -139.4767999531160569 ) ) ;
#2244=CARTESIAN_POINT ( 'NONE',  ( -6.938784185764153456, 37.04974994750939032, -148.5388410751212120 ) ) ;
#2256=CARTESIAN_POINT ( 'NONE',  ( -12.47185022218380723, 37.93970414752843823, -148.6532233943605661 ) ) ;
#2259=CARTESIAN_POINT ( 'NONE',  ( -29.13556667879501560, 41.19822702818812132, -144.4115419828412996 ) ) ;
#2260=ORIENTED_EDGE ( 'NONE', *, *, #9977, .T. ) ;
#2266=CARTESIAN_POINT ( 'NONE',  ( -28.50747929780000334, 33.37084171139999711, -143.6371486329999811 ) ) ;
#2270=CARTESIAN_POINT ( 'NONE',  ( -20.43858045619872144, 40.80995393214885780, -146.3951808076467955 ) ) ;
#2303=CARTESIAN_POINT ( 'NONE',  ( -24.99548980007219612, 37.05651868163715790, -148.5304149358840675 ) ) ;
#2304=CARTESIAN_POINT ( 'NONE',  ( -15.37195868313349045, 34.69747584690560416, -146.9441783042220493 ) ) ;
#2314=CARTESIAN_POINT ( 'NONE',  ( -6.194210391756115541, 38.39815610428787807, -147.2141978122577939 ) ) ;
#2320=FACE_OUTER_BOUND ( 'NONE', #1264, .T. ) ;
#2348=( BOUNDED_SURFACE ( )  B_SPLINE_SURFACE ( 5, 5, ( 
 ( #9323, #22086, #13382, #12910, #20531, #3887 ),
 ( #7551, #18392, #2103, #22308, #4105, #14827 ),
 ( #550, #22199, #9567, #658, #20193, #4343 ),
 ( #8013, #9440, #16596, #310, #5774, #20412 ),
 ( #4232, #11577, #6125, #2564, #11467, #17065 ),
 ( #787, #15295, #7783, #22551, #13033, #15050 ),
 ( #6003, #9675, #20304, #3994, #11227, #16951 ),
 ( #7891, #15171, #22430, #18500, #5886, #2219 ),
 ( #16717, #432, #7670, #14939, #13741, #3156 ),
 ( #15520, #12057, #21005, #10386, #6592, #22781 ),
 ( #22908, #2799, #19458, #6480, #4697, #20765 ),
 ( #13611, #19328, #17662, #4935, #9913, #8490 ) ),
 .UNSPECIFIED., .F., .F., .F. ) 
 B_SPLINE_SURFACE_WITH_KNOTS ( ( 6, 3, 3, 6 ),
 ( 6, 6 ),
 ( 0.000000000000000000, 4.390059406679999832, 8.746277600790000051, 13.07048654049999925 ),
 ( 1.570796326526080033, 3.141592653590000062 ),
 .UNSPECIFIED. ) 
 GEOMETRIC_REPRESENTATION_ITEM ( )  RATIONAL_B_SPLINE_SURFACE ( (
 ( 0.2500000000000000000, 0.2499999999657600003, 0.2999999999486395175, 0.3999999999315194676, 0.5999999999315199783, 1.000000000000000000),
 ( 0.2500000000000000000, 0.2499999999657600003, 0.2999999999486395175, 0.3999999999315194676, 0.5999999999315199783, 1.000000000000000000),
 ( 0.2500000000000000000, 0.2499999999657600003, 0.2999999999486395175, 0.3999999999315194676, 0.5999999999315199783, 1.000000000000000000),
 ( 0.2500000000000000000, 0.2499999999657600003, 0.2999999999486395175, 0.3999999999315194676, 0.5999999999315199783, 1.000000000000000000),
 ( 0.2500000000000000000, 0.2499999999657600003, 0.2999999999486395175, 0.3999999999315194676, 0.5999999999315199783, 1.000000000000000000),
 ( 0.2500000000000000000, 0.2499999999657600003, 0.2999999999486395175, 0.3999999999315194676, 0.5999999999315199783, 1.000000000000000000),
 ( 0.2500000000000000000, 0.2499999999657600003, 0.2999999999486395175, 0.3999999999315194676, 0.5999999999315199783, 1.000000000000000000),
 ( 0.2500000000000000000, 0.2499999999657600003, 0.2999999999486395175, 0.3999999999315194676, 0.5999999999315199783, 1.000000000000000000),
 ( 0.2500000000000000000, 0.2499999999657600003, 0.2999999999486395175, 0.3999999999315194676, 0.5999999999315199783, 1.000000000000000000),
 ( 0.2500000000000000000, 0.2499999999657600003, 0.2999999999486395175, 0.3999999999315194676, 0.5999999999315199783, 1.000000000000000000),
 ( 0.2500000000000000000, 0.2499999999657600003, 0.2999999999486395175, 0.3999999999315194676, 0.5999999999315199783, 1.000000000000000000),
 ( 0.2500000000000000000, 0.2499999999657600003, 0.2999999999486395175, 0.3999999999315194676, 0.5999999999315199783, 1.000000000000000000) ) ) 
 REPRESENTATION_ITEM ( '' )  SURFACE ( )  );
#2356=CARTESIAN_POINT ( 'NONE',  ( -25.46206384012266710, 37.06683745572687627, -140.4480127386052004 ) ) ;
#2359=CARTESIAN_POINT ( 'NONE',  ( -22.33063748467256104, 35.38828378206188319, -140.2025093961515836 ) ) ;
#2370=CARTESIAN_POINT ( 'NONE',  ( -7.529689113779999943, 37.05876528330000497, -139.9906690790000141 ) ) ;
#2371=VERTEX_POINT ( 'NONE', #21854 ) ;
#2379=CARTESIAN_POINT ( 'NONE',  ( -10.76224745929999926, 37.97907322949999553, -139.7231730900000173 ) ) ;
#2380=CARTESIAN_POINT ( 'NONE',  ( -17.39663711204255492, 40.51543712901364103, -146.0950904568249484 ) ) ;
#2381=CARTESIAN_POINT ( 'NONE',  ( -29.19363900808597734, 40.77773483849115621, -144.3769002367588428 ) ) ;
#2390=CARTESIAN_POINT ( 'NONE',  ( -21.80913741070000000, 38.74859698539999897, -147.9243209519999880 ) ) ;
#2392=ORIENTED_EDGE ( 'NONE', *, *, #826, .F. ) ;
#2394=CARTESIAN_POINT ( 'NONE',  ( -27.97684248819999908, 35.51254237909999745, -147.4365014880000047 ) ) ;
#2406=ORIENTED_EDGE ( 'NONE', *, *, #4979, .T. ) ;
#2411=CARTESIAN_POINT ( 'NONE',  ( -18.85469010170000459, 37.03971195569999963, -148.4264296979999926 ) ) ;
#2415=CARTESIAN_POINT ( 'NONE',  ( -8.238646733050000392, 41.24792906369999912, -143.6196368420000056 ) ) ;
#2418=CARTESIAN_POINT ( 'NONE',  ( -9.801780388952463952, 37.03339632390886038, -147.4803110668171939 ) ) ;
#2420=CARTESIAN_POINT ( 'NONE',  ( -23.68820627306414295, 41.09826978516893092, -146.5293788421483043 ) ) ;
#2422=CARTESIAN_POINT ( 'NONE',  ( -17.13033207850000039, 36.08498863180000171, -139.6042211940000186 ) ) ;
#2428=CARTESIAN_POINT ( 'NONE',  ( -4.933950775581154247, 38.47208611112608878, -140.7832461089165292 ) ) ;
#2434=CARTESIAN_POINT ( 'NONE',  ( -21.50145757605700325, 36.99754792876502307, -147.3684231709873416 ) ) ;
#2437=CARTESIAN_POINT ( 'NONE',  ( -12.08777119465849559, 36.07243015074993764, -148.3170434184952740 ) ) ;
#2441=CARTESIAN_POINT ( 'NONE',  ( -26.86963863710371925, 36.92213009831747428, -147.8538433455847496 ) ) ;
#2448=CARTESIAN_POINT ( 'NONE',  ( -13.88194885162993408, 32.82503397475245066, -144.7298409786526747 ) ) ;
#2458=B_SPLINE_CURVE_WITH_KNOTS ( 'NONE', 5,
 ( #989, #17745, #1343, #21330, #22990, #15839, #6676, #23104, #14062, #11910, #5022, #4783 ),
 .UNSPECIFIED., .F., .F.,
 ( 6, 3, 3, 6 ),
 ( 0.000000000000000000, 4.454241660750000165, 8.943513424000000711, 13.47090878500000066 ),
 .UNSPECIFIED. ) ;
#2470=CARTESIAN_POINT ( 'NONE',  ( -23.34852387253397765, 35.17565678551333974, -140.0195222351592861 ) ) ;
#2475=CARTESIAN_POINT ( 'NONE',  ( -27.50477442134641493, 37.98689587843293936, -148.6879642405163224 ) ) ;
#2476=CARTESIAN_POINT ( 'NONE',  ( -14.83278250959999944, 40.60058613829999530, -144.4189779529999953 ) ) ;
#2479=CARTESIAN_POINT ( 'NONE',  ( -7.506111428155179510, 33.37436714669472337, -146.3147224701790208 ) ) ;
#2485=CARTESIAN_POINT ( 'NONE',  ( -24.22314457607385663, 36.96432676151306396, -148.6204621725955235 ) ) ;
#2488=CARTESIAN_POINT ( 'NONE',  ( -13.01389323884992066, 37.83362044807778801, -147.7995900185891003 ) ) ;
#2490=CARTESIAN_POINT ( 'NONE',  ( -23.41786221899999987, 36.12684018730000446, -140.1150171360000058 ) ) ;
#2500=CARTESIAN_POINT ( 'NONE',  ( -20.36280570458463757, 40.92149091583824116, -144.5882336176433967 ) ) ;
#2502=CARTESIAN_POINT ( 'NONE',  ( -27.69172573212000543, 35.55337010885431681, -147.2624953929817480 ) ) ;
#2509=CARTESIAN_POINT ( 'NONE',  ( -10.75221293960000146, 33.20739279120000020, -143.4848104349999858 ) ) ;
#2527=ADVANCED_FACE ( 'NONE', ( #11686 ), #19088, .T. ) ;
#2529=CARTESIAN_POINT ( 'NONE',  ( -17.22605506639999717, 36.97564272059999979, -139.5994799229999899 ) ) ;
#2535=CARTESIAN_POINT ( 'NONE',  ( -9.518386210255387780, 33.60980554410204491, -145.7502876509803684 ) ) ;
#2539=CARTESIAN_POINT ( 'NONE',  ( -22.27877656138748463, 35.45284992532844370, -147.6448678430727455 ) ) ;
#2543=CARTESIAN_POINT ( 'NONE',  ( -12.02450515624455640, 36.94061592734299637, -147.5849826166407013 ) ) ;
#2545=CARTESIAN_POINT ( 'NONE',  ( -14.93328160137761706, 36.92972691758931347, -148.3740393307602972 ) ) ;
#2548=CARTESIAN_POINT ( 'NONE',  ( -8.613431449198317935, 37.75849558882340062, -140.1079839310028206 ) ) ;
#2555=CARTESIAN_POINT ( 'NONE',  ( -14.03815736070903597, 32.86934428549125187, -141.8938335452860997 ) ) ;
#2564=CARTESIAN_POINT ( 'NONE',  ( -21.02182045561234247, 40.23839372147724447, -142.1761255659782250 ) ) ;
#2568=CARTESIAN_POINT ( 'NONE',  ( -18.19668323639750440, 39.07774783162744825, -146.8458198118272549 ) ) ;
#2571=CARTESIAN_POINT ( 'NONE',  ( -23.51619327739999932, 36.94101002280000046, -140.1031831869999849 ) ) ;
#2572=CARTESIAN_POINT ( 'NONE',  ( -24.94615679292102683, 36.31107517788785799, -147.5592587911377791 ) ) ;
#2586=ORIENTED_EDGE ( 'NONE', *, *, #344, .F. ) ;
#2587=CARTESIAN_POINT ( 'NONE',  ( -27.39837063315040311, 38.96261900911265030, -148.4292450421148715 ) ) ;
#2590=CARTESIAN_POINT ( 'NONE',  ( -10.79374130943622134, 37.77220497676849931, -140.6646249280453844 ) ) ;
#2591=CARTESIAN_POINT ( 'NONE',  ( -6.472921198530737996, 34.24272888346551724, -147.8944248432848099 ) ) ;
#2592=CARTESIAN_POINT ( 'NONE',  ( -9.302015002957228162, 41.36125941937655881, -143.4861728416109088 ) ) ;
#2596=CARTESIAN_POINT ( 'NONE',  ( -14.70358821722507159, 36.91864139955099233, -140.0875527721395599 ) ) ;
#2599=EDGE_LOOP ( 'NONE', ( #16523, #22024, #4791, #18185 ) ) ;
#2606=CARTESIAN_POINT ( 'NONE',  ( -21.12162747683233377, 36.95220905038714676, -147.5578847870536947 ) ) ;
#2610=CARTESIAN_POINT ( 'NONE',  ( -19.54668701386443885, 37.05673630843094202, -139.5622637237091226 ) ) ;
#2613=CARTESIAN_POINT ( 'NONE',  ( -28.37659674026075862, 36.31875307945076514, -140.4290075092151824 ) ) ;
#2623=CARTESIAN_POINT ( 'NONE',  ( -10.17933436569999905, 35.38122503049999779, -147.6311798959999919 ) ) ;
#2634=CARTESIAN_POINT ( 'NONE',  ( -13.73025257492641060, 37.03482478361183183, -140.6242165752723565 ) ) ;
#2643=CARTESIAN_POINT ( 'NONE',  ( -24.11597423730821177, 41.68006656443377267, -143.5803335156247158 ) ) ;
#2644=CARTESIAN_POINT ( 'NONE',  ( -16.54277457355827963, 34.95491693754559748, -141.0331736024876079 ) ) ;
#2647=CARTESIAN_POINT ( 'NONE',  ( -20.45144833149999997, 36.94873838139999833, -139.8044047869999815 ) ) ;
#2652=CARTESIAN_POINT ( 'NONE',  ( -9.944031889410000602, 32.62729151690000151, -143.2983400859999961 ) ) ;
#2660=CARTESIAN_POINT ( 'NONE',  ( -21.99818215266191501, 36.31189858315303098, -147.5072904936844509 ) ) ;
#2663=CARTESIAN_POINT ( 'NONE',  ( -24.21201708719999957, 40.99356323119999956, -143.6328343570000072 ) ) ;
#2674=CARTESIAN_POINT ( 'NONE',  ( -28.00347998531936966, 37.05747243975231697, -148.5422211674587629 ) ) ;
#2677=CARTESIAN_POINT ( 'NONE',  ( -14.03631397270657999, 35.00148697007204390, -139.7760274526582407 ) ) ;
#2678=CARTESIAN_POINT ( 'NONE',  ( -25.64792992860000354, 37.04465132570000208, -139.7265440090000084 ) ) ;
#2683=CARTESIAN_POINT ( 'NONE',  ( -14.02405267930000043, 37.94700976039999318, -139.5674429869999926 ) ) ;
#2687=CARTESIAN_POINT ( 'NONE',  ( -18.64767072899999789, 38.89869937459999960, -148.1651290810000319 ) ) ;
#2692=CARTESIAN_POINT ( 'NONE',  ( -26.10314130450000292, 34.70878586860000325, -141.0128996759999893 ) ) ;
#2702=EDGE_CURVE ( 'NONE', #12619, #11114, #14202, .T. ) ;
#2712=CARTESIAN_POINT ( 'NONE',  ( -10.74479785762736661, 39.62990750194220624, -140.6987230986796078 ) ) ;
#2714=CARTESIAN_POINT ( 'NONE',  ( -8.514310886030200365, 36.94123471670563674, -140.1199228274903987 ) ) ;
#2715=CARTESIAN_POINT ( 'NONE',  ( -9.008354782749020018, 41.28660893102239982, -146.4928760736580386 ) ) ;
#2725=CARTESIAN_POINT ( 'NONE',  ( -18.12563077678109380, 37.94526991178427977, -148.6669620614958944 ) ) ;
#2732=CARTESIAN_POINT ( 'NONE',  ( -18.53945141080000170, 39.74065879090000664, -147.6687609889999919 ) ) ;
#2734=CARTESIAN_POINT ( 'NONE',  ( -15.39088246931257942, 40.97264801224785913, -143.5343598390859938 ) ) ;
#2735=CARTESIAN_POINT ( 'NONE',  ( -24.83693579151085373, 35.06568064903114390, -148.4846062725258662 ) ) ;
#2754=CARTESIAN_POINT ( 'NONE',  ( -20.95225485091065565, 36.93199168240901997, -148.3394883768439740 ) ) ;
#2767=CARTESIAN_POINT ( 'NONE',  ( -17.10416939857909213, 33.74918808323167241, -142.0823092718280805 ) ) ;
#2773=CARTESIAN_POINT ( 'NONE',  ( -29.62481956326176658, 40.87340935581828205, -146.3463541501877785 ) ) ;
#2780=FACE_OUTER_BOUND ( 'NONE', #8072, .T. ) ;
#2785=CARTESIAN_POINT ( 'NONE',  ( -10.46044647323697063, 34.41702787325856150, -147.4775189463319407 ) ) ;
#2788=CARTESIAN_POINT ( 'NONE',  ( -7.628878236750000319, 37.90286001179999431, -140.0026079769999683 ) ) ;
#2792=CARTESIAN_POINT ( 'NONE',  ( -7.305231917127300356, 34.61982510821351866, -147.5275647001010100 ) ) ;
#2794=CARTESIAN_POINT ( 'NONE',  ( -20.45144833149999997, 36.94873838139999833, -139.8044047869999815 ) ) ;
#2799=CARTESIAN_POINT ( 'NONE',  ( -21.02348081759773279, 37.67455232199478843, -147.5674820021630467 ) ) ;
#2800=CARTESIAN_POINT ( 'NONE',  ( -17.89449017611291737, 39.21037955099460248, -147.0820833685213813 ) ) ;
#2804=CARTESIAN_POINT ( 'NONE',  ( -25.71899619671468784, 33.84119088110737295, -142.2795079795113224 ) ) ;
#2818=CARTESIAN_POINT ( 'NONE',  ( -18.57919711151616582, 36.32393431488520719, -147.4152369972853762 ) ) ;
#2821=SHAPE_REPRESENTATION ( 'Latch Return Spring', ( #5025 ), #3911 ) ;
#2826=CARTESIAN_POINT ( 'NONE',  ( -27.47244207670000193, 35.09215423530000066, -148.2237751110000090 ) ) ;
#2841=CARTESIAN_POINT ( 'NONE',  ( -14.70419048427484121, 38.44039274178464893, -140.6418676086782682 ) ) ;
#2878=CARTESIAN_POINT ( 'NONE',  ( -4.683324139160000676, 37.83302525630000446, -140.3020749749999823 ) ) ;
#2883=CARTESIAN_POINT ( 'NONE',  ( -9.834719431799998191, 32.58365614919999587, -144.2353630830000100 ) ) ;
#2899=CARTESIAN_POINT ( 'NONE',  ( -10.88223456478890938, 32.81667835592666904, -144.3412242124914258 ) ) ;
#2903=CARTESIAN_POINT ( 'NONE',  ( -20.93854596064992180, 37.74500530009579791, -147.9603137871160072 ) ) ;
#2907=CARTESIAN_POINT ( 'NONE',  ( -7.987711783864115844, 33.66592685080672709, -142.2820551195727319 ) ) ;
#2908=CARTESIAN_POINT ( 'NONE',  ( -29.86462848809999926, 41.46897301219999576, -145.0541174280000121 ) ) ;
#2910=CARTESIAN_POINT ( 'NONE',  ( -21.29590688489999906, 41.28591597809999314, -144.5271551099999954 ) ) ;
#2917=CARTESIAN_POINT ( 'NONE',  ( -17.98362287481939248, 39.30401989832888177, -140.6846516121062223 ) ) ;
#2922=CARTESIAN_POINT ( 'NONE',  ( -24.58801263762544309, 32.96925759728824090, -144.4410906680583082 ) ) ;
#2924=CARTESIAN_POINT ( 'NONE',  ( -12.46649926358460725, 41.37859836428589944, -144.5903357203852124 ) ) ;
#2938=CARTESIAN_POINT ( 'NONE',  ( -18.46643761660000038, 34.84883242739999787, -147.1252693400000169 ) ) ;
#2943=CARTESIAN_POINT ( 'NONE',  ( -7.015833805750000707, 33.30032478630000270, -141.9582197170000200 ) ) ;
#2944=CARTESIAN_POINT ( 'NONE',  ( -9.410060017898935314, 41.36342684009822079, -144.4162120660980122 ) ) ;
#2946=CARTESIAN_POINT ( 'NONE',  ( -28.37825339579999806, 32.94869610819999650, -141.6352474660000098 ) ) ;
#2960=CARTESIAN_POINT ( 'NONE',  ( -18.31895680040000229, 41.06933176500000116, -146.2870363079999834 ) ) ;
#2964=CARTESIAN_POINT ( 'NONE',  ( -26.30700737260927369, 34.29719532912928059, -140.4927034919771245 ) ) ;
#2967=( BOUNDED_SURFACE ( )  B_SPLINE_SURFACE ( 5, 5, ( 
 ( #5332, #10779, #5093, #21521, #19962, #10428 ),
 ( #3664, #23181, #1775, #8641, #16279, #17706 ),
 ( #17825, #1893, #6874, #9116, #7348, #14142 ),
 ( #3307, #23535, #108, #1542, #8764, #6995 ),
 ( #5203, #14953, #9580, #18301, #13047, #12808 ),
 ( #11359, #4246, #2234, #7567, #20318, #18759 ),
 ( #9691, #12927, #678, #4012, #3902, #22214 ),
 ( #3781, #11241, #16966, #14842, #9454, #18513 ),
 ( #20082, #7797, #11023, #11481, #2117, #16733 ),
 ( #22101, #2470, #7910, #2015, #21876, #2359 ),
 ( #20207, #447, #5560, #18641, #9235, #16502 ),
 ( #208, #20426, #7684, #16854, #11133, #7452 ) ),
 .UNSPECIFIED., .F., .F., .F. ) 
 B_SPLINE_SURFACE_WITH_KNOTS ( ( 6, 3, 3, 6 ),
 ( 6, 6 ),
 ( 0.000000000000000000, 4.463483057499999518, 8.880954762089999122, 13.25426345570000031 ),
 ( 0.000000000000000000, 1.570796326817224919 ),
 .UNSPECIFIED. ) 
 GEOMETRIC_REPRESENTATION_ITEM ( )  RATIONAL_B_SPLINE_SURFACE ( (
 ( 1.000000000000000000, 0.5999999999943410600, 0.3999999999943409934, 0.2999999999957554953, 0.2499999999971705134, 0.2500000000000000000),
 ( 1.000000000000000000, 0.5999999999943410600, 0.3999999999943409934, 0.2999999999957554953, 0.2499999999971705134, 0.2500000000000000000),
 ( 1.000000000000000000, 0.5999999999943410600, 0.3999999999943409934, 0.2999999999957554953, 0.2499999999971705134, 0.2500000000000000000),
 ( 1.000000000000000000, 0.5999999999943410600, 0.3999999999943409934, 0.2999999999957554953, 0.2499999999971705134, 0.2500000000000000000),
 ( 1.000000000000000000, 0.5999999999943410600, 0.3999999999943409934, 0.2999999999957554953, 0.2499999999971705134, 0.2500000000000000000),
 ( 1.000000000000000000, 0.5999999999943410600, 0.3999999999943409934, 0.2999999999957554953, 0.2499999999971705134, 0.2500000000000000000),
 ( 1.000000000000000000, 0.5999999999943410600, 0.3999999999943409934, 0.2999999999957554953, 0.2499999999971705134, 0.2500000000000000000),
 ( 1.000000000000000000, 0.5999999999943410600, 0.3999999999943409934, 0.2999999999957554953, 0.2499999999971705134, 0.2500000000000000000),
 ( 1.000000000000000000, 0.5999999999943410600, 0.3999999999943409934, 0.2999999999957554953, 0.2499999999971705134, 0.2500000000000000000),
 ( 1.000000000000000000, 0.5999999999943410600, 0.3999999999943409934, 0.2999999999957554953, 0.2499999999971705134, 0.2500000000000000000),
 ( 1.000000000000000000, 0.5999999999943410600, 0.3999999999943409934, 0.2999999999957554953, 0.2499999999971705134, 0.2500000000000000000),
 ( 1.000000000000000000, 0.5999999999943410600, 0.3999999999943409934, 0.2999999999957554953, 0.2499999999971705134, 0.2500000000000000000) ) ) 
 REPRESENTATION_ITEM ( '' )  SURFACE ( )  );
#2969=ORIENTED_EDGE ( 'NONE', *, *, #11432, .T. ) ;
#2970=CARTESIAN_POINT ( 'NONE',  ( -12.04808041669999952, 40.71874701600000179, -143.7411651109999866 ) ) ;
#2983=CARTESIAN_POINT ( 'NONE',  ( -14.06829009843223766, 40.90462708772086842, -143.6915823990867409 ) ) ;
#3005=ORIENTED_EDGE ( 'NONE', *, *, #4849, .F. ) ;
#3013=CARTESIAN_POINT ( 'NONE',  ( -29.19447537614601274, 33.38066814340002963, -141.9968987688876609 ) ) ;
#3017=CARTESIAN_POINT ( 'NONE',  ( -23.66625742371592978, 40.06790428317820130, -142.3133758147152435 ) ) ;
#3023=CARTESIAN_POINT ( 'NONE',  ( -4.875412749849999727, 39.32116320210000282, -140.9191069839999955 ) ) ;
#3033=CARTESIAN_POINT ( 'NONE',  ( -7.384580498943978277, 36.26220355060780065, -140.3078533517004303 ) ) ;
#3039=CARTESIAN_POINT ( 'NONE',  ( -14.12781175210000129, 38.88127384660000274, -139.8125553750000165 ) ) ;
#3042=CARTESIAN_POINT ( 'NONE',  ( -17.52779041587893971, 36.93962571632589231, -139.7364823516947467 ) ) ;
#3044=CARTESIAN_POINT ( 'NONE',  ( -12.94305406498006761, 37.05025962682653784, -148.5780888799760078 ) ) ;
#3047=CARTESIAN_POINT ( 'NONE',  ( -24.78493530337882333, 34.98244403198583541, -146.8404575437234314 ) ) ;
#3055=ORIENTED_EDGE ( 'NONE', *, *, #14144, .F. ) ;
#3066=CARTESIAN_POINT ( 'NONE',  ( -15.46613156839999981, 36.99333119719999985, -147.5584717940000132 ) ) ;
#3069=CARTESIAN_POINT ( 'NONE',  ( -8.462924335808684972, 36.00512048834733037, -139.7368446338785191 ) ) ;
#3070=CARTESIAN_POINT ( 'NONE',  ( -9.292483939522659497, 40.96918990745680134, -144.3907905727278091 ) ) ;
#3084=CARTESIAN_POINT ( 'NONE',  ( -22.52780672249999938, 37.05898997719999954, -140.0074087190000114 ) ) ;
#3086=ORIENTED_EDGE ( 'NONE', *, *, #14144, .T. ) ;
#3087=CARTESIAN_POINT ( 'NONE',  ( -14.21887350771891967, 37.71951061620244161, -140.5431489171321857 ) ) ;
#3088=CARTESIAN_POINT ( 'NONE',  ( -26.39607007120000048, 36.95534867429999792, -140.3840478969999879 ) ) ;
#3091=CARTESIAN_POINT ( 'NONE',  ( -12.66714788130000002, 37.75265353620000042, -147.6129237410000030 ) ) ;
#3103=CARTESIAN_POINT ( 'NONE',  ( -14.62351239453423091, 39.57503987224152553, -147.6848723493663726 ) ) ;
#3104=CARTESIAN_POINT ( 'NONE',  ( -28.52142019844505327, 37.05975231236403999, -139.6605181375938685 ) ) ;
#3109=( BOUNDED_CURVE ( )  B_SPLINE_CURVE ( 5, ( #1415, #6636, #19610, #14012, #21284, #17467 ),
 .UNSPECIFIED., .F., .F. ) 
 B_SPLINE_CURVE_WITH_KNOTS ( ( 6, 6 ),
 ( 0.000000000000000000, 1.570796326526077813 ),
 .UNSPECIFIED. ) 
 CURVE ( )  GEOMETRIC_REPRESENTATION_ITEM ( )  RATIONAL_B_SPLINE_CURVE ( ( 1.000000000000000000, 0.6000000000684805324, 0.4000000000684805213, 0.3000000000513604048, 0.2500000000342402773, 0.2500000000000000555 ) ) 
 REPRESENTATION_ITEM ( '' )  );
#3118=CARTESIAN_POINT ( 'NONE',  ( -16.36311878257998842, 35.26028592910842008, -139.7765051114957089 ) ) ;
#3122=CARTESIAN_POINT ( 'NONE',  ( -24.78261485200000180, 38.62237172060000034, -147.6366313890000015 ) ) ;
#3129=CARTESIAN_POINT ( 'NONE',  ( -29.35976486581876799, 36.20619751666908570, -140.4758582103364120 ) ) ;
#3133=CARTESIAN_POINT ( 'NONE',  ( -13.59981317924081701, 37.05039483956773694, -139.6306434366684357 ) ) ;
#3139=CARTESIAN_POINT ( 'NONE',  ( -10.66194399654457925, 33.15920395776767293, -144.2988335296967932 ) ) ;
#3141=CARTESIAN_POINT ( 'NONE',  ( -9.801780389418540906, 37.03339632396453851, -147.4803110669293176 ) ) ;
#3147=CARTESIAN_POINT ( 'NONE',  ( -6.554568091467054991, 33.71641555244740829, -145.9835056079819822 ) ) ;
#3149=CARTESIAN_POINT ( 'NONE',  ( -21.19005019800000156, 41.30866696430000218, -143.6114845980000041 ) ) ;
#3155=VERTEX_POINT ( 'NONE', #15483 ) ;
#3156=CARTESIAN_POINT ( 'NONE',  ( -21.70878449369999785, 39.52018264390000013, -147.4849246469999855 ) ) ;
#3161=CARTESIAN_POINT ( 'NONE',  ( -12.28014746100000032, 36.97113097969999984, -148.4919582129999753 ) ) ;
#3162=ADVANCED_FACE ( 'NONE', ( #22986 ), #17740, .F. ) ;
#3164=CARTESIAN_POINT ( 'NONE',  ( -16.37184312240000139, 32.37338091950000063, -144.3414871020000021 ) ) ;
#3176=CARTESIAN_POINT ( 'NONE',  ( -19.09494877090000031, 33.54410563159999725, -142.1858765940000069 ) ) ;
#3181=CARTESIAN_POINT ( 'NONE',  ( -7.033127412180307125, 32.99152251563850768, -141.7906166089485396 ) ) ;
#3190=CARTESIAN_POINT ( 'NONE',  ( -21.03694116389999635, 36.94210036639999828, -147.9486865819999935 ) ) ;
#3192=EDGE_LOOP ( 'NONE', ( #1448, #11981, #6114, #6171 ) ) ;
#3193=CARTESIAN_POINT ( 'NONE',  ( -22.56584646749552903, 37.05444931710232481, -139.6092474952423288 ) ) ;
#3194=CARTESIAN_POINT ( 'NONE',  ( -10.65913935279999869, 37.04331329920000115, -139.7140392919999954 ) ) ;
#3196=CARTESIAN_POINT ( 'NONE',  ( -15.37212823710000009, 38.89807584180000077, -148.3010324070000081 ) ) ;
#3197=CARTESIAN_POINT ( 'NONE',  ( -24.76223978037774032, 32.81123456503314628, -146.4711376325379604 ) ) ;
#3200=CARTESIAN_POINT ( 'NONE',  ( -12.30631862549999944, 40.23402543379999230, -145.9987124289999940 ) ) ;
#3215=CARTESIAN_POINT ( 'NONE',  ( -14.19189821223558567, 41.34771858761131824, -144.5672307995002939 ) ) ;
#3224=EDGE_LOOP ( 'NONE', ( #19194, #10658, #15312, #9213 ) ) ;
#3236=CARTESIAN_POINT ( 'NONE',  ( -29.58443045183165410, 36.11526935725738241, -140.1709594658998981 ) ) ;
#3239=CARTESIAN_POINT ( 'NONE',  ( -24.65454682284185139, 38.48142452593771168, -147.3520111327411257 ) ) ;
#3245=CARTESIAN_POINT ( 'NONE',  ( -4.584402860569999127, 37.05223431090000474, -140.2914745300000163 ) ) ;
#3253=CARTESIAN_POINT ( 'NONE',  ( -8.360775440490805011, 36.18761969327825767, -140.5275716988375336 ) ) ;
#3254=CARTESIAN_POINT ( 'NONE',  ( -7.010349701930000066, 37.05829245179999987, -148.1453878979999956 ) ) ;
#3262=CARTESIAN_POINT ( 'NONE',  ( -16.91592704299999994, 37.75347730500000409, -140.5160138910000001 ) ) ;
#3268=CARTESIAN_POINT ( 'NONE',  ( -16.48779918059999616, 32.42295671489999620, -143.3618442240000093 ) ) ;
#3288=CARTESIAN_POINT ( 'NONE',  ( -11.57053722856168321, 40.11345306623577756, -146.0212872837172711 ) ) ;
#3296=CARTESIAN_POINT ( 'NONE',  ( -8.462973826026381374, 36.94736262684724437, -140.5165674475847197 ) ) ;
#3307=CARTESIAN_POINT ( 'NONE',  ( -22.31464002779999944, 34.51618902799999944, -147.4864127260000259 ) ) ;
#3326=CARTESIAN_POINT ( 'NONE',  ( -14.87492916135365384, 38.44269649874472350, -147.4253129834213780 ) ) ;
#3333=CARTESIAN_POINT ( 'NONE',  ( -24.50448663620845480, 36.99790949616351554, -147.3823814621291888 ) ) ;
#3342=CARTESIAN_POINT ( 'NONE',  ( -6.166004029562527577, 36.95750611116528717, -148.6250205690956534 ) ) ;
#3359=CARTESIAN_POINT ( 'NONE',  ( -18.95027878879999861, 36.16636532760000478, -148.4341920939999966 ) ) ;
#3395=CARTESIAN_POINT ( 'NONE',  ( -27.99900835291655810, 33.07904996078797666, -141.6633825115897025 ) ) ;
#3401=CARTESIAN_POINT ( 'NONE',  ( -18.92206117636284546, 33.99949261441817328, -145.9371503374987356 ) ) ;
#3428=CARTESIAN_POINT ( 'NONE',  ( -15.96254761875824180, 38.65457006438045795, -147.5807964054747856 ) ) ;
#3429=CARTESIAN_POINT ( 'NONE',  ( -29.36832786400000117, 38.86294434210000048, -140.8528603229999874 ) ) ;
#3435=CARTESIAN_POINT ( 'NONE',  ( -26.92295469378113992, 39.53966211714406143, -140.4202993119762368 ) ) ;
#3436=EDGE_CURVE ( 'NONE', #6123, #2118, #669, .T. ) ;
#3441=CARTESIAN_POINT ( 'NONE',  ( -10.65913935279999869, 37.04331329920000115, -139.7140392919999954 ) ) ;
#3452=CARTESIAN_POINT ( 'NONE',  ( -11.38486064697293898, 36.95668670074196172, -140.3965526142782210 ) ) ;
#3453=CARTESIAN_POINT ( 'NONE',  ( -14.68945449529999969, 41.62249060810000145, -143.5408288559999903 ) ) ;
#3465=CARTESIAN_POINT ( 'NONE',  ( -4.626684792761640352, 38.75063101611807070, -140.2397901787329317 ) ) ;
#3471=CARTESIAN_POINT ( 'NONE',  ( -15.86078924153198599, 37.04043998683724226, -147.5134597624269190 ) ) ;
#3477=CARTESIAN_POINT ( 'NONE',  ( -24.22614176569036459, 39.00041403165653975, -146.8502260740512213 ) ) ;
#3478=CARTESIAN_POINT ( 'NONE',  ( -29.57566076271681510, 39.40610565237071228, -139.8786281328294763 ) ) ;
#3485=CARTESIAN_POINT ( 'NONE',  ( -19.48146791446731640, 32.28180044528915005, -143.8017659915034301 ) ) ;
#3487=CARTESIAN_POINT ( 'NONE',  ( -9.341122566677128702, 40.18160354483676144, -145.8224011896586489 ) ) ;
#3494=CARTESIAN_POINT ( 'NONE',  ( -23.24588518179999852, 41.24341284999999857, -143.7187626420000015 ) ) ;
#3529=CARTESIAN_POINT ( 'NONE',  ( -19.34447215129067033, 33.98952392425853475, -145.9993797645266795 ) ) ;
#3530=CARTESIAN_POINT ( 'NONE',  ( -11.48460281164964414, 40.77310199058896245, -146.4361868664954613 ) ) ;
#3545=CARTESIAN_POINT ( 'NONE',  ( -19.79317654020000106, 38.64314174740000141, -140.5356700199999977 ) ) ;
#3557=CARTESIAN_POINT ( 'NONE',  ( -26.71298293347248887, 37.74538646634001537, -140.1185230284342538 ) ) ;
#3559=ORIENTED_EDGE ( 'NONE', *, *, #20029, .T. ) ;
#3568=CARTESIAN_POINT ( 'NONE',  ( -10.65913935279999869, 37.04331329920000115, -139.7140392919999954 ) ) ;
#3570=CARTESIAN_POINT ( 'NONE',  ( -16.92431971701898874, 37.01165972487905265, -139.4624774945162358 ) ) ;
#3586=CARTESIAN_POINT ( 'NONE',  ( -6.163071638762996685, 41.67289232386758613, -144.4686657573369644 ) ) ;
#3589=ORIENTED_EDGE ( 'NONE', *, *, #15447, .T. ) ;
#3595=( BOUNDED_SURFACE ( )  B_SPLINE_SURFACE ( 5, 5, ( 
 ( #21309, #3104, #21666, #17969, #23321, #14275 ),
 ( #5356, #12474, #5225, #23205, #10340, #1568 ),
 ( #5001, #19758, #19522, #1441, #14392, #8902 ),
 ( #14162, #21426, #7132, #18668, #14739, #12832 ),
 ( #18540, #3806, #19985, #7475, #11045, #18202 ),
 ( #22125, #11268, #2259, #2381, #10919, #1917 ),
 ( #584, #236, #18323, #4148, #13180, #13069 ),
 ( #18431, #20340, #3923, #349, #11157, #9602 ),
 ( #20230, #7591, #5580, #5811, #11386, #2145 ) ),
 .UNSPECIFIED., .F., .F., .F. ) 
 B_SPLINE_SURFACE_WITH_KNOTS ( ( 6, 3, 6 ),
 ( 6, 6 ),
 ( 0.000000000000000000, 5.731822293570000504, 9.005131590149998644 ),
 ( 1.570796326704904988, 3.141592653590000062 ),
 .UNSPECIFIED. ) 
 GEOMETRIC_REPRESENTATION_ITEM ( )  RATIONAL_B_SPLINE_SURFACE ( (
 ( 0.2500000000000000000, 0.2499999999885285096, 0.2999999999827930308, 0.3999999999770569858, 0.5999999999770569969, 1.000000000000000000),
 ( 0.2500000000000000000, 0.2499999999885285096, 0.2999999999827930308, 0.3999999999770569858, 0.5999999999770569969, 1.000000000000000000),
 ( 0.2500000000000000000, 0.2499999999885285096, 0.2999999999827930308, 0.3999999999770569858, 0.5999999999770569969, 1.000000000000000000),
 ( 0.2500000000000000000, 0.2499999999885285096, 0.2999999999827930308, 0.3999999999770569858, 0.5999999999770569969, 1.000000000000000000),
 ( 0.2500000000000000000, 0.2499999999885285096, 0.2999999999827930308, 0.3999999999770569858, 0.5999999999770569969, 1.000000000000000000),
 ( 0.2500000000000000000, 0.2499999999885285096, 0.2999999999827930308, 0.3999999999770569858, 0.5999999999770569969, 1.000000000000000000),
 ( 0.2500000000000000000, 0.2499999999885285096, 0.2999999999827930308, 0.3999999999770569858, 0.5999999999770569969, 1.000000000000000000),
 ( 0.2500000000000000000, 0.2499999999885285096, 0.2999999999827930308, 0.3999999999770569858, 0.5999999999770569969, 1.000000000000000000),
 ( 0.2500000000000000000, 0.2499999999885285096, 0.2999999999827930308, 0.3999999999770569858, 0.5999999999770569969, 1.000000000000000000) ) ) 
 REPRESENTATION_ITEM ( '' )  SURFACE ( )  );
#3597=CARTESIAN_POINT ( 'NONE',  ( -24.99548980007219967, 37.05651868163716500, -148.5304149358840391 ) ) ;
#3599=CARTESIAN_POINT ( 'NONE',  ( -23.76507348488087956, 39.47303768213036079, -147.6024660352933893 ) ) ;
#3600=CARTESIAN_POINT ( 'NONE',  ( -29.95440394289919794, 41.49361247766784544, -142.3913186430430073 ) ) ;
#3604=CARTESIAN_POINT ( 'NONE',  ( -20.23971019809999916, 35.09018026569999904, -140.0771129649999978 ) ) ;
#3605=CARTESIAN_POINT ( 'NONE',  ( -9.605700179776247793, 38.47911542068607105, -147.2779594871227857 ) ) ;
#3610=B_SPLINE_CURVE_WITH_KNOTS ( 'NONE', 5,
 ( #5925, #21788, #5473, #3685, #16529, #7371, #14630, #21898, #20570, #19013, #2490, #11977 ),
 .UNSPECIFIED., .F., .F.,
 ( 6, 3, 3, 6 ),
 ( 0.000000000000000000, 4.463483057499999518, 8.880954762089999122, 13.25426345570000031 ),
 .UNSPECIFIED. ) ;
#3614=CARTESIAN_POINT ( 'NONE',  ( -24.06602356359999817, 36.94557182220000158, -148.2530914610000252 ) ) ;
#3621=CARTESIAN_POINT ( 'NONE',  ( -18.85469010170000459, 37.03971195569999963, -148.4264296979999926 ) ) ;
#3626=CARTESIAN_POINT ( 'NONE',  ( -17.68978131335608950, 36.92028947728229582, -140.0842674915935504 ) ) ;
#3637=CARTESIAN_POINT ( 'NONE',  ( -15.79202522179999946, 35.03772048769999969, -148.2850092029999871 ) ) ;
#3638=CARTESIAN_POINT ( 'NONE',  ( -13.14072436392984322, 35.21943041104802319, -148.3635587296070071 ) ) ;
#3644=CARTESIAN_POINT ( 'NONE',  ( -19.88002610979284057, 33.21367146195343167, -143.9008389802610282 ) ) ;
#3661=CARTESIAN_POINT ( 'NONE',  ( -26.59168384020000175, 38.48554521319999822, -140.5676127940000129 ) ) ;
#3664=CARTESIAN_POINT ( 'NONE',  ( -22.10875017890000294, 36.18377167419999552, -148.1739623899999856 ) ) ;
#3670=CARTESIAN_POINT ( 'NONE',  ( -27.35038827430062014, 41.32943388969216159, -143.4915779297264748 ) ) ;
#3684=CARTESIAN_POINT ( 'NONE',  ( -17.27864984452603991, 40.23496799366807863, -142.1532139957253946 ) ) ;
#3685=CARTESIAN_POINT ( 'NONE',  ( -22.31464002779999944, 34.51618902799999944, -147.4864127260000259 ) ) ;
#3698=CARTESIAN_POINT ( 'NONE',  ( -6.909346445852020402, 37.92300339049243973, -148.1333867873126167 ) ) ;
#3701=ORIENTED_EDGE ( 'NONE', *, *, #849, .F. ) ;
#3708=CARTESIAN_POINT ( 'NONE',  ( -24.50448663600032972, 36.99790949613869628, -147.3823814620264159 ) ) ;
#3710=CARTESIAN_POINT ( 'NONE',  ( -29.69384575750991218, 38.86443117690002680, -140.7775166546643391 ) ) ;
#3712=CARTESIAN_POINT ( 'NONE',  ( -21.73453520639999681, 32.91403690879999289, -144.3663112600000318 ) ) ;
#3715=CARTESIAN_POINT ( 'NONE',  ( -10.78990953686118104, 36.10633245638514666, -139.4672549339003353 ) ) ;
#3716=CARTESIAN_POINT ( 'NONE',  ( -19.35423020444331144, 32.65090734717338705, -141.7482459578876615 ) ) ;
#3730=CARTESIAN_POINT ( 'NONE',  ( -4.875412749849999727, 39.32116320210000282, -140.9191069839999955 ) ) ;
#3752=CARTESIAN_POINT ( 'NONE',  ( -16.84295571282639870, 33.21673955036126813, -144.3448215146551661 ) ) ;
#3759=CARTESIAN_POINT ( 'NONE',  ( -19.91220883949999987, 32.96944242089999477, -141.9853941000000077 ) ) ;
#3777=CARTESIAN_POINT ( 'NONE',  ( -24.97797643630000053, 37.05442817780000553, -147.8575004449999994 ) ) ;
#3779=CARTESIAN_POINT ( 'NONE',  ( -26.25246229356530492, 40.09452554318689010, -142.2796191593848221 ) ) ;
#3781=CARTESIAN_POINT ( 'NONE',  ( -23.02519999780000148, 33.35976406540000028, -141.9520978260000277 ) ) ;
#3788=CARTESIAN_POINT ( 'NONE',  ( -26.61707828802655484, 36.92896776167479089, -139.7487649555727103 ) ) ;
#3798=CARTESIAN_POINT ( 'NONE',  ( -16.54277457359999914, 34.95491693750000195, -141.0331736029999945 ) ) ;
#3805=CARTESIAN_POINT ( 'NONE',  ( -17.22605506639999717, 36.97564272059999979, -139.5994799229999899 ) ) ;
#3806=CARTESIAN_POINT ( 'NONE',  ( -29.16261562813939179, 41.45297187880490952, -142.5000714354081595 ) ) ;
#3808=CARTESIAN_POINT ( 'NONE',  ( -8.565647946148805758, 36.93510680655035827, -139.7232782065093488 ) ) ;
#3819=CARTESIAN_POINT ( 'NONE',  ( -26.86963863710373701, 36.92213009831746007, -147.8538433455846359 ) ) ;
#3822=CARTESIAN_POINT ( 'NONE',  ( -4.780317782130000914, 38.61135856239999953, -140.5115181619999873 ) ) ;
#3838=CARTESIAN_POINT ( 'NONE',  ( -19.33242029388426531, 35.08629375165114084, -139.8117605349705173 ) ) ;
#3851=CARTESIAN_POINT ( 'NONE',  ( -6.093288228365016934, 36.94882630176445559, -147.6373263597673997 ) ) ;
#3860=CARTESIAN_POINT ( 'NONE',  ( -12.85940537543597806, 33.96382169714053845, -145.9084692328443964 ) ) ;
#3869=( BOUNDED_CURVE ( )  B_SPLINE_CURVE ( 5, ( #22580, #19121, #2826, #9944, #13776, #12088, #1296, #2946, #13996, #10305, #1179, #4967 ),
 .UNSPECIFIED., .F., .F. ) 
 B_SPLINE_CURVE_WITH_KNOTS ( ( 6, 3, 3, 6 ),
 ( 0.000000000000000000, 4.564346237179999655, 9.066392868600001265, 13.51003987140000007 ),
 .UNSPECIFIED. ) 
 CURVE ( )  GEOMETRIC_REPRESENTATION_ITEM ( )  RATIONAL_B_SPLINE_CURVE ( ( 0.2500000000000000000, 0.2500000000000000000, 0.2500000000000000000, 0.2500000000000000000, 0.2500000000000000000, 0.2500000000000000000, 0.2500000000000000000, 0.2500000000000000000, 0.2500000000000000000, 0.2500000000000000000, 0.2500000000000000000, 0.2500000000000000000 ) ) 
 REPRESENTATION_ITEM ( '' )  );
#3873=CARTESIAN_POINT ( 'NONE',  ( -13.03986231551754749, 36.13583152158137324, -148.5880302933537678 ) ) ;
#3879=B_SPLINE_CURVE_WITH_KNOTS ( 'NONE', 5,
 ( #6996, #12456, #3429, #16280, #20209, #12929, #7686, #11024, #16735 ),
 .UNSPECIFIED., .F., .F.,
 ( 6, 3, 6 ),
 ( 0.000000000000000000, 5.731822293570000504, 9.005131590149998644 ),
 .UNSPECIFIED. ) ;
#3883=CARTESIAN_POINT ( 'NONE',  ( -19.48816230390420046, 36.23023348065551374, -140.2952556283244121 ) ) ;
#3887=CARTESIAN_POINT ( 'NONE',  ( -20.45144833149999997, 36.94873838139999833, -139.8044047869999815 ) ) ;
#3896=CARTESIAN_POINT ( 'NONE',  ( -26.39607007120000048, 36.95534867429999792, -140.3840478969999879 ) ) ;
#3900=CARTESIAN_POINT ( 'NONE',  ( -25.84964047065839665, 38.84307078620516052, -139.9757795271566181 ) ) ;
#3902=CARTESIAN_POINT ( 'NONE',  ( -21.81749540767824769, 32.51398808010975472, -143.4422501083998611 ) ) ;
#3907=CARTESIAN_POINT ( 'NONE',  ( -26.95224972436776056, 39.68365438087440111, -147.7577323693793971 ) ) ;
#3911=( GEOMETRIC_REPRESENTATION_CONTEXT ( 3 ) GLOBAL_UNCERTAINTY_ASSIGNED_CONTEXT ( ( #7317 ) ) GLOBAL_UNIT_ASSIGNED_CONTEXT ( ( #15284, #1005, #9776 ) ) REPRESENTATION_CONTEXT ( 'NONE', 'WORKASPACE' ) );
#3915=CARTESIAN_POINT ( 'NONE',  ( -8.271665395864435055, 36.97019838859878149, -139.4157638768422203 ) ) ;
#3919=ORIENTED_EDGE ( 'NONE', *, *, #849, .T. ) ;
#3921=CARTESIAN_POINT ( 'NONE',  ( -12.06588019170748183, 41.72429084328257431, -143.6635755491118402 ) ) ;
#3922=CARTESIAN_POINT ( 'NONE',  ( -17.20598434367817120, 40.91627233628883431, -144.4696775178145174 ) ) ;
#3923=CARTESIAN_POINT ( 'NONE',  ( -29.28558960869785466, 40.89060929661447119, -145.6601555479529111 ) ) ;
#3926=CARTESIAN_POINT ( 'NONE',  ( -26.39607007120000048, 36.95534867429999792, -140.3840478969999879 ) ) ;
#3931=CARTESIAN_POINT ( 'NONE',  ( -20.08037650824895692, 40.50744741020064055, -142.1449807696999983 ) ) ;
#3936=CARTESIAN_POINT ( 'NONE',  ( -12.58047663530000015, 34.35960099889999952, -147.8017659109999897 ) ) ;
#3948=EDGE_CURVE ( 'NONE', #15229, #22408, #13537, .T. ) ;
#3954=CARTESIAN_POINT ( 'NONE',  ( -20.07061698099752789, 34.98295635200901188, -139.7991296525235043 ) ) ;
#3957=CARTESIAN_POINT ( 'NONE',  ( -24.89658049647220039, 37.98069042798901052, -148.5190484855092166 ) ) ;
#3966=CARTESIAN_POINT ( 'NONE',  ( -5.288267155659133856, 38.37431289982901461, -140.9004779445601798 ) ) ;
#3969=CARTESIAN_POINT ( 'NONE',  ( -22.72559961389999827, 32.84666773589999877, -144.4841142160000231 ) ) ;
#3972=CARTESIAN_POINT ( 'NONE',  ( -12.05141338350562563, 35.34196401310663305, -147.7430715653573827 ) ) ;
#3984=CARTESIAN_POINT ( 'NONE',  ( -13.27736068057458141, 36.23365056575769216, -148.2500542414416600 ) ) ;
#3994=CARTESIAN_POINT ( 'NONE',  ( -21.27630696881890771, 40.59564883395965751, -144.4447941612343982 ) ) ;
#4001=( BOUNDED_CURVE ( )  B_SPLINE_CURVE ( 5, ( #23158, #8618, #13878, #15893, #13991, #17575, #10518, #1288, #19593, #1519, #4837, #20912 ),
 .UNSPECIFIED., .F., .F. ) 
 B_SPLINE_CURVE_WITH_KNOTS ( ( 6, 3, 3, 6 ),
 ( 0.000000000000000000, 4.371092480729999785, 8.745625541600000830, 13.12578902609999965 ),
 .UNSPECIFIED. ) 
 CURVE ( )  GEOMETRIC_REPRESENTATION_ITEM ( )  RATIONAL_B_SPLINE_CURVE ( ( 0.2500000000000000000, 0.2500000000000000000, 0.2500000000000000000, 0.2500000000000000000, 0.2500000000000000000, 0.2500000000000000000, 0.2500000000000000000, 0.2500000000000000000, 0.2500000000000000000, 0.2500000000000000000, 0.2500000000000000000, 0.2500000000000000000 ) ) 
 REPRESENTATION_ITEM ( '' )  );
#4005=ORIENTED_EDGE ( 'NONE', *, *, #4979, .F. ) ;
#4009=ORIENTED_EDGE ( 'NONE', *, *, #23226, .F. ) ;
#4010=CARTESIAN_POINT ( 'NONE',  ( -26.49328647146516147, 40.50686637268883317, -144.4416391455084181 ) ) ;
#4012=CARTESIAN_POINT ( 'NONE',  ( -22.13782755527650892, 32.22299539119053691, -143.4425233068306227 ) ) ;
#4019=CARTESIAN_POINT ( 'NONE',  ( -29.68301555208973852, 36.92109708054170625, -140.1550845752986731 ) ) ;
#4031=CARTESIAN_POINT ( 'NONE',  ( -12.08222824379999949, 38.77433534089999512, -148.2726881729999775 ) ) ;
#4040=CARTESIAN_POINT ( 'NONE',  ( -28.94327676059999988, 35.53474617860000251, -140.7339624629999832 ) ) ;
#4043=CARTESIAN_POINT ( 'NONE',  ( -21.19005019800000156, 41.30866696430000218, -143.6114845980000041 ) ) ;
#4046=CARTESIAN_POINT ( 'NONE',  ( -27.21970299319120912, 36.21690482628893193, -147.5085197383852176 ) ) ;
#4058=CARTESIAN_POINT ( 'NONE',  ( -23.51619327739999932, 36.94101002280000046, -140.1031831869999849 ) ) ;
#4059=EDGE_CURVE ( 'NONE', #4528, #20985, #9745, .T. ) ;
#4068=CARTESIAN_POINT ( 'NONE',  ( -24.07371653998410821, 40.87477276122073278, -141.8080750009974906 ) ) ;
#4069=CARTESIAN_POINT ( 'NONE',  ( -16.13502618060000060, 32.80445174449999968, -146.2787800969999807 ) ) ;
#4076=CARTESIAN_POINT ( 'NONE',  ( -4.780317782130000914, 38.61135856239999953, -140.5115181619999873 ) ) ;
#4080=CARTESIAN_POINT ( 'NONE',  ( -21.89685178202452320, 37.04474463553799524, -147.4979728336869869 ) ) ;
#4083=CARTESIAN_POINT ( 'NONE',  ( -12.71428973609129365, 32.54945626905336553, -144.6365914293318440 ) ) ;
#4094=CARTESIAN_POINT ( 'NONE',  ( -28.38533628227742867, 35.33089335701146894, -147.9595813284715007 ) ) ;
#4097=CARTESIAN_POINT ( 'NONE',  ( -14.11967125418341951, 36.98834135281187940, -140.5455248811661875 ) ) ;
#4105=CARTESIAN_POINT ( 'NONE',  ( -20.71903412364733299, 37.77148386094349064, -140.0779489345810589 ) ) ;
#4107=CARTESIAN_POINT ( 'NONE',  ( -18.85469010170000459, 37.03971195569999963, -148.4264296979999926 ) ) ;
#4118=CARTESIAN_POINT ( 'NONE',  ( -26.67031178456957008, 38.52782902798677611, -147.6692609235824989 ) ) ;
#4131=CARTESIAN_POINT ( 'NONE',  ( -7.138130562210037944, 35.21651592843031864, -148.3216512489436241 ) ) ;
#4134=CARTESIAN_POINT ( 'NONE',  ( -7.671834446767463511, 37.96637496773506371, -139.6710333262370796 ) ) ;
#4146=CARTESIAN_POINT ( 'NONE',  ( -11.09667937100654989, 38.99134170279717182, -139.7423566497915886 ) ) ;
#4147=CARTESIAN_POINT ( 'NONE',  ( -17.59229711595959955, 39.34301127023525879, -147.3183469250201654 ) ) ;
#4148=CARTESIAN_POINT ( 'NONE',  ( -29.26198848999914759, 40.69426223529025322, -144.9540979635152098 ) ) ;
#4160=CARTESIAN_POINT ( 'NONE',  ( -20.45144833149999997, 36.94873838139999833, -139.8044047869999815 ) ) ;
#4181=CARTESIAN_POINT ( 'NONE',  ( -23.01895658101113540, 35.59613479725317120, -140.8867697970091797 ) ) ;
#4192=CARTESIAN_POINT ( 'NONE',  ( -23.85957119133389881, 39.58299060703604511, -140.4713739358294333 ) ) ;
#4193=CARTESIAN_POINT ( 'NONE',  ( -15.46352699119206697, 34.98433354313474553, -148.3064882238327016 ) ) ;
#4194=CARTESIAN_POINT ( 'NONE',  ( -17.03115501030000090, 35.19590004879999867, -139.8299307730000010 ) ) ;
#4202=CARTESIAN_POINT ( 'NONE',  ( -5.801925844418948763, 39.15421101755954680, -147.0556221922513487 ) ) ;
#4205=ORIENTED_EDGE ( 'NONE', *, *, #15447, .F. ) ;
#4207=CARTESIAN_POINT ( 'NONE',  ( -22.10875017890000294, 36.18377167419999552, -148.1739623899999856 ) ) ;
#4217=CARTESIAN_POINT ( 'NONE',  ( -27.77832206610000298, 37.03059619289999915, -147.6270870419999710 ) ) ;
#4221=CARTESIAN_POINT ( 'NONE',  ( -14.26108793495632554, 34.19565738791286691, -140.4808705499285111 ) ) ;
#4232=CARTESIAN_POINT ( 'NONE',  ( -20.08037650815199981, 40.50744741039175523, -142.1449807696052119 ) ) ;
#4246=CARTESIAN_POINT ( 'NONE',  ( -22.70111404018277668, 32.50422370117523485, -144.5121409266673140 ) ) ;
#4251=CARTESIAN_POINT ( 'NONE',  ( -27.60583033794648600, 37.01000650950496862, -148.6900182104589589 ) ) ;
#4256=CARTESIAN_POINT ( 'NONE',  ( -7.243544775885156994, 34.37889476601232275, -147.8566374764138516 ) ) ;
#4268=CARTESIAN_POINT ( 'NONE',  ( -12.74435279828027490, 38.88449211440367748, -148.3283390160977717 ) ) ;
#4276=CARTESIAN_POINT ( 'NONE',  ( -21.50145757625659826, 36.99754792878884757, -147.3684231710527399 ) ) ;
#4280=CARTESIAN_POINT ( 'NONE',  ( -21.90852802850000103, 37.90475843469999973, -148.1502781210000137 ) ) ;
#4300=FACE_OUTER_BOUND ( 'NONE', #5072, .T. ) ;
#4303=CARTESIAN_POINT ( 'NONE',  ( -8.764836022000000781, 39.53398178709999655, -147.5842891229999907 ) ) ;
#4307=CARTESIAN_POINT ( 'NONE',  ( -24.78261485200000180, 38.62237172060000034, -147.6366313890000015 ) ) ;
#4309=CARTESIAN_POINT ( 'NONE',  ( -15.25588521237791539, 34.19578262203260977, -147.5708427275093015 ) ) ;
#4311=CARTESIAN_POINT ( 'NONE',  ( -16.58211931832967068, 33.51686747480896855, -143.5423247306498240 ) ) ;
#4313=CARTESIAN_POINT ( 'NONE',  ( -20.23971019809999916, 35.09018026569999904, -140.0771129649999978 ) ) ;
#4318=CARTESIAN_POINT ( 'NONE',  ( -9.971101149771200767, 37.05360750094124000, -147.8421425034415790 ) ) ;
#4322=CARTESIAN_POINT ( 'NONE',  ( -21.22299042056730300, 36.20661401050380590, -147.5479327630602029 ) ) ;
#4325=CARTESIAN_POINT ( 'NONE',  ( -12.79720822650000045, 32.99715178900000012, -146.4964997610000239 ) ) ;
#4334=CARTESIAN_POINT ( 'NONE',  ( -27.70749540540193578, 36.02653024062528431, -148.6920955691318795 ) ) ;
#4336=CARTESIAN_POINT ( 'NONE',  ( -13.67845320973112244, 33.33591541118190094, -146.4032996680919041 ) ) ;
#4343=CARTESIAN_POINT ( 'NONE',  ( -20.65692115970000131, 38.75897267589999728, -140.0270467099999792 ) ) ;
#4345=CARTESIAN_POINT ( 'NONE',  ( -17.75002847806602091, 38.41025389510169674, -140.6489478483555331 ) ) ;
#4347=( BOUNDED_CURVE ( )  B_SPLINE_CURVE ( 5, ( #509, #7975, #389, #5960, #2418, #16908 ),
 .UNSPECIFIED., .F., .F. ) 
 B_SPLINE_CURVE_WITH_KNOTS ( ( 6, 6 ),
 ( 0.000000000000000000, 1.570796326521524344 ),
 .UNSPECIFIED. ) 
 CURVE ( )  GEOMETRIC_REPRESENTATION_ITEM ( )  RATIONAL_B_SPLINE_CURVE ( ( 1.000000000000000000, 0.6000000000696400493, 0.4000000000696400382, 0.3000000000522300425, 0.2500000000348200357, 0.2500000000000000000 ) ) 
 REPRESENTATION_ITEM ( '' )  );
#4349=CARTESIAN_POINT ( 'NONE',  ( -25.51633159842389986, 34.96116192632524644, -141.2416905447548459 ) ) ;
#4362=CARTESIAN_POINT ( 'NONE',  ( -27.97930636479113531, 38.80653505726444763, -147.9089998809065776 ) ) ;
#4366=CARTESIAN_POINT ( 'NONE',  ( -7.462508610423953748, 33.01377392928537802, -146.5273241004201168 ) ) ;
#4367=CARTESIAN_POINT ( 'NONE',  ( -7.856058713499369794, 37.01980778200731237, -139.4032252962407483 ) ) ;
#4375=CARTESIAN_POINT ( 'NONE',  ( -17.89449577229860111, 36.92509720026602338, -147.9522036891450227 ) ) ;
#4386=CARTESIAN_POINT ( 'NONE',  ( -19.70010857004652394, 39.59599344006944222, -140.6831085099040308 ) ) ;
#4388=CARTESIAN_POINT ( 'NONE',  ( -28.80902675602211715, 36.08666534565443840, -139.5659208845989951 ) ) ;
#4404=CARTESIAN_POINT ( 'NONE',  ( -13.59981317924081701, 37.05039483956773694, -139.6306434366684357 ) ) ;
#4414=CARTESIAN_POINT ( 'NONE',  ( -24.68734501193447883, 39.74142694379266771, -147.7937591735077376 ) ) ;
#4422=B_SPLINE_CURVE_WITH_KNOTS ( 'NONE', 5,
 ( #3194, #10426, #12452, #21519, #14254, #12575, #7109, #8639, #15914, #5201, #23179, #10663 ),
 .UNSPECIFIED., .F., .F.,
 ( 6, 3, 3, 6 ),
 ( 0.000000000000000000, 4.398006073320000375, 8.633600727160001043, 12.71824907600000110 ),
 .UNSPECIFIED. ) ;
#4423=CARTESIAN_POINT ( 'NONE',  ( -10.44165342908376282, 33.50172955924855955, -144.2564428470086568 ) ) ;
#4431=CARTESIAN_POINT ( 'NONE',  ( -21.69807436992272542, 35.58641824452431734, -147.1799120564807879 ) ) ;
#4434=CARTESIAN_POINT ( 'NONE',  ( -22.99045472634351128, 38.45061197251095564, -140.9013473425142990 ) ) ;
#4435=EDGE_CURVE ( 'NONE', #17995, #22397, #2458, .T. ) ;
#4441=CARTESIAN_POINT ( 'NONE',  ( -9.953901650897911679, 37.05155446197423430, -148.5872971972358698 ) ) ;
#4443=CARTESIAN_POINT ( 'NONE',  ( -7.965235931336511754, 40.46410429990334023, -142.0948817276852765 ) ) ;
#4446=CARTESIAN_POINT ( 'NONE',  ( -28.25100290369999811, 33.74243115720000219, -145.9160084049999853 ) ) ;
#4449=CARTESIAN_POINT ( 'NONE',  ( -13.69130674751348131, 32.44151991234195975, -144.7631074377568439 ) ) ;
#4459=CARTESIAN_POINT ( 'NONE',  ( -18.89556302255113707, 38.83158734770280773, -147.9443928096210641 ) ) ;
#4461=( GEOMETRIC_REPRESENTATION_CONTEXT ( 3 ) GLOBAL_UNCERTAINTY_ASSIGNED_CONTEXT ( ( #5171 ) ) GLOBAL_UNIT_ASSIGNED_CONTEXT ( ( #18238, #5138, #12863 ) ) REPRESENTATION_CONTEXT ( 'NONE', 'WORKASPACE' ) );
#4464=CARTESIAN_POINT ( 'NONE',  ( -24.88338928008620599, 33.38756628440417984, -141.9140409061389789 ) ) ;
#4474=VERTEX_POINT ( 'NONE', #4669 ) ;
#4478=CARTESIAN_POINT ( 'NONE',  ( -11.58731752088923983, 38.53682247848004039, -140.5940415736972113 ) ) ;
#4480=( BOUNDED_CURVE ( )  B_SPLINE_CURVE ( 5, ( #19726, #1410, #3545, #18056, #1769, #23061, #6746, #8989, #4973, #12221, #19496, #3190 ),
 .UNSPECIFIED., .F., .F. ) 
 B_SPLINE_CURVE_WITH_KNOTS ( ( 6, 3, 3, 6 ),
 ( 0.000000000000000000, 4.390059406679999832, 8.746277600790000051, 13.07048654050000103 ),
 .UNSPECIFIED. ) 
 CURVE ( )  GEOMETRIC_REPRESENTATION_ITEM ( )  RATIONAL_B_SPLINE_CURVE ( ( 0.2500000000000000000, 0.2500000000000000000, 0.2500000000000000000, 0.2500000000000000000, 0.2500000000000000000, 0.2500000000000000000, 0.2500000000000000000, 0.2500000000000000000, 0.2500000000000000000, 0.2500000000000000000, 0.2500000000000000000, 0.2500000000000000000 ) ) 
 REPRESENTATION_ITEM ( '' )  );
#4481=CARTESIAN_POINT ( 'NONE',  ( -5.974012367538356294, 36.93458879463112510, -148.2930816546006270 ) ) ;
#4483=CARTESIAN_POINT ( 'NONE',  ( -8.971913342289999704, 37.83624783359999810, -148.2794752869999968 ) ) ;
#4493=CARTESIAN_POINT ( 'NONE',  ( -17.38944842999775986, 40.90832038325887510, -146.3151781682031469 ) ) ;
#4501=CARTESIAN_POINT ( 'NONE',  ( -14.74965217825583963, 40.59671102096088191, -143.6490422507538085 ) ) ;
#4502=CARTESIAN_POINT ( 'NONE',  ( -25.27079369000000142, 34.74837955689999802, -147.2605407199999945 ) ) ;
#4524=CARTESIAN_POINT ( 'NONE',  ( -30.21939605167673903, 40.49321534555046043, -144.7934438824989627 ) ) ;
#4528=VERTEX_POINT ( 'NONE', #12375 ) ;
#4533=CARTESIAN_POINT ( 'NONE',  ( -10.65913935279999869, 37.04331329920000115, -139.7140392919999954 ) ) ;
#4536=CARTESIAN_POINT ( 'NONE',  ( -16.62359605985811228, 34.33467835833456405, -140.1452178716700416 ) ) ;
#4537=CARTESIAN_POINT ( 'NONE',  ( -16.72278394136257873, 36.31586521337963802, -140.5063707124225800 ) ) ;
#4538=CARTESIAN_POINT ( 'NONE',  ( -5.371344480559407053, 37.92202225338002819, -139.4604987659717210 ) ) ;
#4543=CARTESIAN_POINT ( 'NONE',  ( -10.00627339321910370, 35.52121383151546752, -147.2841668858195305 ) ) ;
#4553=CARTESIAN_POINT ( 'NONE',  ( -29.09183339365888799, 35.07783725239920614, -139.7319361797842703 ) ) ;
#4556=CARTESIAN_POINT ( 'NONE',  ( -13.82058007329999860, 36.03909227049999942, -139.5626078809999910 ) ) ;
#4561=CARTESIAN_POINT ( 'NONE',  ( -9.779395745850974819, 34.94622798711487377, -148.4453435301223010 ) ) ;
#4578=CARTESIAN_POINT ( 'NONE',  ( -17.44989882367886125, 40.67283837543727998, -143.6255418396315804 ) ) ;
#4584=CARTESIAN_POINT ( 'NONE',  ( -26.19803085470000070, 35.41001212129999942, -140.6029839040000127 ) ) ;
#4590=CARTESIAN_POINT ( 'NONE',  ( 0.000000000000000000, 0.000000000000000000, 0.000000000000000000 ) ) ;
#4594=EDGE_CURVE ( 'NONE', #20921, #20510, #6428, .T. ) ;
#4604=CARTESIAN_POINT ( 'NONE',  ( -18.48412402369122631, 36.99547888836894316, -147.4161207264432676 ) ) ;
#4607=CARTESIAN_POINT ( 'NONE',  ( -22.00705883600000234, 37.05789963359999462, -148.1619053240000028 ) ) ;
#4629=CARTESIAN_POINT ( 'NONE',  ( -25.64792992843672081, 37.04465132569895758, -139.7265440088568198 ) ) ;
#4632=( BOUNDED_SURFACE ( )  B_SPLINE_SURFACE ( 5, 5, ( 
 ( #10370, #1475, #8821, #15977, #6932, #19663 ),
 ( #3359, #10599, #1601, #12987, #18355, #7399 ),
 ( #18239, #14661, #11186, #16215, #7508, #21700 ),
 ( #10833, #14429, #14897, #156, #7624, #21929 ),
 ( #20021, #7163, #23467, #16558, #2064, #22155 ),
 ( #12864, #41, #5729, #12510, #19792, #5387 ),
 ( #9285, #3485, #10955, #20146, #7287, #20262 ),
 ( #14554, #8934, #3716, #10721, #1827, #14775 ),
 ( #2175, #18002, #12635, #9396, #19906, #16449 ),
 ( #3604, #3954, #1712, #3838, #1952, #5611 ),
 ( #18116, #9044, #21818, #386, #16334, #18462 ),
 ( #5502, #16672, #9172, #12749, #11075, #266 ) ),
 .UNSPECIFIED., .F., .F., .F. ) 
 B_SPLINE_SURFACE_WITH_KNOTS ( ( 6, 3, 3, 6 ),
 ( 6, 6 ),
 ( 0.000000000000000000, 4.059123295939999210, 8.340116530639999581, 12.86134770560000007 ),
 ( 0.000000000000000000, 1.570796326715864888 ),
 .UNSPECIFIED. ) 
 GEOMETRIC_REPRESENTATION_ITEM ( )  RATIONAL_B_SPLINE_SURFACE ( (
 ( 1.000000000000000000, 0.6000000000201509698, 0.4000000000201515138, 0.3000000000151135104, 0.2500000000100754960, 0.2500000000000000000),
 ( 1.000000000000000000, 0.6000000000201509698, 0.4000000000201515138, 0.3000000000151135104, 0.2500000000100754960, 0.2500000000000000000),
 ( 1.000000000000000000, 0.6000000000201509698, 0.4000000000201515138, 0.3000000000151135104, 0.2500000000100754960, 0.2500000000000000000),
 ( 1.000000000000000000, 0.6000000000201509698, 0.4000000000201515138, 0.3000000000151135104, 0.2500000000100754960, 0.2500000000000000000),
 ( 1.000000000000000000, 0.6000000000201509698, 0.4000000000201515138, 0.3000000000151135104, 0.2500000000100754960, 0.2500000000000000000),
 ( 1.000000000000000000, 0.6000000000201509698, 0.4000000000201515138, 0.3000000000151135104, 0.2500000000100754960, 0.2500000000000000000),
 ( 1.000000000000000000, 0.6000000000201509698, 0.4000000000201515138, 0.3000000000151135104, 0.2500000000100754960, 0.2500000000000000000),
 ( 1.000000000000000000, 0.6000000000201509698, 0.4000000000201515138, 0.3000000000151135104, 0.2500000000100754960, 0.2500000000000000000),
 ( 1.000000000000000000, 0.6000000000201509698, 0.4000000000201515138, 0.3000000000151135104, 0.2500000000100754960, 0.2500000000000000000),
 ( 1.000000000000000000, 0.6000000000201509698, 0.4000000000201515138, 0.3000000000151135104, 0.2500000000100754960, 0.2500000000000000000),
 ( 1.000000000000000000, 0.6000000000201509698, 0.4000000000201515138, 0.3000000000151135104, 0.2500000000100754960, 0.2500000000000000000),
 ( 1.000000000000000000, 0.6000000000201509698, 0.4000000000201515138, 0.3000000000151135104, 0.2500000000100754960, 0.2500000000000000000) ) ) 
 REPRESENTATION_ITEM ( '' )  SURFACE ( )  );
#4660=VERTEX_POINT ( 'NONE', #5492 ) ;
#4667=CARTESIAN_POINT ( 'NONE',  ( -10.25355660807601232, 34.02186660424427345, -142.1157150913619773 ) ) ;
#4669=CARTESIAN_POINT ( 'NONE',  ( -27.26567793380000282, 36.96940380710000085, -148.4835048639999968 ) ) ;
#4677=CARTESIAN_POINT ( 'NONE',  ( -23.31072407292720428, 37.69002698299868115, -140.6967118636591181 ) ) ;
#4681=CARTESIAN_POINT ( 'NONE',  ( -9.072898850179999641, 36.94639249900000522, -148.2684494029999769 ) ) ;
#4683=CARTESIAN_POINT ( 'NONE',  ( -7.585922026740613333, 37.83934505584353758, -140.3341826278673636 ) ) ;
#4690=CARTESIAN_POINT ( 'NONE',  ( -6.518232409689999507, 33.41592120480000006, -146.1606736330000160 ) ) ;
#4691=CARTESIAN_POINT ( 'NONE',  ( -29.32937220839999881, 40.41939957099999958, -140.7656299760000138 ) ) ;
#4697=CARTESIAN_POINT ( 'NONE',  ( -21.97930707628684033, 37.84604761964991582, -147.8229183002398770 ) ) ;
#4698=CARTESIAN_POINT ( 'NONE',  ( -17.37084003756964279, 38.37330577533303710, -140.8480132324181966 ) ) ;
#4703=CARTESIAN_POINT ( 'NONE',  ( -24.39503929831862195, 33.43607675443129068, -146.0584967254518460 ) ) ;
#4705=CARTESIAN_POINT ( 'NONE',  ( -10.97748938910000049, 39.75689975739999937, -140.4868351200000234 ) ) ;
#4719=CARTESIAN_POINT ( 'NONE',  ( -18.91006587269999883, 33.19603641719999843, -143.7906546520000006 ) ) ;
#4720=CARTESIAN_POINT ( 'NONE',  ( -10.64004713443764061, 38.83279341006178953, -140.2200294818480302 ) ) ;
#4722=CARTESIAN_POINT ( 'NONE',  ( -8.554523812450000264, 40.80811760249999764, -146.2789059460000090 ) ) ;
#4742=CARTESIAN_POINT ( 'NONE',  ( -25.91593243209636199, 32.87307245982592718, -143.7099744806644139 ) ) ;
#4752=CARTESIAN_POINT ( 'NONE',  ( -24.79371418840000274, 32.62011804889999667, -144.5039952340000013 ) ) ;
#4761=CARTESIAN_POINT ( 'NONE',  ( -14.70777071217397314, 41.11523651854984962, -146.4493477498343168 ) ) ;
#4766=( BOUNDED_SURFACE ( )  B_SPLINE_SURFACE ( 5, 5, ( 
 ( #9375, #11514, #3819, #5822, #18681, #5940 ),
 ( #22363, #18791, #20465, #4046, #14986, #14750 ),
 ( #22247, #12964, #13192, #11399, #2502, #2394 ),
 ( #11054, #13314, #20242, #12840, #11169, #9614 ),
 ( #596, #21909, #9724, #5591, #18441, #9267 ),
 ( #2156, #16999, #16538, #6062, #16887, #14877 ),
 ( #16011, #13987, #13426, #19701, #5176, #8507 ),
 ( #6178, #3395, #8612, #10637, #21259, #12076 ),
 ( #17918, #23276, #1635, #4955, #12199, #6966 ),
 ( #17122, #12424, #14231, #19588, #20695, #19350 ),
 ( #4388, #8396, #15230, #2613, #22484, #11627 ),
 ( #18903, #15777, #17794, #23154, #23039, #6611 ) ),
 .UNSPECIFIED., .F., .F., .F. ) 
 B_SPLINE_SURFACE_WITH_KNOTS ( ( 6, 3, 3, 6 ),
 ( 6, 6 ),
 ( 0.000000000000000000, 4.564346237179999655, 9.066392868600001265, 13.51003987140000007 ),
 ( 1.570796326695754974, 3.141592653590000062 ),
 .UNSPECIFIED. ) 
 GEOMETRIC_REPRESENTATION_ITEM ( )  RATIONAL_B_SPLINE_SURFACE ( (
 ( 0.2500000000000000000, 0.2499999999873634970, 0.2999999999810455398, 0.3999999999747270163, 0.5999999999747269719, 1.000000000000000000),
 ( 0.2500000000000000000, 0.2499999999873634970, 0.2999999999810455398, 0.3999999999747270163, 0.5999999999747269719, 1.000000000000000000),
 ( 0.2500000000000000000, 0.2499999999873634970, 0.2999999999810455398, 0.3999999999747270163, 0.5999999999747269719, 1.000000000000000000),
 ( 0.2500000000000000000, 0.2499999999873634970, 0.2999999999810455398, 0.3999999999747270163, 0.5999999999747269719, 1.000000000000000000),
 ( 0.2500000000000000000, 0.2499999999873634970, 0.2999999999810455398, 0.3999999999747270163, 0.5999999999747269719, 1.000000000000000000),
 ( 0.2500000000000000000, 0.2499999999873634970, 0.2999999999810455398, 0.3999999999747270163, 0.5999999999747269719, 1.000000000000000000),
 ( 0.2500000000000000000, 0.2499999999873634970, 0.2999999999810455398, 0.3999999999747270163, 0.5999999999747269719, 1.000000000000000000),
 ( 0.2500000000000000000, 0.2499999999873634970, 0.2999999999810455398, 0.3999999999747270163, 0.5999999999747269719, 1.000000000000000000),
 ( 0.2500000000000000000, 0.2499999999873634970, 0.2999999999810455398, 0.3999999999747270163, 0.5999999999747269719, 1.000000000000000000),
 ( 0.2500000000000000000, 0.2499999999873634970, 0.2999999999810455398, 0.3999999999747270163, 0.5999999999747269719, 1.000000000000000000),
 ( 0.2500000000000000000, 0.2499999999873634970, 0.2999999999810455398, 0.3999999999747270163, 0.5999999999747269719, 1.000000000000000000),
 ( 0.2500000000000000000, 0.2499999999873634970, 0.2999999999810455398, 0.3999999999747270163, 0.5999999999747269719, 1.000000000000000000) ) ) 
 REPRESENTATION_ITEM ( '' )  SURFACE ( )  );
#4783=CARTESIAN_POINT ( 'NONE',  ( -26.39607007120000048, 36.95534867429999792, -140.3840478969999879 ) ) ;
#4788=CARTESIAN_POINT ( 'NONE',  ( -29.62827070405596430, 36.92763176543257941, -139.7399851633785488 ) ) ;
#4791=ORIENTED_EDGE ( 'NONE', *, *, #23482, .T. ) ;
#4792=CARTESIAN_POINT ( 'NONE',  ( -22.83308877303491968, 39.55027303352079571, -140.7145628013014118 ) ) ;
#4797=CARTESIAN_POINT ( 'NONE',  ( -10.28060652843288025, 34.62853500624063940, -147.1732277804927946 ) ) ;
#4803=SURFACE_SIDE_STYLE ('',( #17534 ) ) ;
#4806=CARTESIAN_POINT ( 'NONE',  ( -6.284562654584142649, 35.48787867574768029, -147.4335637949685065 ) ) ;
#4807=CARTESIAN_POINT ( 'NONE',  ( -25.74743564699999965, 37.94517732370000118, -139.7356315989999871 ) ) ;
#4816=CARTESIAN_POINT ( 'NONE',  ( -17.97686571119999854, 41.53571570570000659, -143.4577736070000071 ) ) ;
#4822=CARTESIAN_POINT ( 'NONE',  ( -25.28614709708956809, 36.22712742843352629, -140.0123646937360036 ) ) ;
#4826=CARTESIAN_POINT ( 'NONE',  ( -23.81889237380000068, 39.38287674749999923, -140.7489234159999967 ) ) ;
#4837=CARTESIAN_POINT ( 'NONE',  ( -9.870393330389999775, 37.85345449830000319, -147.8311166189999994 ) ) ;
#4840=CARTESIAN_POINT ( 'NONE',  ( -7.324031428439999658, 35.31041870520000003, -140.2046280479999893 ) ) ;
#4849=EDGE_CURVE ( 'NONE', #16183, #18180, #22559, .T. ) ;
#4856=CARTESIAN_POINT ( 'NONE',  ( -23.51619327739999932, 36.94101002280000046, -140.1031831869999849 ) ) ;
#4858=ORIENTED_EDGE ( 'NONE', *, *, #16935, .T. ) ;
#4859=CARTESIAN_POINT ( 'NONE',  ( -15.43367019712668053, 41.39476109361318379, -144.4317641176221798 ) ) ;
#4860=CARTESIAN_POINT ( 'NONE',  ( -25.90907760989742670, 37.01347911741230945, -139.4251635482865765 ) ) ;
#4861=ORIENTED_EDGE ( 'NONE', *, *, #8433, .T. ) ;
#4877=CARTESIAN_POINT ( 'NONE',  ( -14.74521098486907889, 37.74183931348511578, -147.9812505911391156 ) ) ;
#4890=CARTESIAN_POINT ( 'NONE',  ( -16.15855174276306272, 35.42854167619758954, -140.1130648018951206 ) ) ;
#4896=CARTESIAN_POINT ( 'NONE',  ( -24.30767937719999949, 40.97374044589999897, -144.4830919949999952 ) ) ;
#4904=CARTESIAN_POINT ( 'NONE',  ( -28.85277900879999891, 34.87340808660000135, -141.1101275619999740 ) ) ;
#4907=( BOUNDED_SURFACE ( )  B_SPLINE_SURFACE ( 5, 5, ( 
 ( #18371, #19924, #7309, #21837, #7526, #20041 ),
 ( #5632, #5520, #12769, #20277, #2192, #10072 ),
 ( #21055, #1310, #12105, #2735, #6284, #13540 ),
 ( #4502, #17351, #6640, #4981, #8424, #21288 ),
 ( #19503, #15339, #22707, #9962, #3197, #11986 ),
 ( #10429, #10322, #6525, #10196, #19141, #1064 ),
 ( #11871, #4742, #15446, #8532, #22595, #838 ),
 ( #19382, #19251, #6754, #14016, #17471, #6400 ),
 ( #20937, #13902, #2964, #15570, #1196, #20811 ),
 ( #15805, #8061, #15694, #11743, #8295, #19024 ),
 ( #17235, #22957, #22835, #946, #21174, #13793 ),
 ( #3088, #8174, #23069, #13662, #4860, #4629 ) ),
 .UNSPECIFIED., .F., .F., .F. ) 
 B_SPLINE_SURFACE_WITH_KNOTS ( ( 6, 3, 3, 6 ),
 ( 6, 6 ),
 ( 0.000000000000000000, 4.454241660750000165, 8.943513424000000711, 13.47090878500000066 ),
 ( 0.000000000000000000, 1.570796327036555029 ),
 .UNSPECIFIED. ) 
 GEOMETRIC_REPRESENTATION_ITEM ( )  RATIONAL_B_SPLINE_SURFACE ( (
 ( 1.000000000000000000, 0.5999999999384889593, 0.3999999999384890037, 0.2999999999538665030, 0.2499999999692444907, 0.2500000000000000000),
 ( 1.000000000000000000, 0.5999999999384889593, 0.3999999999384890037, 0.2999999999538665030, 0.2499999999692444907, 0.2500000000000000000),
 ( 1.000000000000000000, 0.5999999999384889593, 0.3999999999384890037, 0.2999999999538665030, 0.2499999999692444907, 0.2500000000000000000),
 ( 1.000000000000000000, 0.5999999999384889593, 0.3999999999384890037, 0.2999999999538665030, 0.2499999999692444907, 0.2500000000000000000),
 ( 1.000000000000000000, 0.5999999999384889593, 0.3999999999384890037, 0.2999999999538665030, 0.2499999999692444907, 0.2500000000000000000),
 ( 1.000000000000000000, 0.5999999999384889593, 0.3999999999384890037, 0.2999999999538665030, 0.2499999999692444907, 0.2500000000000000000),
 ( 1.000000000000000000, 0.5999999999384889593, 0.3999999999384890037, 0.2999999999538665030, 0.2499999999692444907, 0.2500000000000000000),
 ( 1.000000000000000000, 0.5999999999384889593, 0.3999999999384890037, 0.2999999999538665030, 0.2499999999692444907, 0.2500000000000000000),
 ( 1.000000000000000000, 0.5999999999384889593, 0.3999999999384890037, 0.2999999999538665030, 0.2499999999692444907, 0.2500000000000000000),
 ( 1.000000000000000000, 0.5999999999384889593, 0.3999999999384890037, 0.2999999999538665030, 0.2499999999692444907, 0.2500000000000000000),
 ( 1.000000000000000000, 0.5999999999384889593, 0.3999999999384890037, 0.2999999999538665030, 0.2499999999692444907, 0.2500000000000000000),
 ( 1.000000000000000000, 0.5999999999384889593, 0.3999999999384890037, 0.2999999999538665030, 0.2499999999692444907, 0.2500000000000000000) ) ) 
 REPRESENTATION_ITEM ( '' )  SURFACE ( )  );
#4909=CARTESIAN_POINT ( 'NONE',  ( -23.65394330256869182, 40.08423268064209566, -145.9325622199873465 ) ) ;
#4915=CARTESIAN_POINT ( 'NONE',  ( -5.345822467930000599, 40.94956462150000220, -144.4907973060000188 ) ) ;
#4917=CARTESIAN_POINT ( 'NONE',  ( -9.292483939661099868, 40.96918990792104154, -144.3907905727577941 ) ) ;
#4926=CARTESIAN_POINT ( 'NONE',  ( -7.812322887936786309, 34.92289332027021231, -141.3159265060239704 ) ) ;
#4935=CARTESIAN_POINT ( 'NONE',  ( -21.89685178203216864, 37.04474463553891184, -147.4979728337013682 ) ) ;
#4936=CARTESIAN_POINT ( 'NONE',  ( -18.18930989797999942, 36.96028804431571757, -147.6841622079159890 ) ) ;
#4939=CARTESIAN_POINT ( 'NONE',  ( -7.010349701930000066, 37.05829245179999987, -148.1453878979999956 ) ) ;
#4940=CARTESIAN_POINT ( 'NONE',  ( -15.68268784160000173, 36.02211616019999951, -148.5535485649999998 ) ) ;
#4955=CARTESIAN_POINT ( 'NONE',  ( -28.18916860660990764, 34.88657501822456908, -140.9963367595939872 ) ) ;
#4961=CARTESIAN_POINT ( 'NONE',  ( -12.30631862551127931, 40.23402543387735619, -145.9987124283914000 ) ) ;
#4967=CARTESIAN_POINT ( 'NONE',  ( -28.90798551740000022, 37.01360947639999921, -139.5686590450000040 ) ) ;
#4973=CARTESIAN_POINT ( 'NONE',  ( -20.74418227179999974, 39.28578094470000082, -147.3492911870000057 ) ) ;
#4979=EDGE_CURVE ( 'NONE', #20921, #10191, #16029, .T. ) ;
#4980=CARTESIAN_POINT ( 'NONE',  ( -15.03885004549999849, 41.12207116019999376, -146.4108951270000034 ) ) ;
#4981=CARTESIAN_POINT ( 'NONE',  ( -24.94748837732958080, 34.18267032390015459, -147.9795192610947367 ) ) ;
#4985=ORIENTED_EDGE ( 'NONE', *, *, #8504, .F. ) ;
#5000=CARTESIAN_POINT ( 'NONE',  ( -14.40511015815818041, 39.11695720675039212, -141.1121292871179946 ) ) ;
#5001=CARTESIAN_POINT ( 'NONE',  ( -29.18503926097451995, 39.40432144733799902, -139.9690405635991794 ) ) ;
#5021=EDGE_CURVE ( 'NONE', #20985, #13908, #2204, .T. ) ;
#5022=CARTESIAN_POINT ( 'NONE',  ( -26.29566636579999894, 36.18167175180000328, -140.3932108110000172 ) ) ;
#5025=AXIS2_PLACEMENT_3D ( 'NONE', #4590, #17084, #1161 ) ;
#5036=CARTESIAN_POINT ( 'NONE',  ( -10.24572398529664063, 36.15958899794869552, -148.2198882318936910 ) ) ;
#5045=CARTESIAN_POINT ( 'NONE',  ( -6.812760379890000273, 32.88798608609999974, -143.6676051400000063 ) ) ;
#5046=CARTESIAN_POINT ( 'NONE',  ( -6.807579269459999693, 38.78453684440000160, -147.8970667739999953 ) ) ;
#5065=ORIENTED_EDGE ( 'NONE', *, *, #15126, .F. ) ;
#5072=EDGE_LOOP ( 'NONE', ( #12436, #19935, #10941, #11211 ) ) ;
#5074=CARTESIAN_POINT ( 'NONE',  ( -19.48816230409999761, 36.23023348070000083, -140.2952556289999961 ) ) ;
#5075=CARTESIAN_POINT ( 'NONE',  ( -12.57385931496360065, 38.47543513205931731, -147.4253642442816101 ) ) ;
#5077=CARTESIAN_POINT ( 'NONE',  ( -7.753123200440416696, 36.02113668015080350, -139.3990843276119449 ) ) ;
#5081=CARTESIAN_POINT ( 'NONE',  ( -8.514310886080000529, 36.94123471670000214, -140.1199228270000106 ) ) ;
#5093=CARTESIAN_POINT ( 'NONE',  ( -21.63220705382456899, 37.01315499804844222, -148.7192284428847415 ) ) ;
#5103=CARTESIAN_POINT ( 'NONE',  ( -16.81794493339999619, 37.02435727940000731, -140.5111119820000170 ) ) ;
#5110=CARTESIAN_POINT ( 'NONE',  ( -15.24898703717404125, 36.96741147809888162, -148.5896301378343196 ) ) ;
#5123=CARTESIAN_POINT ( 'NONE',  ( -5.765044504979666584, 41.82099204264250858, -144.5279374446441238 ) ) ;
#5132=CARTESIAN_POINT ( 'NONE',  ( -24.84704225922425280, 37.03879906167826164, -147.5513581852341360 ) ) ;
#5138=( NAMED_UNIT ( * ) PLANE_ANGLE_UNIT ( ) SI_UNIT ( $, .RADIAN. ) );
#5139=FACE_OUTER_BOUND ( 'NONE', #5145, .T. ) ;
#5145=EDGE_LOOP ( 'NONE', ( #8880, #15457, #5544, #4985 ) ) ;
#5146=CARTESIAN_POINT ( 'NONE',  ( -7.484002448341838587, 33.56044099697500371, -143.7975408956788215 ) ) ;
#5147=CARTESIAN_POINT ( 'NONE',  ( -23.03778781510000329, 40.78628791080000582, -141.9896475660000306 ) ) ;
#5156=CARTESIAN_POINT ( 'NONE',  ( -17.98964812810000069, 38.50830570029999933, -147.4920370689999913 ) ) ;
#5163=CARTESIAN_POINT ( 'NONE',  ( -15.79202522179999946, 35.03772048769999969, -148.2850092029999871 ) ) ;
#5171=UNCERTAINTY_MEASURE_WITH_UNIT (LENGTH_MEASURE( 1.000000000000000082E-05 ), #18238, 'distance_accuracy_value', 'NONE');
#5173=B_SPLINE_CURVE_WITH_KNOTS ( 'NONE', 5,
 ( #11814, #2683, #3039, #19200, #15400, #22659, #19092, #10276, #10025, #17301, #15517, #22779 ),
 .UNSPECIFIED., .F., .F.,
 ( 6, 3, 3, 6 ),
 ( 0.000000000000000000, 4.151671928079999851, 8.316542232069998875, 12.50501063799999990 ),
 .UNSPECIFIED. ) ;
#5176=CARTESIAN_POINT ( 'NONE',  ( -28.19843657148410188, 33.49775354811340122, -143.6175028023312166 ) ) ;
#5182=CARTESIAN_POINT ( 'NONE',  ( -19.61368621442406024, 33.72156397702593011, -146.2040437318905788 ) ) ;
#5184=CARTESIAN_POINT ( 'NONE',  ( -11.09715128152969754, 40.92510525134454014, -143.8328159740042338 ) ) ;
#5201=CARTESIAN_POINT ( 'NONE',  ( -12.08222824379999949, 38.77433534089999512, -148.2726881729999775 ) ) ;
#5203=CARTESIAN_POINT ( 'NONE',  ( -22.52056272209999932, 33.27763168300000274, -146.2006519230000094 ) ) ;
#5211=EDGE_CURVE ( 'NONE', #4474, #6561, #3869, .T. ) ;
#5212=CARTESIAN_POINT ( 'NONE',  ( -11.38486064709999823, 36.95668670079999885, -140.3965526140000009 ) ) ;
#5224=CARTESIAN_POINT ( 'NONE',  ( -15.04288342797402578, 38.87661853468269868, -148.3497549206679480 ) ) ;
#5225=CARTESIAN_POINT ( 'NONE',  ( -28.46722477587058009, 38.15066728402772611, -140.0554881084096053 ) ) ;
#5241=CARTESIAN_POINT ( 'NONE',  ( -24.21201708719999957, 40.99356323119999956, -143.6328343570000072 ) ) ;
#5248=( BOUNDED_CURVE ( )  B_SPLINE_CURVE ( 5, ( #765, #6108, #2441, #9893, #5983, #9659 ),
 .UNSPECIFIED., .F., .F. ) 
 B_SPLINE_CURVE_WITH_KNOTS ( ( 6, 6 ),
 ( 1.570796326695738099, 3.141592653590000062 ),
 .UNSPECIFIED. ) 
 CURVE ( )  GEOMETRIC_REPRESENTATION_ITEM ( )  RATIONAL_B_SPLINE_CURVE ( ( 0.2500000000000000000, 0.2499999999873616097, 0.2999999999810423756, 0.3999999999747231860, 0.5999999999747231971, 1.000000000000000000 ) ) 
 REPRESENTATION_ITEM ( '' )  );
#5253=CARTESIAN_POINT ( 'NONE',  ( -29.18503926082679811, 39.40432144733731690, -139.9690405636331718 ) ) ;
#5258=CARTESIAN_POINT ( 'NONE',  ( -11.29029698159100015, 36.23043332057599741, -140.4049246349841837 ) ) ;
#5260=CARTESIAN_POINT ( 'NONE',  ( -9.515077267811255624, 39.13325659334626039, -146.8938814410688849 ) ) ;
#5264=SURFACE_STYLE_USAGE ( .BOTH. , #4803 ) ;
#5272=CARTESIAN_POINT ( 'NONE',  ( -4.683324139160000676, 37.83302525630000446, -140.3020749749999823 ) ) ;
#5304=CARTESIAN_POINT ( 'NONE',  ( -19.42944164597027523, 34.87483979447872429, -147.2857474030845424 ) ) ;
#5305=CARTESIAN_POINT ( 'NONE',  ( -12.41698512492444095, 36.98746477265328991, -147.4237781434714520 ) ) ;
#5326=CARTESIAN_POINT ( 'NONE',  ( -19.14899212251034299, 37.07484167171372746, -147.8220480109189054 ) ) ;
#5332=CARTESIAN_POINT ( 'NONE',  ( -22.00705883600000234, 37.05789963359999462, -148.1619053240000028 ) ) ;
#5341=CARTESIAN_POINT ( 'NONE',  ( -25.74743564683659969, 37.94517732363827633, -139.7356315996115939 ) ) ;
#5347=ORIENTED_EDGE ( 'NONE', *, *, #6481, .F. ) ;
#5348=CARTESIAN_POINT ( 'NONE',  ( -15.57039528540000006, 36.22627288620000030, -147.5570433400000070 ) ) ;
#5355=FACE_OUTER_BOUND ( 'NONE', #16430, .T. ) ;
#5356=CARTESIAN_POINT ( 'NONE',  ( -29.04405754857383926, 38.20917013906876036, -139.5702141475971985 ) ) ;
#5368=CARTESIAN_POINT ( 'NONE',  ( -5.251527070960000820, 40.93408815870000694, -143.6492421949999994 ) ) ;
#5379=CARTESIAN_POINT ( 'NONE',  ( -23.90890255102420525, 36.92681688278783270, -147.8857207497513855 ) ) ;
#5387=CARTESIAN_POINT ( 'NONE',  ( -18.82091118372255778, 33.23810407352063834, -144.5979112941300286 ) ) ;
#5389=CARTESIAN_POINT ( 'NONE',  ( -9.032885736896121287, 36.94161628545217724, -147.5965110584316164 ) ) ;
#5396=CARTESIAN_POINT ( 'NONE',  ( -6.909346445769999789, 37.92300339060000169, -148.1333867879999957 ) ) ;
#5398=( BOUNDED_CURVE ( )  B_SPLINE_CURVE ( 5, ( #11521, #606, #13088, #17008, #14995, #20474 ),
 .UNSPECIFIED., .F., .F. ) 
 B_SPLINE_CURVE_WITH_KNOTS ( ( 6, 6 ),
 ( 1.570796326526077813, 3.141592653590000062 ),
 .UNSPECIFIED. ) 
 CURVE ( )  GEOMETRIC_REPRESENTATION_ITEM ( )  RATIONAL_B_SPLINE_CURVE ( ( 0.2500000000000000555, 0.2499999999657597782, 0.2999999999486396840, 0.3999999999315195232, 0.5999999999315195343, 1.000000000000000000 ) ) 
 REPRESENTATION_ITEM ( '' )  );
#5406=CARTESIAN_POINT ( 'NONE',  ( -17.89449017629999616, 39.21037955089999372, -147.0820833679999851 ) ) ;
#5411=ADVANCED_FACE ( 'NONE', ( #16599 ), #15397, .F. ) ;
#5413=CARTESIAN_POINT ( 'NONE',  ( -17.18002735256250446, 36.98113687425440332, -140.6755148967336595 ) ) ;
#5424=FACE_OUTER_BOUND ( 'NONE', #12549, .T. ) ;
#5425=CARTESIAN_POINT ( 'NONE',  ( -12.56920363940049512, 37.00563451942266369, -148.6543378380284821 ) ) ;
#5431=CARTESIAN_POINT ( 'NONE',  ( -12.04808041671338081, 40.71874701608464164, -143.7411651109900106 ) ) ;
#5443=CARTESIAN_POINT ( 'NONE',  ( -6.033650297970000409, 36.94170754819999303, -147.9652040070000112 ) ) ;
#5448=CARTESIAN_POINT ( 'NONE',  ( -25.74974290510757413, 39.24565833955466587, -141.0594917313689791 ) ) ;
#5450=CARTESIAN_POINT ( 'NONE',  ( -15.27002291891846042, 38.46844526377296347, -147.3668459616297923 ) ) ;
#5456=CARTESIAN_POINT ( 'NONE',  ( -27.10435930909369517, 40.49789879880128041, -141.9338419167955010 ) ) ;
#5460=CARTESIAN_POINT ( 'NONE',  ( -10.22994911489607262, 35.59422248375447140, -140.5010413741651689 ) ) ;
#5465=CARTESIAN_POINT ( 'NONE',  ( -13.91784526140000011, 35.46792342009999288, -140.7554205120000006 ) ) ;
#5472=CARTESIAN_POINT ( 'NONE',  ( -17.75130813170000366, 41.00325609940000504, -141.6328284839999867 ) ) ;
#5473=CARTESIAN_POINT ( 'NONE',  ( -22.21135766849999982, 35.30661492690000358, -147.9492090369999744 ) ) ;
#5485=CARTESIAN_POINT ( 'NONE',  ( -6.622935940118527931, 39.79829474619231888, -147.7685723067526737 ) ) ;
#5490=CARTESIAN_POINT ( 'NONE',  ( -27.77832206610000298, 37.03059619289999915, -147.6270870419999710 ) ) ;
#5492=CARTESIAN_POINT ( 'NONE',  ( -21.03694116389999635, 36.94210036639999828, -147.9486865819999935 ) ) ;
#5494=CARTESIAN_POINT ( 'NONE',  ( -26.33255611194163137, 36.96293009473755831, -139.4434112040621585 ) ) ;
#5497=CARTESIAN_POINT ( 'NONE',  ( -29.57813679455983902, 37.90625934871609815, -140.4594347136643080 ) ) ;
#5498=CARTESIAN_POINT ( 'NONE',  ( -21.13851658209999940, 36.11334442980000148, -147.9366295160000107 ) ) ;
#5501=CARTESIAN_POINT ( 'NONE',  ( -11.65594158663979485, 36.92432879709620863, -140.1042033537094085 ) ) ;
#5502=CARTESIAN_POINT ( 'NONE',  ( -20.45144833149999997, 36.94873838139999833, -139.8044047869999815 ) ) ;
#5513=CARTESIAN_POINT ( 'NONE',  ( -6.599926022991117414, 40.46602300537465879, -145.9459310978139968 ) ) ;
#5520=CARTESIAN_POINT ( 'NONE',  ( -25.20835066603357433, 36.21492759592103283, -148.1779083850792915 ) ) ;
#5528=( BOUNDED_CURVE ( )  B_SPLINE_CURVE ( 5, ( #1361, #20032, #7297, #19561, #19672, #21356, #10729, #19914, #6819, #5046, #5396, #3254 ),
 .UNSPECIFIED., .F., .F. ) 
 B_SPLINE_CURVE_WITH_KNOTS ( ( 6, 3, 3, 6 ),
 ( 0.000000000000000000, 4.445608688430000122, 8.917804078430000558, 13.41780914199999941 ),
 .UNSPECIFIED. ) 
 CURVE ( )  GEOMETRIC_REPRESENTATION_ITEM ( )  RATIONAL_B_SPLINE_CURVE ( ( 0.2500000000000000000, 0.2500000000000000000, 0.2500000000000000000, 0.2500000000000000000, 0.2500000000000000000, 0.2500000000000000000, 0.2500000000000000000, 0.2500000000000000000, 0.2500000000000000000, 0.2500000000000000000, 0.2500000000000000000, 0.2500000000000000000 ) ) 
 REPRESENTATION_ITEM ( '' )  );
#5533=CARTESIAN_POINT ( 'NONE',  ( -17.02323386554646589, 33.09469489192927938, -141.6593809025141013 ) ) ;
#5541=CARTESIAN_POINT ( 'NONE',  ( -20.13043194029999938, 34.25277599949999541, -140.5881547479999938 ) ) ;
#5544=ORIENTED_EDGE ( 'NONE', *, *, #1110, .T. ) ;
#5546=ORIENTED_EDGE ( 'NONE', *, *, #9010, .T. ) ;
#5558=CARTESIAN_POINT ( 'NONE',  ( -25.99376360891585236, 38.42570013690371411, -140.8815290731379832 ) ) ;
#5560=CARTESIAN_POINT ( 'NONE',  ( -23.22979221369066849, 36.01619379403584276, -139.4644529137362952 ) ) ;
#5570=CARTESIAN_POINT ( 'NONE',  ( -10.14672265977482191, 34.69385710102684328, -140.5370343418454979 ) ) ;
#5580=CARTESIAN_POINT ( 'NONE',  ( -29.36003260549882654, 40.56893091388222672, -146.2070596150487916 ) ) ;
#5588=CARTESIAN_POINT ( 'NONE',  ( -17.53224077489999999, 39.64394931100000008, -140.2973660050000149 ) ) ;
#5591=CARTESIAN_POINT ( 'NONE',  ( -27.58442046400475789, 33.75941976971765968, -145.8216020747523487 ) ) ;
#5595=CARTESIAN_POINT ( 'NONE',  ( -5.038554799627442904, 41.08894039876798843, -141.7131813093625681 ) ) ;
#5605=CARTESIAN_POINT ( 'NONE',  ( -23.20965953747223764, 36.97759979273075714, -140.7013664825230705 ) ) ;
#5610=CARTESIAN_POINT ( 'NONE',  ( -11.19828263913021971, 35.50589712243412066, -140.5907466445859768 ) ) ;
#5611=CARTESIAN_POINT ( 'NONE',  ( -19.38605492674887998, 35.40602226203012037, -140.5130341975410317 ) ) ;
#5625=CARTESIAN_POINT ( 'NONE',  ( -6.703522560530410068, 37.74709865770818595, -147.4226397534824287 ) ) ;
#5632=CARTESIAN_POINT ( 'NONE',  ( -25.07725372939999886, 36.26300138690000097, -147.8685835880000070 ) ) ;
#5651=CARTESIAN_POINT ( 'NONE',  ( -18.91006587252563875, 33.19603641697479190, -143.7906546518351831 ) ) ;
#5660=( BOUNDED_CURVE ( )  B_SPLINE_CURVE ( 5, ( #8667, #12360, #23442, #1220, #23092, #23327 ),
 .UNSPECIFIED., .F., .F. ) 
 B_SPLINE_CURVE_WITH_KNOTS ( ( 6, 6 ),
 ( 1.570796326712887714, 3.141592653590000062 ),
 .UNSPECIFIED. ) 
 CURVE ( )  GEOMETRIC_REPRESENTATION_ITEM ( )  RATIONAL_B_SPLINE_CURVE ( ( 0.2499999999999999445, 0.2499999999895451408, 0.2999999999843177001, 0.3999999999790902483, 0.5999999999790902594, 1.000000000000000000 ) ) 
 REPRESENTATION_ITEM ( '' )  );
#5669=CARTESIAN_POINT ( 'NONE',  ( -25.56118619078102583, 37.81731597404795764, -140.4616157252740720 ) ) ;
#5678=CARTESIAN_POINT ( 'NONE',  ( -27.46357115055653253, 41.16992305278137820, -146.3751964293791730 ) ) ;
#5680=CARTESIAN_POINT ( 'NONE',  ( -24.87949572109999963, 37.83967983510000010, -147.8465544160000036 ) ) ;
#5684=CARTESIAN_POINT ( 'NONE',  ( -10.32240832042323220, 36.33503176822112124, -140.3275047487922791 ) ) ;
#5686=CARTESIAN_POINT ( 'NONE',  ( -8.641895390041296920, 41.79448446390107108, -143.5108926868431638 ) ) ;
#5692=CARTESIAN_POINT ( 'NONE',  ( -11.21018092005731326, 39.88389201235554538, -140.2749471409629507 ) ) ;
#5697=CARTESIAN_POINT ( 'NONE',  ( -6.713398844220000328, 32.91877557720000169, -144.5413327229999823 ) ) ;
#5706=CARTESIAN_POINT ( 'NONE',  ( -12.76385253890000016, 37.02886902030000016, -147.6186336929999925 ) ) ;
#5707=CARTESIAN_POINT ( 'NONE',  ( -20.48150773484949028, 41.30355579012158529, -141.6474779220080222 ) ) ;
#5723=CARTESIAN_POINT ( 'NONE',  ( -29.45815224832645640, 36.94793816026548683, -140.4653836173310424 ) ) ;
#5729=CARTESIAN_POINT ( 'NONE',  ( -18.98529451538199808, 32.25804622538513655, -144.7693189751299485 ) ) ;
#5732=CARTESIAN_POINT ( 'NONE',  ( -24.42831371752963676, 38.94399743566808070, -148.4797511750901720 ) ) ;
#5737=CARTESIAN_POINT ( 'NONE',  ( -20.13043194029999938, 34.25277599949999541, -140.5881547479999938 ) ) ;
#5741=CARTESIAN_POINT ( 'NONE',  ( -6.321504075339339224, 40.89356757824499766, -143.5328527138602794 ) ) ;
#5751=CARTESIAN_POINT ( 'NONE',  ( -13.38862532799084804, 35.13131036095179383, -139.8726686351679689 ) ) ;
#5763=FACE_OUTER_BOUND ( 'NONE', #18255, .T. ) ;
#5764=CARTESIAN_POINT ( 'NONE',  ( -9.611837139799998653, 32.98927337829999829, -146.0840312179999785 ) ) ;
#5774=CARTESIAN_POINT ( 'NONE',  ( -20.92079889867846276, 39.38003206206091278, -140.7371765277328279 ) ) ;
#5786=CARTESIAN_POINT ( 'NONE',  ( -26.38328323801417241, 40.40271240115249896, -146.0760205945481118 ) ) ;
#5794=CARTESIAN_POINT ( 'NONE',  ( -27.96130559120596715, 37.85361357870127108, -147.7859560200423061 ) ) ;
#5795=CARTESIAN_POINT ( 'NONE',  ( -14.40511015810000117, 39.11695720679999511, -141.1121292869999877 ) ) ;
#5800=CARTESIAN_POINT ( 'NONE',  ( -6.766664769653541356, 35.09179379324020687, -148.4985462000928180 ) ) ;
#5809=CARTESIAN_POINT ( 'NONE',  ( -12.67903993044300215, 40.83408799367548880, -146.3170871812478708 ) ) ;
#5811=CARTESIAN_POINT ( 'NONE',  ( -29.40140556760018953, 40.21055626237175318, -145.9944493861516435 ) ) ;
#5812=ORIENTED_EDGE ( 'NONE', *, *, #13240, .T. ) ;
#5820=CARTESIAN_POINT ( 'NONE',  ( -20.28536656038299668, 36.96856293253134851, -139.5160734783616476 ) ) ;
#5822=CARTESIAN_POINT ( 'NONE',  ( -27.11867290101617556, 36.95185637389150912, -147.5185143933871075 ) ) ;
#5836=CARTESIAN_POINT ( 'NONE',  ( -22.48976697757457544, 37.06353063726731278, -140.4055699430355730 ) ) ;
#5838=CARTESIAN_POINT ( 'NONE',  ( -21.83347610789999749, 32.92361448670000357, -143.4947777360000032 ) ) ;
#5845=CARTESIAN_POINT ( 'NONE',  ( -23.96729089091851961, 37.81249143152112424, -148.2640374881100058 ) ) ;
#5846=CARTESIAN_POINT ( 'NONE',  ( -16.48779918059999616, 32.42295671489999620, -143.3618442240000093 ) ) ;
#5853=CARTESIAN_POINT ( 'NONE',  ( -5.199058631898605398, 40.19233567625393988, -142.2195710326207347 ) ) ;
#5861=CARTESIAN_POINT ( 'NONE',  ( -13.01778940292994946, 33.53025516020306185, -144.5305955197007393 ) ) ;
#5870=CARTESIAN_POINT ( 'NONE',  ( -28.18164916495271655, 37.07873981898632110, -148.1638686014701989 ) ) ;
#5876=CARTESIAN_POINT ( 'NONE',  ( -13.75718804428722741, 33.24050247982404471, -144.6561462772629056 ) ) ;
#5877=CARTESIAN_POINT ( 'NONE',  ( -10.46662683120000104, 35.31824366040000029, -139.9138328150000063 ) ) ;
#5886=CARTESIAN_POINT ( 'NONE',  ( -21.59845619502680591, 40.49633916123557498, -146.0585726302816454 ) ) ;
#5899=CARTESIAN_POINT ( 'NONE',  ( -26.50527565058495938, 41.51083911114544378, -144.5405030844974021 ) ) ;
#5903=EDGE_CURVE ( 'NONE', #17995, #16183, #6287, .T. ) ;
#5910=CARTESIAN_POINT ( 'NONE',  ( -27.79745750754647560, 38.94545112596043879, -148.2735626928909483 ) ) ;
#5914=CARTESIAN_POINT ( 'NONE',  ( -6.131111726649999483, 36.14321585209999910, -147.9535578170000178 ) ) ;
#5915=CARTESIAN_POINT ( 'NONE',  ( -7.828824709450000086, 39.51093879980000168, -140.6700787229999889 ) ) ;
#5923=CARTESIAN_POINT ( 'NONE',  ( -12.94305406498005162, 37.05025962682652363, -148.5780888799759794 ) ) ;
#5924=CARTESIAN_POINT ( 'NONE',  ( -18.39977846769595615, 38.96581140717537295, -148.3858654058074080 ) ) ;
#5925=CARTESIAN_POINT ( 'NONE',  ( -22.00705883600000234, 37.05789963359999462, -148.1619053240000028 ) ) ;
#5937=CARTESIAN_POINT ( 'NONE',  ( -21.31949744912997957, 39.81204609393142846, -147.9708906465881455 ) ) ;
#5940=CARTESIAN_POINT ( 'NONE',  ( -27.77832206610000298, 37.03059619289999915, -147.6270870419999710 ) ) ;
#5951=CARTESIAN_POINT ( 'NONE',  ( -23.38637323487361286, 36.19895251858893204, -140.4460590724356450 ) ) ;
#5952=CARTESIAN_POINT ( 'NONE',  ( -30.26175564716108823, 41.48858102658289226, -145.0104668248091286 ) ) ;
#5958=EDGE_CURVE ( 'NONE', #22397, #18180, #8707, .T. ) ;
#5960=CARTESIAN_POINT ( 'NONE',  ( -9.389499115566652065, 36.98418387195368950, -147.3811924092332788 ) ) ;
#5962=CARTESIAN_POINT ( 'NONE',  ( -24.08804847542923255, 41.25040067026291979, -146.5677998250044425 ) ) ;
#5964=CARTESIAN_POINT ( 'NONE',  ( -15.35382742459208494, 35.97464847315127656, -148.5826496918325859 ) ) ;
#5966=CARTESIAN_POINT ( 'NONE',  ( -17.23374593961228740, 34.42700048754028330, -140.4054235586860955 ) ) ;
#5972=CARTESIAN_POINT ( 'NONE',  ( -5.673950476189068226, 38.39705415069988703, -140.7335603934562585 ) ) ;
#5978=CARTESIAN_POINT ( 'NONE',  ( -12.18657821949179798, 35.21158449346761898, -148.0902736314953643 ) ) ;
#5983=CARTESIAN_POINT ( 'NONE',  ( -27.49486172903680981, 36.99676060752976525, -147.4549925864818363 ) ) ;
#5988=CARTESIAN_POINT ( 'NONE',  ( -28.72801644006947797, 33.22604713767264428, -144.4610326614979954 ) ) ;
#5992=CARTESIAN_POINT ( 'NONE',  ( -6.389646268539595830, 36.98420143703149421, -147.3954793909555008 ) ) ;
#6003=CARTESIAN_POINT ( 'NONE',  ( -20.36280570450795935, 40.92149091605320166, -144.5882336176783838 ) ) ;
#6005=( BOUNDED_CURVE ( )  B_SPLINE_CURVE ( 5, ( #15554, #22463, #2596, #21039, #820, #13408 ),
 .UNSPECIFIED., .F., .F. ) 
 B_SPLINE_CURVE_WITH_KNOTS ( ( 6, 6 ),
 ( 1.570796326821625177, 3.141592653590000062 ),
 .UNSPECIFIED. ) 
 CURVE ( )  GEOMETRIC_REPRESENTATION_ITEM ( )  RATIONAL_B_SPLINE_CURVE ( ( 0.2500000000000000000, 0.2500000000033899550, 0.3000000000050849769, 0.4000000000067799877, 0.6000000000067799988, 1.000000000000000000 ) ) 
 REPRESENTATION_ITEM ( '' )  );
#6017=CARTESIAN_POINT ( 'NONE',  ( -26.92260725150358525, 38.41501433962203294, -147.3424669775142206 ) ) ;
#6025=CARTESIAN_POINT ( 'NONE',  ( -26.73151279712584127, 41.02465574057303854, -146.3859699703060073 ) ) ;
#6027=CARTESIAN_POINT ( 'NONE',  ( -15.17828643430000035, 39.13746915040000118, -146.9793796819999727 ) ) ;
#6031=CARTESIAN_POINT ( 'NONE',  ( -7.305231917203080627, 34.61982510850948103, -147.5275646996967964 ) ) ;
#6033=CARTESIAN_POINT ( 'NONE',  ( -7.955559433785680312, 37.98585944842262307, -139.4072494953622083 ) ) ;
#6045=CARTESIAN_POINT ( 'NONE',  ( -12.63886943596979684, 40.45021591189686916, -146.0874523975345483 ) ) ;
#6059=CARTESIAN_POINT ( 'NONE',  ( -20.75267599334476643, 38.70207599832220069, -148.1344118532358323 ) ) ;
#6062=CARTESIAN_POINT ( 'NONE',  ( -27.75437169045599006, 33.36630509636427178, -144.3381695521194104 ) ) ;
#6078=CARTESIAN_POINT ( 'NONE',  ( -22.42941481617252109, 36.22509709906984199, -139.9955747711319702 ) ) ;
#6079=CARTESIAN_POINT ( 'NONE',  ( -30.57243748982824982, 40.56622750711377279, -145.3687906872534654 ) ) ;
#6090=CARTESIAN_POINT ( 'NONE',  ( -15.05377294108086517, 35.21183796446418057, -147.7020849018581146 ) ) ;
#6091=CARTESIAN_POINT ( 'NONE',  ( -17.18002735256251512, 36.98113687425442464, -140.6755148967337448 ) ) ;
#6098=CARTESIAN_POINT ( 'NONE',  ( -10.10076658436545216, 34.84004213900681890, -146.8689366150676960 ) ) ;
#6102=CARTESIAN_POINT ( 'NONE',  ( -22.37635798571903223, 34.72418241744752976, -147.2189273405841732 ) ) ;
#6105=CARTESIAN_POINT ( 'NONE',  ( -12.82588262004118818, 32.50735092710331031, -143.6846524684992232 ) ) ;
#6108=CARTESIAN_POINT ( 'NONE',  ( -26.92552552937695154, 36.92880110468701105, -148.2769915172783328 ) ) ;
#6111=FACE_OUTER_BOUND ( 'NONE', #21017, .T. ) ;
#6113=CARTESIAN_POINT ( 'NONE',  ( -28.16296462212046947, 36.26993904298343807, -147.8125575884918703 ) ) ;
#6114=ORIENTED_EDGE ( 'NONE', *, *, #23106, .T. ) ;
#6115=CARTESIAN_POINT ( 'NONE',  ( -14.40594365123728693, 36.16454659438798558, -140.4790970264384953 ) ) ;
#6123=VERTEX_POINT ( 'NONE', #933 ) ;
#6125=CARTESIAN_POINT ( 'NONE',  ( -20.66689333112363869, 40.05648423817540760, -142.3232910573508150 ) ) ;
#6131=CARTESIAN_POINT ( 'NONE',  ( -24.39187863320301730, 34.86260241805631921, -146.9285476356863285 ) ) ;
#6148=CARTESIAN_POINT ( 'NONE',  ( -27.16475626468855964, 37.90277890276032480, -148.4897851378476048 ) ) ;
#6153=CARTESIAN_POINT ( 'NONE',  ( -6.272593219194217085, 34.41819306988834626, -147.6053705869175019 ) ) ;
#6154=CARTESIAN_POINT ( 'NONE',  ( -9.197324267851360702, 40.96642299144375698, -143.5436038170500126 ) ) ;
#6171=ORIENTED_EDGE ( 'NONE', *, *, #8046, .F. ) ;
#6173=CARTESIAN_POINT ( 'NONE',  ( -20.22605346220231937, 41.30495387708683097, -144.6507171862060090 ) ) ;
#6175=ORIENTED_EDGE ( 'NONE', *, *, #23106, .F. ) ;
#6178=CARTESIAN_POINT ( 'NONE',  ( -28.37825339590731843, 32.94869610818383876, -141.6352474658662004 ) ) ;
#6186=CARTESIAN_POINT ( 'NONE',  ( -10.07619956200000111, 36.21908991349999951, -147.8536995439999941 ) ) ;
#6204=CARTESIAN_POINT ( 'NONE',  ( -25.10891061333510166, 37.07005729393355864, -148.1636427046707070 ) ) ;
#6205=CARTESIAN_POINT ( 'NONE',  ( -15.55493608092991131, 33.62053755351711715, -145.7762437450627431 ) ) ;
#6209=CARTESIAN_POINT ( 'NONE',  ( -19.91220883949999987, 32.96944242089999477, -141.9853941000000077 ) ) ;
#6219=CARTESIAN_POINT ( 'NONE',  ( -22.03156944975851772, 33.39557638515176308, -141.8445571065512070 ) ) ;
#6222=CARTESIAN_POINT ( 'NONE',  ( -22.89493301684351678, 37.73932509630494536, -140.7085940212591595 ) ) ;
#6227=CARTESIAN_POINT ( 'NONE',  ( -8.657020695883439032, 38.42035764118494967, -140.6896201932340773 ) ) ;
#6229=CARTESIAN_POINT ( 'NONE',  ( -28.07061429630000049, 34.82490105569999628, -147.0351741510000068 ) ) ;
#6234=CARTESIAN_POINT ( 'NONE',  ( -13.37265858230000148, 32.83955069500000690, -141.7941727500000013 ) ) ;
#6243=CARTESIAN_POINT ( 'NONE',  ( -18.37171575634234699, 40.97338532158482138, -143.4834898677627564 ) ) ;
#6246=CARTESIAN_POINT ( 'NONE',  ( -25.64792992871111821, 37.04465132566619445, -139.7265440085400030 ) ) ;
#6264=CARTESIAN_POINT ( 'NONE',  ( -10.43323856990612875, 37.07027821888497954, -139.9576636760149313 ) ) ;
#6265=CARTESIAN_POINT ( 'NONE',  ( -12.76385253890000016, 37.02886902030000016, -147.6186336929999925 ) ) ;
#6267=CARTESIAN_POINT ( 'NONE',  ( -9.953901650897908127, 37.05155446197428404, -148.5872971972359551 ) ) ;
#6284=CARTESIAN_POINT ( 'NONE',  ( -24.42715506630251454, 35.06635613588049694, -148.3612119513088885 ) ) ;
#6287=( BOUNDED_CURVE ( )  B_SPLINE_CURVE ( 5, ( #1818, #10822, #3597, #7928, #2485, #1704 ),
 .UNSPECIFIED., .F., .F. ) 
 B_SPLINE_CURVE_WITH_KNOTS ( ( 6, 6 ),
 ( 0.000000000000000000, 1.570796326807921472 ),
 .UNSPECIFIED. ) 
 CURVE ( )  GEOMETRIC_REPRESENTATION_ITEM ( )  RATIONAL_B_SPLINE_CURVE ( ( 1.000000000000000000, 0.5999999999967096098, 0.3999999999967095987, 0.2999999999975321852, 0.2499999999983548160, 0.2500000000000000000 ) ) 
 REPRESENTATION_ITEM ( '' )  );
#6316=CARTESIAN_POINT ( 'NONE',  ( -16.80500177779741122, 32.51593824403059330, -143.4123969145075534 ) ) ;
#6317=CARTESIAN_POINT ( 'NONE',  ( -4.584402860569999127, 37.05223431090000474, -140.2914745300000163 ) ) ;
#6321=CARTESIAN_POINT ( 'NONE',  ( -10.52090578602543758, 33.54316366365962665, -143.5130757456077504 ) ) ;
#6329=CARTESIAN_POINT ( 'NONE',  ( -22.19109655566130357, 33.58841674673155353, -143.6176153979714911 ) ) ;
#6332=CARTESIAN_POINT ( 'NONE',  ( -23.82499398344462449, 40.43198470725418758, -143.7282993410326810 ) ) ;
#6338=CARTESIAN_POINT ( 'NONE',  ( -10.14042191040790009, 37.07381867795185570, -148.2039739393879074 ) ) ;
#6348=CARTESIAN_POINT ( 'NONE',  ( -13.47165290112877933, 33.35876621949892495, -143.8174469061082164 ) ) ;
#6350=CARTESIAN_POINT ( 'NONE',  ( -4.565705854129999963, 38.02161370010000496, -148.1538225310000030 ) ) ;
#6357=CARTESIAN_POINT ( 'NONE',  ( -18.25771465379125758, 41.35085647821183841, -143.4491198483315202 ) ) ;
#6362=CARTESIAN_POINT ( 'NONE',  ( -24.90252082163620173, 32.60880315492728698, -143.5690609613722017 ) ) ;
#6368=CARTESIAN_POINT ( 'NONE',  ( -26.92552552937697996, 36.92880110468703947, -148.2769915172784181 ) ) ;
#6374=ORIENTED_EDGE ( 'NONE', *, *, #12755, .F. ) ;
#6377=CARTESIAN_POINT ( 'NONE',  ( -18.18930989791016017, 36.96028804430739712, -147.6841622079794263 ) ) ;
#6380=CARTESIAN_POINT ( 'NONE',  ( -7.856058713508018876, 37.01980778200626077, -139.4032252962329324 ) ) ;
#6381=CARTESIAN_POINT ( 'NONE',  ( -9.971101149592600521, 37.05360750091987398, -147.8421425030599892 ) ) ;
#6391=CARTESIAN_POINT ( 'NONE',  ( -18.08788331829543949, 37.73304001162023980, -147.6923967947225833 ) ) ;
#6396=CARTESIAN_POINT ( 'NONE',  ( -21.89685178209297334, 37.04474463554617358, -147.4979728338151119 ) ) ;
#6397=CARTESIAN_POINT ( 'NONE',  ( -18.64767072899999789, 38.89869937459999960, -148.1651290810000319 ) ) ;
#6399=CARTESIAN_POINT ( 'NONE',  ( -14.60833405737009905, 37.68941485723577500, -140.4549841786794957 ) ) ;
#6400=CARTESIAN_POINT ( 'NONE',  ( -25.12153080207939837, 33.08100675596072193, -141.7696838824860208 ) ) ;
#6416=EDGE_CURVE ( 'NONE', #9000, #4474, #11146, .T. ) ;
#6428=( BOUNDED_CURVE ( )  B_SPLINE_CURVE ( 5, ( #1701, #3471, #8920, #14760, #22027, #17869 ),
 .UNSPECIFIED., .F., .F. ) 
 B_SPLINE_CURVE_WITH_KNOTS ( ( 6, 6 ),
 ( 1.570796326769926310, 3.141592653590000062 ),
 .UNSPECIFIED. ) 
 CURVE ( )  GEOMETRIC_REPRESENTATION_ITEM ( )  RATIONAL_B_SPLINE_CURVE ( ( 0.2499999999999999445, 0.2499999999968074982, 0.2999999999952112639, 0.3999999999936150186, 0.5999999999936149742, 1.000000000000000000 ) ) 
 REPRESENTATION_ITEM ( '' )  );
#6432=CARTESIAN_POINT ( 'NONE',  ( -11.26413364422059082, 36.97109742518000530, -139.4278719022547079 ) ) ;
#6444=CARTESIAN_POINT ( 'NONE',  ( -9.857095426776597336, 33.85551485821954287, -145.6647977573206560 ) ) ;
#6457=CARTESIAN_POINT ( 'NONE',  ( -23.49236497903126164, 40.48720019302773210, -144.5163663921258603 ) ) ;
#6461=CARTESIAN_POINT ( 'NONE',  ( -9.178237216079999428, 36.01795878010000251, -148.2568923610000127 ) ) ;
#6463=CARTESIAN_POINT ( 'NONE',  ( -7.977873771066918529, 39.10042569864757667, -141.2099287470478828 ) ) ;
#6471=CARTESIAN_POINT ( 'NONE',  ( -6.998540199153231001, 33.60912705789826305, -142.1258228245172290 ) ) ;
#6478=ADVANCED_FACE ( 'NONE', ( #2224 ), #14640, .F. ) ;
#6480=CARTESIAN_POINT ( 'NONE',  ( -21.79874322595727421, 37.75473737279066455, -147.4889873734535399 ) ) ;
#6481=EDGE_CURVE ( 'NONE', #10191, #19149, #8850, .T. ) ;
#6483=CARTESIAN_POINT ( 'NONE',  ( -18.99860119798404412, 37.95224228446289061, -148.1887462952859096 ) ) ;
#6489=CARTESIAN_POINT ( 'NONE',  ( -25.13189125417029501, 34.91836258124934744, -146.9977978136419949 ) ) ;
#6491=CARTESIAN_POINT ( 'NONE',  ( -13.18072986969131932, 37.07863008620352474, -148.2345011165226651 ) ) ;
#6505=CARTESIAN_POINT ( 'NONE',  ( -18.66943014212572649, 35.65202800753842638, -147.2469133860827526 ) ) ;
#6507=CARTESIAN_POINT ( 'NONE',  ( -10.65913935279999869, 37.04331329920000115, -139.7140392919999954 ) ) ;
#6508=CARTESIAN_POINT ( 'NONE',  ( -6.812760379890000273, 32.88798608609999974, -143.6676051400000063 ) ) ;
#6524=CARTESIAN_POINT ( 'NONE',  ( -14.11967125435642068, 36.98834135279123814, -140.5455248811313993 ) ) ;
#6525=CARTESIAN_POINT ( 'NONE',  ( -25.75289790537111045, 32.48043154014510492, -144.6283460670170768 ) ) ;
#6543=CARTESIAN_POINT ( 'NONE',  ( -14.74965217832113851, 40.59671102096423567, -143.6490422507460210 ) ) ;
#6558=CARTESIAN_POINT ( 'NONE',  ( -5.459597139290000456, 36.94776568910000236, -139.8191173760000083 ) ) ;
#6561=VERTEX_POINT ( 'NONE', #23262 ) ;
#6562=CARTESIAN_POINT ( 'NONE',  ( -9.285539185979999388, 35.09287230280000358, -147.9937876190000168 ) ) ;
#6565=( GEOMETRIC_REPRESENTATION_CONTEXT ( 3 ) GLOBAL_UNCERTAINTY_ASSIGNED_CONTEXT ( ( #2092 ) ) GLOBAL_UNIT_ASSIGNED_CONTEXT ( ( #8479, #23124, #7050 ) ) REPRESENTATION_CONTEXT ( 'NONE', 'WORKASPACE' ) );
#6572=CARTESIAN_POINT ( 'NONE',  ( -22.48976697756137710, 37.06353063726883335, -140.4055699430226412 ) ) ;
#6576=CARTESIAN_POINT ( 'NONE',  ( -9.562013113524754360, 37.00477621356877478, -148.7272342976183381 ) ) ;
#6580=B_SPLINE_CURVE_WITH_KNOTS ( 'NONE', 5,
 ( #20378, #18716, #11307, #20618, #18584, #9403, #14905, #6209, #5737, #4313, #16914, #11542 ),
 .UNSPECIFIED., .F., .F.,
 ( 6, 3, 3, 6 ),
 ( 0.000000000000000000, 4.059123295939999210, 8.340116530639999581, 12.86134770560000007 ),
 .UNSPECIFIED. ) ;
#6582=CARTESIAN_POINT ( 'NONE',  ( -21.03694116386247970, 36.94210036639699979, -147.9486865819903869 ) ) ;
#6584=CARTESIAN_POINT ( 'NONE',  ( -8.262608331957180141, 35.43026936969504703, -140.7385567855430963 ) ) ;
#6585=CARTESIAN_POINT ( 'NONE',  ( -29.55850978550000363, 41.47329217819999769, -142.4456950389999861 ) ) ;
#6591=ORIENTED_EDGE ( 'NONE', *, *, #23033, .T. ) ;
#6592=CARTESIAN_POINT ( 'NONE',  ( -21.88274988998765735, 38.62264069534737843, -147.6131461927444377 ) ) ;
#6594=CARTESIAN_POINT ( 'NONE',  ( -17.22605506639999717, 36.97564272059999979, -139.5994799229999899 ) ) ;
#6598=CARTESIAN_POINT ( 'NONE',  ( -24.79371418848295860, 32.62011804878908094, -144.5039952333927999 ) ) ;
#6601=EDGE_CURVE ( 'NONE', #20510, #19149, #9595, .T. ) ;
#6611=CARTESIAN_POINT ( 'NONE',  ( -29.13601448249999848, 36.98639052360000079, -140.5419328609999923 ) ) ;
#6616=CARTESIAN_POINT ( 'NONE',  ( -18.99756833806441492, 36.36014154320098157, -147.4937258815151608 ) ) ;
#6619=CARTESIAN_POINT ( 'NONE',  ( -7.344042119375912669, 32.21321104593293683, -144.7067442997065996 ) ) ;
#6620=CARTESIAN_POINT ( 'NONE',  ( -9.007281809890079316, 38.87169400220813742, -148.3307225037476371 ) ) ;
#6631=ORIENTED_EDGE ( 'NONE', *, *, #17358, .F. ) ;
#6636=CARTESIAN_POINT ( 'NONE',  ( -20.28536656041405450, 36.96856293252766790, -139.5160734784155636 ) ) ;
#6639=CARTESIAN_POINT ( 'NONE',  ( -14.78397831697835763, 38.75612598996944769, -139.9015999578828655 ) ) ;
#6640=CARTESIAN_POINT ( 'NONE',  ( -25.30581943868956429, 34.34500769354227856, -147.8257434426395207 ) ) ;
#6644=CARTESIAN_POINT ( 'NONE',  ( -11.86981903010000039, 40.35288497620000214, -142.1893091610000113 ) ) ;
#6656=CARTESIAN_POINT ( 'NONE',  ( -15.14817811019070248, 37.92142832241574268, -148.5963073275012221 ) ) ;
#6670=CARTESIAN_POINT ( 'NONE',  ( -5.480550747629762576, 36.94526453639895180, -140.5641745855584190 ) ) ;
#6674=CARTESIAN_POINT ( 'NONE',  ( -10.41700570847820551, 37.07221587398769458, -140.3414633426675380 ) ) ;
#6676=CARTESIAN_POINT ( 'NONE',  ( -25.73504040789999792, 33.16200571349999393, -143.7184748760000161 ) ) ;
#6679=CARTESIAN_POINT ( 'NONE',  ( -29.17292895941881881, 34.79208654433700332, -141.0602999640023256 ) ) ;
#6684=CARTESIAN_POINT ( 'NONE',  ( -22.96991264454272752, 40.42754630402341576, -142.1998910728711962 ) ) ;
#6690=CARTESIAN_POINT ( 'NONE',  ( -10.05941948556869292, 36.05287800962796751, -148.5984116296196476 ) ) ;
#6699=CARTESIAN_POINT ( 'NONE',  ( -6.486810516462077736, 36.30202410411560976, -147.3923230133318043 ) ) ;
#6700=CARTESIAN_POINT ( 'NONE',  ( -29.94412816099999830, 41.23953273989999957, -145.7122098469999969 ) ) ;
#6708=CARTESIAN_POINT ( 'NONE',  ( -18.58114728243741709, 40.89578867383085736, -146.1569481741396999 ) ) ;
#6712=CARTESIAN_POINT ( 'NONE',  ( -7.081915218180246718, 37.06683495600067602, -147.7519347211649006 ) ) ;
#6746=CARTESIAN_POINT ( 'NONE',  ( -20.36280570459999595, 40.92149091569999797, -144.5882336180000038 ) ) ;
#6752=CARTESIAN_POINT ( 'NONE',  ( -14.56152959349201481, 39.73338309561681569, -140.2290243436648609 ) ) ;
#6754=CARTESIAN_POINT ( 'NONE',  ( -26.09056442780078910, 32.98054588081366489, -141.8362709652814715 ) ) ;
#6762=EDGE_CURVE ( 'NONE', #20510, #20921, #18452, .T. ) ;
#6770=( BOUNDED_CURVE ( )  B_SPLINE_CURVE ( 5, ( #4107, #18050, #7674, #18396, #11122, #21970 ),
 .UNSPECIFIED., .F., .F. ) 
 B_SPLINE_CURVE_WITH_KNOTS ( ( 6, 6 ),
 ( 0.000000000000000000, 1.570796326683616906 ),
 .UNSPECIFIED. ) 
 CURVE ( )  GEOMETRIC_REPRESENTATION_ITEM ( )  RATIONAL_B_SPLINE_CURVE ( ( 1.000000000000000000, 0.6000000000283634005, 0.4000000000283634449, 0.3000000000212725837, 0.2500000000141817114, 0.2499999999999999722 ) ) 
 REPRESENTATION_ITEM ( '' )  );
#6773=CARTESIAN_POINT ( 'NONE',  ( -14.93328160134642957, 36.92972691758554049, -148.3740393307390661 ) ) ;
#6786=CARTESIAN_POINT ( 'NONE',  ( -17.22605506639999717, 36.97564272059999979, -139.5994799229999899 ) ) ;
#6809=CARTESIAN_POINT ( 'NONE',  ( -4.683324139160000676, 37.83302525630000446, -140.3020749749999823 ) ) ;
#6818=CARTESIAN_POINT ( 'NONE',  ( -7.593515551632238569, 36.30629168799562478, -140.6345953673100553 ) ) ;
#6819=CARTESIAN_POINT ( 'NONE',  ( -6.705189174439999178, 39.56570632409999888, -147.4373625599999968 ) ) ;
#6830=CARTESIAN_POINT ( 'NONE',  ( -19.14899212251805949, 37.07484167171462275, -147.8220480108583956 ) ) ;
#6834=CARTESIAN_POINT ( 'NONE',  ( -17.22605506639999717, 36.97564272059999979, -139.5994799229999899 ) ) ;
#6842=CARTESIAN_POINT ( 'NONE',  ( -29.13601448249999848, 36.98639052360000079, -140.5419328609999923 ) ) ;
#6846=CARTESIAN_POINT ( 'NONE',  ( -16.16658683015744202, 37.07694188522086876, -148.2333767340493011 ) ) ;
#6858=CARTESIAN_POINT ( 'NONE',  ( -8.411849887919201407, 36.09637009089656345, -140.1322081666141912 ) ) ;
#6874=CARTESIAN_POINT ( 'NONE',  ( -21.84190187641215886, 35.02767429215685269, -148.4596182608835875 ) ) ;
#6893=CARTESIAN_POINT ( 'NONE',  ( -14.35880640235731143, 41.60548537699954608, -143.5801344958343861 ) ) ;
#6912=CARTESIAN_POINT ( 'NONE',  ( -5.345822467930000599, 40.94956462150000220, -144.4907973060000188 ) ) ;
#6931=CARTESIAN_POINT ( 'NONE',  ( -11.49975391485736509, 36.06355900336099296, -139.6950141698461891 ) ) ;
#6932=CARTESIAN_POINT ( 'NONE',  ( -17.89449577229611776, 36.92509720026576758, -147.9522036891032428 ) ) ;
#6940=CARTESIAN_POINT ( 'NONE',  ( -7.366919058817297028, 34.86075545065775572, -147.1984919235340783 ) ) ;
#6941=CARTESIAN_POINT ( 'NONE',  ( -23.96729089089999931, 37.81249143149999981, -148.2640374880000138 ) ) ;
#6945=CARTESIAN_POINT ( 'NONE',  ( -5.195035615602224155, 37.68216517631442741, -140.7224638479279690 ) ) ;
#6961=CARTESIAN_POINT ( 'NONE',  ( -23.75346069390047887, 38.76012023700184983, -139.9914357966623015 ) ) ;
#6966=CARTESIAN_POINT ( 'NONE',  ( -28.85277900879999891, 34.87340808660000135, -141.1101275619999740 ) ) ;
#6971=B_SPLINE_CURVE_WITH_KNOTS ( 'NONE', 5,
 ( #7261, #9491, #15095, #14873, #22014, #20345, #2266, #7826, #22131, #4040, #11507, #16764 ),
 .UNSPECIFIED., .F., .F.,
 ( 6, 3, 3, 6 ),
 ( 0.000000000000000000, 4.564346237179999655, 9.066392868600001265, 13.51003987140000007 ),
 .UNSPECIFIED. ) ;
#6972=CARTESIAN_POINT ( 'NONE',  ( -19.74460998602464201, 33.84556549679342652, -142.4254691117371578 ) ) ;
#6973=CARTESIAN_POINT ( 'NONE',  ( -12.22876056493469221, 38.35711075933631520, -147.2541758749702581 ) ) ;
#6993=ORIENTED_EDGE ( 'NONE', *, *, #4594, .T. ) ;
#6995=CARTESIAN_POINT ( 'NONE',  ( -21.33871772395523791, 34.54066873271768401, -147.2646375961022045 ) ) ;
#6996=CARTESIAN_POINT ( 'NONE',  ( -29.13601448249999848, 36.98639052360000079, -140.5419328609999923 ) ) ;
#7000=CARTESIAN_POINT ( 'NONE',  ( -26.22336464713773196, 39.81244140399248721, -140.1811132391529497 ) ) ;
#7006=CARTESIAN_POINT ( 'NONE',  ( -13.64404366370000155, 33.71937897319999422, -142.3027892629999940 ) ) ;
#7011=CARTESIAN_POINT ( 'NONE',  ( -14.83278250960868050, 40.60058613835127517, -144.4189779529964142 ) ) ;
#7015=EDGE_CURVE ( 'NONE', #4660, #19550, #20898, .T. ) ;
#7016=CARTESIAN_POINT ( 'NONE',  ( -26.17844700328911145, 36.98132551454334305, -140.6351982806022818 ) ) ;
#7019=CARTESIAN_POINT ( 'NONE',  ( -24.97797643630000053, 37.05442817780000553, -147.8575004449999994 ) ) ;
#7027=CARTESIAN_POINT ( 'NONE',  ( -6.464115716629577513, 37.99579816708060065, -148.7400127089275372 ) ) ;
#7037=CARTESIAN_POINT ( 'NONE',  ( -24.56431249151015805, 39.13927797951933485, -146.9768926602517354 ) ) ;
#7038=CARTESIAN_POINT ( 'NONE',  ( -29.93285177491310378, 39.00107643762004273, -140.4906359816092447 ) ) ;
#7050=( NAMED_UNIT ( * ) SI_UNIT ( $, .STERADIAN. ) SOLID_ANGLE_UNIT ( ) );
#7073=CARTESIAN_POINT ( 'NONE',  ( -26.39607007120000048, 36.95534867429999792, -140.3840478969999879 ) ) ;
#7085=CARTESIAN_POINT ( 'NONE',  ( -15.67014142446072178, 35.45905754578375024, -147.3461856841366000 ) ) ;
#7091=CARTESIAN_POINT ( 'NONE',  ( -20.54812748657687038, 36.93719815735425271, -140.4704715740689949 ) ) ;
#7092=CARTESIAN_POINT ( 'NONE',  ( -11.92782157744108140, 37.65756807781640703, -147.5967280858595245 ) ) ;
#7105=CARTESIAN_POINT ( 'NONE',  ( -18.85469010170000459, 37.03971195569999963, -148.4264296979999926 ) ) ;
#7109=CARTESIAN_POINT ( 'NONE',  ( -11.53909816450000037, 41.50279269539999660, -144.7127947380000137 ) ) ;
#7125=CARTESIAN_POINT ( 'NONE',  ( -16.63107678139999734, 35.60580843630000203, -140.6802342589999739 ) ) ;
#7132=CARTESIAN_POINT ( 'NONE',  ( -28.72360428835138535, 40.14058537508078928, -141.1268109065168801 ) ) ;
#7144=CARTESIAN_POINT ( 'NONE',  ( -13.60030749279999895, 34.19157895370000233, -140.3499153360000093 ) ) ;
#7145=CARTESIAN_POINT ( 'NONE',  ( -6.244164552826013015, 39.88079648725181414, -147.9541347234863622 ) ) ;
#7157=CARTESIAN_POINT ( 'NONE',  ( -29.62827070404598118, 36.92763176543375891, -139.7399851633028618 ) ) ;
#7162=CARTESIAN_POINT ( 'NONE',  ( -10.96486579892240520, 34.29678926733738820, -140.1220017724852482 ) ) ;
#7163=CARTESIAN_POINT ( 'NONE',  ( -19.13109106545264737, 32.92487917598572267, -146.6426253244906945 ) ) ;
#7164=CARTESIAN_POINT ( 'NONE',  ( -9.870393330421920908, 37.85345449832967546, -147.8311166192347912 ) ) ;
#7175=CARTESIAN_POINT ( 'NONE',  ( -5.096343650290934058, 36.99112588043591643, -140.7242647647981073 ) ) ;
#7196=( BOUNDED_SURFACE ( )  B_SPLINE_SURFACE ( 5, 5, ( 
 ( #16479, #18151, #12902, #20183, #5425, #22077 ),
 ( #1865, #12546, #3984, #3873, #16135, #16588 ),
 ( #18036, #1747, #7541, #3638, #14819, #13023 ),
 ( #21735, #12669, #10873, #7322, #20524, #15394 ),
 ( #9428, #9779, #4336, #22540, #16709, #650 ),
 ( #13369, #5876, #2448, #4449, #17055, #9666 ),
 ( #6348, #17179, #22190, #2209, #22653, #543 ),
 ( #11808, #11333, #9557, #2555, #11684, #6234 ),
 ( #18963, #13248, #13482, #4221, #16941, #13602 ),
 ( #7660, #18618, #778, #7883, #2677, #422 ),
 ( #8004, #6115, #20875, #15286, #11457, #18738 ),
 ( #4097, #8121, #20643, #15161, #22423, #11569 ) ),
 .UNSPECIFIED., .F., .F., .F. ) 
 B_SPLINE_SURFACE_WITH_KNOTS ( ( 6, 3, 3, 6 ),
 ( 6, 6 ),
 ( 0.000000000000000000, 4.066159495680000013, 8.252146144990000209, 12.56898909050000057 ),
 ( 1.570796326630355066, 3.141592653590000062 ),
 .UNSPECIFIED. ) 
 GEOMETRIC_REPRESENTATION_ITEM ( )  RATIONAL_B_SPLINE_SURFACE ( (
 ( 0.2500000000000000000, 0.2499999999790369909, 0.2999999999685555307, 0.3999999999580740040, 0.5999999999580739596, 1.000000000000000000),
 ( 0.2500000000000000000, 0.2499999999790369909, 0.2999999999685555307, 0.3999999999580740040, 0.5999999999580739596, 1.000000000000000000),
 ( 0.2500000000000000000, 0.2499999999790369909, 0.2999999999685555307, 0.3999999999580740040, 0.5999999999580739596, 1.000000000000000000),
 ( 0.2500000000000000000, 0.2499999999790369909, 0.2999999999685555307, 0.3999999999580740040, 0.5999999999580739596, 1.000000000000000000),
 ( 0.2500000000000000000, 0.2499999999790369909, 0.2999999999685555307, 0.3999999999580740040, 0.5999999999580739596, 1.000000000000000000),
 ( 0.2500000000000000000, 0.2499999999790369909, 0.2999999999685555307, 0.3999999999580740040, 0.5999999999580739596, 1.000000000000000000),
 ( 0.2500000000000000000, 0.2499999999790369909, 0.2999999999685555307, 0.3999999999580740040, 0.5999999999580739596, 1.000000000000000000),
 ( 0.2500000000000000000, 0.2499999999790369909, 0.2999999999685555307, 0.3999999999580740040, 0.5999999999580739596, 1.000000000000000000),
 ( 0.2500000000000000000, 0.2499999999790369909, 0.2999999999685555307, 0.3999999999580740040, 0.5999999999580739596, 1.000000000000000000),
 ( 0.2500000000000000000, 0.2499999999790369909, 0.2999999999685555307, 0.3999999999580740040, 0.5999999999580739596, 1.000000000000000000),
 ( 0.2500000000000000000, 0.2499999999790369909, 0.2999999999685555307, 0.3999999999580740040, 0.5999999999580739596, 1.000000000000000000),
 ( 0.2500000000000000000, 0.2499999999790369909, 0.2999999999685555307, 0.3999999999580740040, 0.5999999999580739596, 1.000000000000000000) ) ) 
 REPRESENTATION_ITEM ( '' )  SURFACE ( )  );
#7212=CARTESIAN_POINT ( 'NONE',  ( -11.76172848620000089, 40.95326072219999958, -146.5101368410000191 ) ) ;
#7234=CARTESIAN_POINT ( 'NONE',  ( -15.59320802965877917, 39.76776338515035292, -147.7580614746654817 ) ) ;
#7237=VERTEX_POINT ( 'NONE', #2411 ) ;
#7241=CARTESIAN_POINT ( 'NONE',  ( -26.43221227920010463, 37.92234065499331308, -139.4358666115665812 ) ) ;
#7242=CARTESIAN_POINT ( 'NONE',  ( -10.65913935279999869, 37.04331329920000115, -139.7140392919999954 ) ) ;
#7243=EDGE_LOOP ( 'NONE', ( #22210, #18270, #15191, #21331 ) ) ;
#7249=CARTESIAN_POINT ( 'NONE',  ( -28.75749843875100709, 32.81834225557554419, -141.6071124201210694 ) ) ;
#7254=CARTESIAN_POINT ( 'NONE',  ( -16.64819173719487111, 39.54152330607143995, -140.6182326551606252 ) ) ;
#7261=CARTESIAN_POINT ( 'NONE',  ( -27.77832206610000298, 37.03059619289999915, -147.6270870419999710 ) ) ;
#7268=CARTESIAN_POINT ( 'NONE',  ( -6.498948513254279469, 40.81543344996319433, -146.1568765785165738 ) ) ;
#7287=CARTESIAN_POINT ( 'NONE',  ( -18.66256475003282489, 32.87452234919609850, -143.7440942753966056 ) ) ;
#7291=ADVANCED_FACE ( 'NONE', ( #4300 ), #17835, .F. ) ;
#7297=CARTESIAN_POINT ( 'NONE',  ( -5.659867863649999720, 38.70771930269999928, -140.0293976189999796 ) ) ;
#7306=CARTESIAN_POINT ( 'NONE',  ( -18.18930989820000121, 36.96028804430000037, -147.6841622079999752 ) ) ;
#7309=CARTESIAN_POINT ( 'NONE',  ( -24.99548980002266774, 37.05651868163121065, -148.5304149360441386 ) ) ;
#7317=UNCERTAINTY_MEASURE_WITH_UNIT (LENGTH_MEASURE( 1.000000000000000082E-05 ), #15284, 'distance_accuracy_value', 'NONE');
#7322=CARTESIAN_POINT ( 'NONE',  ( -13.24550845540447597, 34.38214360666451341, -147.9047044067351635 ) ) ;
#7328=CARTESIAN_POINT ( 'NONE',  ( -18.75480078877485823, 35.03674905134475637, -146.9103430178364533 ) ) ;
#7335=ADVANCED_FACE ( 'NONE', ( #5355 ), #23325, .F. ) ;
#7339=( BOUNDED_SURFACE ( )  B_SPLINE_SURFACE ( 5, 5, ( 
 ( #17793, #8611, #10636, #6846, #14110, #1514 ),
 ( #12668, #8736, #16010, #23275, #8855, #23388 ),
 ( #7085, #14340, #12545, #8969, #19936, #3637 ),
 ( #13569, #20842, #17150, #15131, #18275, #11778 ),
 ( #13343, #12783, #19056, #20054, #17027, #20494 ),
 ( #16913, #9992, #3752, #22514, #870, #15368 ),
 ( #979, #4311, #746, #22625, #6316, #625 ),
 ( #7747, #185, #2767, #17270, #5533, #14583 ),
 ( #15013, #21851, #10996, #22274, #5966, #13219 ),
 ( #16478, #11541, #1985, #20616, #9208, #4194 ),
 ( #4537, #8096, #22393, #11431, #18714, #2422 ),
 ( #7858, #6091, #9639, #18817, #7977, #2529 ) ),
 .UNSPECIFIED., .F., .F., .F. ) 
 B_SPLINE_SURFACE_WITH_KNOTS ( ( 6, 3, 3, 6 ),
 ( 6, 6 ),
 ( 0.000000000000000000, 4.358589029760000066, 8.533830367689999363, 12.54112731390000057 ),
 ( 1.570796326654110064, 3.141592653590000062 ),
 .UNSPECIFIED. ) 
 GEOMETRIC_REPRESENTATION_ITEM ( )  RATIONAL_B_SPLINE_SURFACE ( (
 ( 0.2500000000000000000, 0.2499999999820609886, 0.2999999999730915134, 0.3999999999641219994, 0.5999999999641220105, 1.000000000000000000),
 ( 0.2500000000000000000, 0.2499999999820609886, 0.2999999999730915134, 0.3999999999641219994, 0.5999999999641220105, 1.000000000000000000),
 ( 0.2500000000000000000, 0.2499999999820609886, 0.2999999999730915134, 0.3999999999641219994, 0.5999999999641220105, 1.000000000000000000),
 ( 0.2500000000000000000, 0.2499999999820609886, 0.2999999999730915134, 0.3999999999641219994, 0.5999999999641220105, 1.000000000000000000),
 ( 0.2500000000000000000, 0.2499999999820609886, 0.2999999999730915134, 0.3999999999641219994, 0.5999999999641220105, 1.000000000000000000),
 ( 0.2500000000000000000, 0.2499999999820609886, 0.2999999999730915134, 0.3999999999641219994, 0.5999999999641220105, 1.000000000000000000),
 ( 0.2500000000000000000, 0.2499999999820609886, 0.2999999999730915134, 0.3999999999641219994, 0.5999999999641220105, 1.000000000000000000),
 ( 0.2500000000000000000, 0.2499999999820609886, 0.2999999999730915134, 0.3999999999641219994, 0.5999999999641220105, 1.000000000000000000),
 ( 0.2500000000000000000, 0.2499999999820609886, 0.2999999999730915134, 0.3999999999641219994, 0.5999999999641220105, 1.000000000000000000),
 ( 0.2500000000000000000, 0.2499999999820609886, 0.2999999999730915134, 0.3999999999641219994, 0.5999999999641220105, 1.000000000000000000),
 ( 0.2500000000000000000, 0.2499999999820609886, 0.2999999999730915134, 0.3999999999641219994, 0.5999999999641220105, 1.000000000000000000),
 ( 0.2500000000000000000, 0.2499999999820609886, 0.2999999999730915134, 0.3999999999641219994, 0.5999999999641220105, 1.000000000000000000) ) ) 
 REPRESENTATION_ITEM ( '' )  SURFACE ( )  );
#7346=CARTESIAN_POINT ( 'NONE',  ( -27.13199227600000185, 40.71900643419999710, -144.3906906950000177 ) ) ;
#7348=CARTESIAN_POINT ( 'NONE',  ( -21.15827341640166992, 35.11213290585252622, -148.0734965375279160 ) ) ;
#7362=CARTESIAN_POINT ( 'NONE',  ( -13.04270098970000014, 34.92521805810000046, -147.0831430689999877 ) ) ;
#7371=CARTESIAN_POINT ( 'NONE',  ( -22.72559961389999827, 32.84666773589999877, -144.4841142160000231 ) ) ;
#7383=CARTESIAN_POINT ( 'NONE',  ( -5.810489697651222585, 41.13568347802100078, -141.5859922120193914 ) ) ;
#7398=CARTESIAN_POINT ( 'NONE',  ( -10.15741051819999896, 33.19655140199999721, -141.5761258080000005 ) ) ;
#7399=CARTESIAN_POINT ( 'NONE',  ( -18.28451977777580240, 36.23520409085267602, -147.6763998119407972 ) ) ;
#7402=CARTESIAN_POINT ( 'NONE',  ( -22.73109880832327789, 38.77532135884324305, -140.2559096066406141 ) ) ;
#7408=CARTESIAN_POINT ( 'NONE',  ( -5.992616235259950130, 37.70616357870241586, -147.6478618792677366 ) ) ;
#7432=ORIENTED_EDGE ( 'NONE', *, *, #307, .T. ) ;
#7434=CARTESIAN_POINT ( 'NONE',  ( -20.34334609172888264, 35.37018562970122559, -140.7073119323060268 ) ) ;
#7450=CARTESIAN_POINT ( 'NONE',  ( -26.63329978995851022, 40.09797676221232621, -142.2284921075155921 ) ) ;
#7452=CARTESIAN_POINT ( 'NONE',  ( -22.52780672250980132, 37.05898997718779952, -140.0074087194032018 ) ) ;
#7460=CARTESIAN_POINT ( 'NONE',  ( -8.208807763370000288, 34.49436158469999469, -140.8229124829999819 ) ) ;
#7463=CARTESIAN_POINT ( 'NONE',  ( -6.565507373411123559, 37.00519331013514801, -148.7410818962522114 ) ) ;
#7474=CARTESIAN_POINT ( 'NONE',  ( -17.02285281771896308, 37.95643371699240731, -139.4648240190154524 ) ) ;
#7475=CARTESIAN_POINT ( 'NONE',  ( -29.00775545215896400, 40.69683423424014990, -142.7914494781169026 ) ) ;
#7484=CARTESIAN_POINT ( 'NONE',  ( -20.49362533948273679, 38.90000993910273763, -139.7618038651926327 ) ) ;
#7504=CARTESIAN_POINT ( 'NONE',  ( -21.33871772390000032, 34.54066873269999860, -147.2646375960000000 ) ) ;
#7508=CARTESIAN_POINT ( 'NONE',  ( -18.08440866526200352, 35.37133319620465954, -147.7332747159482551 ) ) ;
#7511=CARTESIAN_POINT ( 'NONE',  ( -22.62924774399843741, 37.91877106612172099, -140.0196664482663778 ) ) ;
#7526=CARTESIAN_POINT ( 'NONE',  ( -24.22314457578830016, 36.96432676147898633, -148.6204621725165964 ) ) ;
#7527=CARTESIAN_POINT ( 'NONE',  ( -13.10382330435357190, 34.73913613269233736, -140.9738839404401460 ) ) ;
#7541=CARTESIAN_POINT ( 'NONE',  ( -13.37538095157338880, 35.38499319558606970, -148.0468720929505082 ) ) ;
#7551=CARTESIAN_POINT ( 'NONE',  ( -19.69393976287956249, 37.84845892294580239, -140.3168504267079868 ) ) ;
#7561=EDGE_LOOP ( 'NONE', ( #16203, #4861, #17002, #4205 ) ) ;
#7564=CARTESIAN_POINT ( 'NONE',  ( -26.19677859571902445, 41.24837624377309453, -144.5491401104135605 ) ) ;
#7566=EDGE_CURVE ( 'NONE', #12438, #13908, #18414, .T. ) ;
#7567=CARTESIAN_POINT ( 'NONE',  ( -22.01591886049312308, 32.20669244871583459, -144.4616323330807290 ) ) ;
#7589=CARTESIAN_POINT ( 'NONE',  ( -11.58731752069515863, 38.53682247841263830, -140.5940415739001708 ) ) ;
#7590=CARTESIAN_POINT ( 'NONE',  ( -16.91592704284670035, 37.75347730502732446, -140.5160138913198011 ) ) ;
#7591=CARTESIAN_POINT ( 'NONE',  ( -29.62481956335792788, 40.87340935592879276, -146.3463541502384544 ) ) ;
#7601=CARTESIAN_POINT ( 'NONE',  ( -20.11972240904378495, 41.31329007930804664, -143.7317463393834203 ) ) ;
#7619=CARTESIAN_POINT ( 'NONE',  ( -30.64259443220337786, 40.28463426600038133, -145.8661425198802988 ) ) ;
#7624=CARTESIAN_POINT ( 'NONE',  ( -18.17807444413858775, 34.66091580349097256, -147.3401956634381236 ) ) ;
#7629=CARTESIAN_POINT ( 'NONE',  ( -23.03778781513472040, 40.78628791076015858, -141.9896475656336179 ) ) ;
#7631=CARTESIAN_POINT ( 'NONE',  ( -15.73345061033185210, 33.26188818293405802, -144.2173886784002548 ) ) ;
#7636=CARTESIAN_POINT ( 'NONE',  ( -5.832642628619999492, 38.59814668869999821, -147.7665506369999662 ) ) ;
#7642=CARTESIAN_POINT ( 'NONE',  ( -22.36052286279805301, 33.87069800589680568, -145.8484948931464089 ) ) ;
#7647=CARTESIAN_POINT ( 'NONE',  ( -12.49728671969152494, 33.10632428298641372, -146.3897782398302923 ) ) ;
#7660=CARTESIAN_POINT ( 'NONE',  ( -13.91784526120884102, 35.46792342019083577, -140.7554205114054184 ) ) ;
#7670=CARTESIAN_POINT ( 'NONE',  ( -21.22372860086487023, 38.99008670914216879, -146.8399696847710914 ) ) ;
#7674=CARTESIAN_POINT ( 'NONE',  ( -18.22769797923111668, 36.96487028399717900, -148.6596776398728537 ) ) ;
#7676=CARTESIAN_POINT ( 'NONE',  ( -27.77832206610000298, 37.03059619289999915, -147.6270870419999710 ) ) ;
#7682=CARTESIAN_POINT ( 'NONE',  ( -26.79508209637365468, 40.49614020271001635, -143.6492312593390750 ) ) ;
#7684=CARTESIAN_POINT ( 'NONE',  ( -23.32853373970316468, 36.96341023006359450, -139.4571126576117024 ) ) ;
#7685=ORIENTED_EDGE ( 'NONE', *, *, #6601, .T. ) ;
#7686=CARTESIAN_POINT ( 'NONE',  ( -29.88845675159999971, 40.47687533140000227, -144.8298193859999969 ) ) ;
#7696=CARTESIAN_POINT ( 'NONE',  ( -8.475885007274353455, 38.89800807253860881, -139.6558146860800207 ) ) ;
#7699=ADVANCED_FACE ( 'NONE', ( #6111 ), #21811, .F. ) ;
#7706=CARTESIAN_POINT ( 'NONE',  ( -11.86981902993892035, 40.35288497610176250, -142.1893091613364106 ) ) ;
#7712=CARTESIAN_POINT ( 'NONE',  ( -30.68396739435302223, 40.64794745105156437, -146.0701989576815549 ) ) ;
#7718=CARTESIAN_POINT ( 'NONE',  ( -20.24766572715067525, 39.88812938375418327, -140.1838214082657146 ) ) ;
#7721=FACE_OUTER_BOUND ( 'NONE', #3192, .T. ) ;
#7734=CARTESIAN_POINT ( 'NONE',  ( -22.29630802378710541, 35.55620207364702168, -140.5780526047887520 ) ) ;
#7745=CARTESIAN_POINT ( 'NONE',  ( -15.68268784160000173, 36.02211616019999951, -148.5535485649999998 ) ) ;
#7747=CARTESIAN_POINT ( 'NONE',  ( -16.36784392959527779, 33.86562477376711655, -142.0582287346993837 ) ) ;
#7753=CARTESIAN_POINT ( 'NONE',  ( -6.518342001254413987, 39.10550174654262179, -146.8501022327429268 ) ) ;
#7757=CARTESIAN_POINT ( 'NONE',  ( -22.93117458072607207, 34.96482181345525930, -141.2446360092426971 ) ) ;
#7761=CARTESIAN_POINT ( 'NONE',  ( -12.95309207269206020, 35.58606224184668321, -147.4460499725167892 ) ) ;
#7767=CARTESIAN_POINT ( 'NONE',  ( -13.73025257492642126, 37.03482478361185315, -140.6242165752722997 ) ) ;
#7771=CARTESIAN_POINT ( 'NONE',  ( -27.80359210608580156, 32.89696731219263626, -146.3345487532673701 ) ) ;
#7783=CARTESIAN_POINT ( 'NONE',  ( -20.82480350055617535, 40.41812776023138554, -143.7337601291241356 ) ) ;
#7795=CARTESIAN_POINT ( 'NONE',  ( -25.65708489768155331, 38.56472069215177356, -140.6657235122787881 ) ) ;
#7797=CARTESIAN_POINT ( 'NONE',  ( -23.24537173081721164, 34.37218318494526414, -140.4769510064934082 ) ) ;
#7808=( BOUNDED_SURFACE ( )  B_SPLINE_SURFACE ( 5, 5, ( 
 ( #22641, #6572, #20987, #8109, #13836, #17166 ),
 ( #20740, #8574, #6222, #4677, #8226, #21100 ),
 ( #15382, #885, #4434, #15495, #10008, #19427 ),
 ( #4792, #11671, #8350, #12035, #19184, #15622 ),
 ( #18948, #6684, #19304, #3017, #10254, #22756 ),
 ( #17519, #9889, #1244, #6332, #8467, #2663 ),
 ( #13586, #20861, #6457, #15735, #22995, #13713 ),
 ( #13945, #21217, #4909, #12157, #21571, #23461 ),
 ( #3599, #14071, #12629, #3477, #7037, #18231 ),
 ( #1820, #21338, #12742, #1946, #3239, #20013 ),
 ( #10715, #12503, #21451, #9164, #17996, #1706 ),
 ( #10945, #5379, #17878, #3708, #5132, #12383 ) ),
 .UNSPECIFIED., .F., .F., .F. ) 
 B_SPLINE_SURFACE_WITH_KNOTS ( ( 6, 3, 3, 6 ),
 ( 6, 6 ),
 ( 0.000000000000000000, 4.509114667229999540, 8.972055907920001516, 13.39149027790000090 ),
 ( 1.570796326489795058, 3.141592653590000062 ),
 .UNSPECIFIED. ) 
 GEOMETRIC_REPRESENTATION_ITEM ( )  RATIONAL_B_SPLINE_SURFACE ( (
 ( 0.2500000000000000000, 0.2499999999611400014, 0.2999999999417100049, 0.3999999999222799696, 0.5999999999222800362, 1.000000000000000000),
 ( 0.2500000000000000000, 0.2499999999611400014, 0.2999999999417100049, 0.3999999999222799696, 0.5999999999222800362, 1.000000000000000000),
 ( 0.2500000000000000000, 0.2499999999611400014, 0.2999999999417100049, 0.3999999999222799696, 0.5999999999222800362, 1.000000000000000000),
 ( 0.2500000000000000000, 0.2499999999611400014, 0.2999999999417100049, 0.3999999999222799696, 0.5999999999222800362, 1.000000000000000000),
 ( 0.2500000000000000000, 0.2499999999611400014, 0.2999999999417100049, 0.3999999999222799696, 0.5999999999222800362, 1.000000000000000000),
 ( 0.2500000000000000000, 0.2499999999611400014, 0.2999999999417100049, 0.3999999999222799696, 0.5999999999222800362, 1.000000000000000000),
 ( 0.2500000000000000000, 0.2499999999611400014, 0.2999999999417100049, 0.3999999999222799696, 0.5999999999222800362, 1.000000000000000000),
 ( 0.2500000000000000000, 0.2499999999611400014, 0.2999999999417100049, 0.3999999999222799696, 0.5999999999222800362, 1.000000000000000000),
 ( 0.2500000000000000000, 0.2499999999611400014, 0.2999999999417100049, 0.3999999999222799696, 0.5999999999222800362, 1.000000000000000000),
 ( 0.2500000000000000000, 0.2499999999611400014, 0.2999999999417100049, 0.3999999999222799696, 0.5999999999222800362, 1.000000000000000000),
 ( 0.2500000000000000000, 0.2499999999611400014, 0.2999999999417100049, 0.3999999999222799696, 0.5999999999222800362, 1.000000000000000000),
 ( 0.2500000000000000000, 0.2499999999611400014, 0.2999999999417100049, 0.3999999999222799696, 0.5999999999222800362, 1.000000000000000000) ) ) 
 REPRESENTATION_ITEM ( '' )  SURFACE ( )  );
#7818=CARTESIAN_POINT ( 'NONE',  ( -12.63906142178066538, 39.72050110283642255, -147.8595189120993894 ) ) ;
#7819=CARTESIAN_POINT ( 'NONE',  ( -17.67542686956860720, 41.20418847383326266, -146.4439386566194514 ) ) ;
#7822=CARTESIAN_POINT ( 'NONE',  ( -7.856058713298979868, 37.01980778203124345, -139.4032252964223630 ) ) ;
#7826=CARTESIAN_POINT ( 'NONE',  ( -28.67645553090000021, 33.79622934780000065, -142.1760638819999940 ) ) ;
#7827=VERTEX_POINT ( 'NONE', #20023 ) ;
#7829=CARTESIAN_POINT ( 'NONE',  ( -21.41042584029257512, 41.06450079727203217, -146.4204638434819969 ) ) ;
#7854=CARTESIAN_POINT ( 'NONE',  ( -24.63187620858801807, 37.01311550629854707, -148.7335123083401243 ) ) ;
#7858=CARTESIAN_POINT ( 'NONE',  ( -16.81794493326261986, 37.02435727938188137, -140.5111119823011734 ) ) ;
#7861=CARTESIAN_POINT ( 'NONE',  ( -5.459597139290000456, 36.94776568910000236, -139.8191173760000083 ) ) ;
#7865=CARTESIAN_POINT ( 'NONE',  ( -5.064279449469999861, 40.47653686799999662, -142.0698957560000224 ) ) ;
#7868=CARTESIAN_POINT ( 'NONE',  ( -21.03694116380903978, 36.94210036639064043, -147.9486865822370021 ) ) ;
#7871=CARTESIAN_POINT ( 'NONE',  ( -12.47876718462605616, 33.77260538731622574, -145.9764135834861065 ) ) ;
#7883=CARTESIAN_POINT ( 'NONE',  ( -14.37102166023024807, 35.04507042385125004, -139.9665150629348318 ) ) ;
#7891=CARTESIAN_POINT ( 'NONE',  ( -20.55139866881591715, 40.46905695072928211, -146.1780460798107981 ) ) ;
#7895=CARTESIAN_POINT ( 'NONE',  ( -23.20965953747225541, 36.97759979273073583, -140.7013664825230421 ) ) ;
#7910=CARTESIAN_POINT ( 'NONE',  ( -23.12623614695305108, 35.07139013615802270, -139.7131972622368323 ) ) ;
#7916=CARTESIAN_POINT ( 'NONE',  ( -27.87685576917573371, 39.58963625183361046, -147.4493226070128742 ) ) ;
#7920=CARTESIAN_POINT ( 'NONE',  ( -7.104147058966693962, 32.78722980359287220, -146.6177089082302416 ) ) ;
#7922=CARTESIAN_POINT ( 'NONE',  ( -8.871724173964516069, 39.55783021574837477, -140.3984215277044711 ) ) ;
#7928=CARTESIAN_POINT ( 'NONE',  ( -24.63187620858803228, 37.01311550629856839, -148.7335123083400106 ) ) ;
#7931=CARTESIAN_POINT ( 'NONE',  ( -13.11071995283477953, 37.07027326795081734, -147.8134892432882452 ) ) ;
#7933=CARTESIAN_POINT ( 'NONE',  ( -18.64767072899999789, 38.89869937459999960, -148.1651290810000319 ) ) ;
#7946=CARTESIAN_POINT ( 'NONE',  ( -19.89002371296891880, 39.36161564549420433, -140.9617346337927870 ) ) ;
#7965=CARTESIAN_POINT ( 'NONE',  ( -29.88845675159999971, 40.47687533140000227, -144.8298193859999969 ) ) ;
#7975=CARTESIAN_POINT ( 'NONE',  ( -8.931798216517609745, 36.92954985152155700, -147.9669232059208070 ) ) ;
#7976=CARTESIAN_POINT ( 'NONE',  ( -23.34997301937064051, 41.23575095005864455, -144.6233831888736177 ) ) ;
#7977=CARTESIAN_POINT ( 'NONE',  ( -17.52779041586176945, 36.93962571632794578, -139.7364823516872434 ) ) ;
#7984=CARTESIAN_POINT ( 'NONE',  ( -9.651143958800396661, 32.86909415028417669, -144.2000375143311715 ) ) ;
#7988=CARTESIAN_POINT ( 'NONE',  ( -22.60316433423102822, 33.52336180732346804, -143.6562582910067363 ) ) ;
#7991=CARTESIAN_POINT ( 'NONE',  ( -12.73635673082345576, 33.27079122909506026, -143.7284791742528114 ) ) ;
#7993=CARTESIAN_POINT ( 'NONE',  ( -16.55827375309849714, 37.05535324330074332, -139.5705083843459136 ) ) ;
#7994=CARTESIAN_POINT ( 'NONE',  ( -15.46613156839999981, 36.99333119719999985, -147.5584717940000132 ) ) ;
#8000=CARTESIAN_POINT ( 'NONE',  ( -8.292543378966758638, 38.36969968732901037, -140.9136116612680780 ) ) ;
#8004=CARTESIAN_POINT ( 'NONE',  ( -14.01657753848344079, 36.22806874879579908, -140.5479840251611847 ) ) ;
#8005=CARTESIAN_POINT ( 'NONE',  ( -29.04405754849999965, 38.20917013909999582, -139.5702141479999909 ) ) ;
#8013=CARTESIAN_POINT ( 'NONE',  ( -19.89002371286244042, 39.36161564562564052, -140.9617346336366097 ) ) ;
#8014=CARTESIAN_POINT ( 'NONE',  ( -17.98964812789086309, 38.50830570032488254, -147.4920370692890117 ) ) ;
#8017=CARTESIAN_POINT ( 'NONE',  ( -26.07820652087960056, 36.26055466349079381, -140.6390304775231925 ) ) ;
#8042=CARTESIAN_POINT ( 'NONE',  ( -9.410006930593050711, 41.20806710879531920, -146.3969463093499712 ) ) ;
#8046=EDGE_CURVE ( 'NONE', #6561, #20464, #5660, .T. ) ;
#8059=CARTESIAN_POINT ( 'NONE',  ( -14.02405267930000043, 37.94700976039999318, -139.5674429869999926 ) ) ;
#8061=CARTESIAN_POINT ( 'NONE',  ( -26.41321238348850642, 35.27984194833333476, -140.3745674731081579 ) ) ;
#8072=EDGE_LOOP ( 'NONE', ( #17132, #3589, #3919, #11838 ) ) ;
#8086=CARTESIAN_POINT ( 'NONE',  ( -30.34130859797645030, 41.26057227206133149, -145.6696127677633967 ) ) ;
#8096=CARTESIAN_POINT ( 'NONE',  ( -17.08496771056256947, 36.30549575163614406, -140.6791867003299785 ) ) ;
#8101=CARTESIAN_POINT ( 'NONE',  ( -10.27640102954716816, 33.81552902124293780, -145.7376306576129537 ) ) ;
#8109=CARTESIAN_POINT ( 'NONE',  ( -23.20965953746479116, 36.97759979273159558, -140.7013664825302612 ) ) ;
#8115=CARTESIAN_POINT ( 'NONE',  ( -7.529689113779999943, 37.05876528330000497, -139.9906690790000141 ) ) ;
#8121=CARTESIAN_POINT ( 'NONE',  ( -14.50908993377715639, 36.94185792197168894, -140.4668331871908435 ) ) ;
#8132=CARTESIAN_POINT ( 'NONE',  ( -18.38287346733138250, 37.71117569361661737, -147.4170582157152580 ) ) ;
#8135=CARTESIAN_POINT ( 'NONE',  ( -24.36912841293447940, 34.40976477756748153, -147.5507798125887859 ) ) ;
#8151=CARTESIAN_POINT ( 'NONE',  ( -11.57675713931716821, 40.11775891596531807, -142.3540931478985669 ) ) ;
#8153=CARTESIAN_POINT ( 'NONE',  ( -12.28014746100000032, 36.97113097969999984, -148.4919582129999753 ) ) ;
#8154=CARTESIAN_POINT ( 'NONE',  ( -8.060221343263076932, 34.98053230926937118, -139.6932736515213662 ) ) ;
#8155=CARTESIAN_POINT ( 'NONE',  ( -9.213999483924272482, 36.96323514650488562, -148.5699756000874459 ) ) ;
#8163=CARTESIAN_POINT ( 'NONE',  ( -17.69217738326715761, 38.58884013740755137, -147.7569206260365036 ) ) ;
#8174=CARTESIAN_POINT ( 'NONE',  ( -26.61369313923914603, 36.92937183404335855, -140.1328975134355517 ) ) ;
#8190=B_SPLINE_CURVE_WITH_KNOTS ( 'NONE', 5,
 ( #13183, #20456, #14868, #11388, #586, #5697, #11047, #16990, #13071, #15091, #18433, #22353 ),
 .UNSPECIFIED., .F., .F.,
 ( 6, 3, 3, 6 ),
 ( 0.000000000000000000, 4.346865784160000246, 8.778337911509998648, 13.29702284770000098 ),
 .UNSPECIFIED. ) ;
#8213=CARTESIAN_POINT ( 'NONE',  ( -5.096343650251323076, 36.99112588044069838, -140.7242647647827312 ) ) ;
#8217=CARTESIAN_POINT ( 'NONE',  ( -10.28060652869188196, 34.62853500593604394, -147.1732277809310006 ) ) ;
#8226=CARTESIAN_POINT ( 'NONE',  ( -23.58570254345633543, 37.71378429759510453, -140.4235127406076913 ) ) ;
#8230=CARTESIAN_POINT ( 'NONE',  ( -10.67196964177461638, 33.18472025305887030, -146.1142301646851251 ) ) ;
#8231=CARTESIAN_POINT ( 'NONE',  ( -9.213999483924276035, 36.96323514650488562, -148.5699756000874743 ) ) ;
#8233=CARTESIAN_POINT ( 'NONE',  ( -7.794473646117169530, 37.74767836363313478, -140.6506544358082920 ) ) ;
#8239=CARTESIAN_POINT ( 'NONE',  ( -6.833331567582606958, 33.96895959207153481, -145.8669957953534038 ) ) ;
#8240=CARTESIAN_POINT ( 'NONE',  ( -20.97542662470000252, 40.85881720449999932, -141.8340754020000247 ) ) ;
#8247=CARTESIAN_POINT ( 'NONE',  ( -18.08788331821740414, 37.73304001162604493, -147.6923967947956271 ) ) ;
#8253=CARTESIAN_POINT ( 'NONE',  ( -25.04112998497079445, 35.58084596877723982, -147.3751007919723577 ) ) ;
#8267=EDGE_LOOP ( 'NONE', ( #16115, #17294, #14040, #9147 ) ) ;
#8272=CARTESIAN_POINT ( 'NONE',  ( -10.41700570847820551, 37.07221587398769458, -140.3414633426675380 ) ) ;
#8274=CARTESIAN_POINT ( 'NONE',  ( -7.806459626923599515, 32.86659014932959622, -143.7778124396562021 ) ) ;
#8275=CARTESIAN_POINT ( 'NONE',  ( -8.764208581537477727, 41.80648535992416015, -144.5325683263670271 ) ) ;
#8295=CARTESIAN_POINT ( 'NONE',  ( -25.70171731128227677, 35.06206091446468776, -139.6775904388746312 ) ) ;
#8325=CARTESIAN_POINT ( 'NONE',  ( -11.65594158655517454, 36.92432879710629123, -140.1042033531252571 ) ) ;
#8329=CARTESIAN_POINT ( 'NONE',  ( -15.82083308688285506, 33.29371180489421533, -143.4209982738438214 ) ) ;
#8350=CARTESIAN_POINT ( 'NONE',  ( -23.08033233722681032, 39.09424655247641311, -141.2811153005157507 ) ) ;
#8366=CARTESIAN_POINT ( 'NONE',  ( -7.643000129979401258, 33.91462222170895302, -142.3752337145176625 ) ) ;
#8376=CARTESIAN_POINT ( 'NONE',  ( -17.45880800003273592, 39.00787884620090296, -141.2058029617074624 ) ) ;
#8385=CARTESIAN_POINT ( 'NONE',  ( -25.33725402877131927, 34.39035690824012192, -140.4300890441823810 ) ) ;
#8388=CARTESIAN_POINT ( 'NONE',  ( -12.04808041649379824, 40.71874701590343903, -143.7411651110283799 ) ) ;
#8396=CARTESIAN_POINT ( 'NONE',  ( -28.42251996826504623, 36.15178013674928792, -139.6484962583844833 ) ) ;
#8400=CARTESIAN_POINT ( 'NONE',  ( -18.85469010170000459, 37.03971195569999963, -148.4264296979999926 ) ) ;
#8403=CARTESIAN_POINT ( 'NONE',  ( -8.309953467205138722, 35.25464643893679551, -140.3668538354673956 ) ) ;
#8405=CARTESIAN_POINT ( 'NONE',  ( -9.834107546974056646, 39.61220777223162770, -147.4819523409258295 ) ) ;
#8419=EDGE_LOOP ( 'NONE', ( #22245, #71, #12327, #13243 ) ) ;
#8423=CARTESIAN_POINT ( 'NONE',  ( -15.00096184705712510, 39.32882771142540435, -140.7014506208544731 ) ) ;
#8424=CARTESIAN_POINT ( 'NONE',  ( -24.53581133586112273, 34.20578514941706771, -147.8660713000161877 ) ) ;
#8433=EDGE_CURVE ( 'NONE', #4660, #11114, #20848, .T. ) ;
#8441=CARTESIAN_POINT ( 'NONE',  ( -15.37212823710000009, 38.89807584180000077, -148.3010324070000081 ) ) ;
#8452=CARTESIAN_POINT ( 'NONE',  ( -17.03115501030000090, 35.19590004879999867, -139.8299307730000010 ) ) ;
#8455=CARTESIAN_POINT ( 'NONE',  ( -4.855180678435623953, 37.01991258974685906, -139.3889649350432194 ) ) ;
#8464=CARTESIAN_POINT ( 'NONE',  ( -28.40010805446878095, 32.24922851640265975, -144.5145871741030135 ) ) ;
#8467=CARTESIAN_POINT ( 'NONE',  ( -24.13442235245820555, 40.66074140249224200, -143.6722919103460185 ) ) ;
#8473=CARTESIAN_POINT ( 'NONE',  ( -9.213999483942407309, 36.96323514650706699, -148.5699756001263552 ) ) ;
#8475=CARTESIAN_POINT ( 'NONE',  ( -7.486908230310626244, 37.06387187510053849, -140.3212062627006560 ) ) ;
#8479=( LENGTH_UNIT ( ) NAMED_UNIT ( * ) SI_UNIT ( .MILLI., .METRE. ) );
#8482=CARTESIAN_POINT ( 'NONE',  ( -8.411849887981940554, 36.09637009078448244, -140.1322081661286063 ) ) ;
#8490=CARTESIAN_POINT ( 'NONE',  ( -22.00705883600000234, 37.05789963359999462, -148.1619053240000028 ) ) ;
#8491=CARTESIAN_POINT ( 'NONE',  ( -18.09080689940000397, 41.54765954780000214, -144.4256796519999853 ) ) ;
#8494=CARTESIAN_POINT ( 'NONE',  ( -6.389646268321175882, 36.98420143700544571, -147.3954793911336765 ) ) ;
#8504=EDGE_CURVE ( 'NONE', #12619, #10397, #3109, .T. ) ;
#8507=CARTESIAN_POINT ( 'NONE',  ( -28.50747929780000334, 33.37084171139999711, -143.6371486329999811 ) ) ;
#8513=EDGE_CURVE ( 'NONE', #8868, #19550, #23287, .T. ) ;
#8514=CARTESIAN_POINT ( 'NONE',  ( -19.59255166829999695, 37.05126161860000167, -140.3061871179999969 ) ) ;
#8519=CARTESIAN_POINT ( 'NONE',  ( -7.695630400395970128, 37.03895750127041708, -140.6427397355593030 ) ) ;
#8532=CARTESIAN_POINT ( 'NONE',  ( -25.54181139845054460, 32.21533750178601707, -143.6018648084610447 ) ) ;
#8541=CARTESIAN_POINT ( 'NONE',  ( -25.33725402870000210, 34.39035690829999936, -140.4300890439999705 ) ) ;
#8546=CARTESIAN_POINT ( 'NONE',  ( -15.57786843150000067, 37.00666880280000726, -148.5521201120000114 ) ) ;
#8559=CARTESIAN_POINT ( 'NONE',  ( -16.40179927705826302, 32.92604696800222541, -141.4709451251691235 ) ) ;
#8568=( BOUNDED_CURVE ( )  B_SPLINE_CURVE ( 5, ( #9883, #2773, #876, #11547, #22399, #85 ),
 .UNSPECIFIED., .F., .F. ) 
 B_SPLINE_CURVE_WITH_KNOTS ( ( 6, 6 ),
 ( 1.570796326823717504, 3.141592653590000062 ),
 .UNSPECIFIED. ) 
 CURVE ( )  GEOMETRIC_REPRESENTATION_ITEM ( )  RATIONAL_B_SPLINE_CURVE ( ( 0.2500000000000000000, 0.2500000000036564085, 0.3000000000054846572, 0.4000000000073128392, 0.6000000000073127948, 1.000000000000000000 ) ) 
 REPRESENTATION_ITEM ( '' )  );
#8570=CARTESIAN_POINT ( 'NONE',  ( -28.98364196379448288, 34.21857839837574744, -140.2214642502308095 ) ) ;
#8574=CARTESIAN_POINT ( 'NONE',  ( -22.59099198853654400, 37.83876679235774532, -140.4187711903797151 ) ) ;
#8579=CARTESIAN_POINT ( 'NONE',  ( -5.832642628619999492, 38.59814668869999821, -147.7665506369999662 ) ) ;
#8581=CARTESIAN_POINT ( 'NONE',  ( -8.937029861356405647, 40.04003061621273218, -145.7935507840504386 ) ) ;
#8586=FILL_AREA_STYLE_COLOUR ( '', #12625 ) ;
#8589=CARTESIAN_POINT ( 'NONE',  ( -7.274215502043762882, 35.55331374630061703, -147.5814222184934863 ) ) ;
#8603=CARTESIAN_POINT ( 'NONE',  ( -17.03115501030000090, 35.19590004879999867, -139.8299307730000010 ) ) ;
#8611=CARTESIAN_POINT ( 'NONE',  ( -15.86078924142569058, 37.04043998682460170, -147.5134597623204229 ) ) ;
#8612=CARTESIAN_POINT ( 'NONE',  ( -27.84557903575859328, 33.44846360924746165, -141.8624113474437536 ) ) ;
#8618=CARTESIAN_POINT ( 'NONE',  ( -8.613431449180000143, 37.75849558879999535, -140.1079839310000068 ) ) ;
#8620=CARTESIAN_POINT ( 'NONE',  ( -12.48399912372551945, 39.13586957977820191, -147.0556079067775954 ) ) ;
#8622=CARTESIAN_POINT ( 'NONE',  ( -7.946466173734080485, 34.08464986948869324, -140.2285039449382964 ) ) ;
#8639=CARTESIAN_POINT ( 'NONE',  ( -11.76172848620000089, 40.95326072219999958, -146.5101368410000191 ) ) ;
#8641=CARTESIAN_POINT ( 'NONE',  ( -21.32113804967662318, 35.98137087654780686, -148.6635683972468200 ) ) ;
#8653=CARTESIAN_POINT ( 'NONE',  ( -25.64792992860000354, 37.04465132570000208, -139.7265440090000084 ) ) ;
#8654=EDGE_CURVE ( 'NONE', #20985, #4528, #2165, .T. ) ;
#8659=CARTESIAN_POINT ( 'NONE',  ( -14.93342499249067679, 39.74098246769964504, -147.8506186731679577 ) ) ;
#8667=CARTESIAN_POINT ( 'NONE',  ( -28.90798551740000022, 37.01360947639999921, -139.5686590450000040 ) ) ;
#8675=CARTESIAN_POINT ( 'NONE',  ( -4.510059210066969193, 37.06110843049351899, -139.6225057176259554 ) ) ;
#8676=CARTESIAN_POINT ( 'NONE',  ( -8.411849887969999884, 36.09637009080000070, -140.1322081659999981 ) ) ;
#8678=ORIENTED_EDGE ( 'NONE', *, *, #5958, .T. ) ;
#8686=CARTESIAN_POINT ( 'NONE',  ( -29.42801897262304678, 35.14847534977624832, -139.9943774615429390 ) ) ;
#8704=CARTESIAN_POINT ( 'NONE',  ( -7.179265401243958067, 36.31188407385540273, -147.7652876112470892 ) ) ;
#8705=CARTESIAN_POINT ( 'NONE',  ( -23.55797472129999903, 40.74841938830000743, -146.3388075610000101 ) ) ;
#8707=( BOUNDED_CURVE ( )  B_SPLINE_CURVE ( 5, ( #15083, #16982, #18773, #5494, #466, #13294 ),
 .UNSPECIFIED., .F., .F. ) 
 B_SPLINE_CURVE_WITH_KNOTS ( ( 6, 6 ),
 ( 0.000000000000000000, 1.570796327036584783 ),
 .UNSPECIFIED. ) 
 CURVE ( )  GEOMETRIC_REPRESENTATION_ITEM ( )  RATIONAL_B_SPLINE_CURVE ( ( 1.000000000000000000, 0.5999999999384809657, 0.3999999999384809546, 0.2999999999538607298, 0.2499999999692404939, 0.2500000000000000000 ) ) 
 REPRESENTATION_ITEM ( '' )  );
#8731=CARTESIAN_POINT ( 'NONE',  ( -23.71856152630000025, 38.62313066519999438, -140.3058339320000130 ) ) ;
#8732=PRODUCT_DEFINITION_CONTEXT ( 'detailed design', #18008, 'design' ) ;
#8736=CARTESIAN_POINT ( 'NONE',  ( -15.96502778565563041, 36.28323411072798166, -147.5221219874169947 ) ) ;
#8742=CARTESIAN_POINT ( 'NONE',  ( -19.14968637899999848, 34.49201595030000078, -147.7870032629999741 ) ) ;
#8764=CARTESIAN_POINT ( 'NONE',  ( -21.26465617525127527, 34.29107666494682860, -147.5856200583803854 ) ) ;
#8770=CARTESIAN_POINT ( 'NONE',  ( -26.00874347327740566, 37.97668472797509054, -139.4279068652941191 ) ) ;
#8777=CARTESIAN_POINT ( 'NONE',  ( -16.11775386689999934, 33.36946837800000054, -144.2542744049999897 ) ) ;
#8784=CARTESIAN_POINT ( 'NONE',  ( -13.88298315131738114, 40.45381564898249138, -142.1226073618484520 ) ) ;
#8801=CARTESIAN_POINT ( 'NONE',  ( -12.79720822650000045, 32.99715178900000012, -146.4964997610000239 ) ) ;
#8803=CARTESIAN_POINT ( 'NONE',  ( -6.183234097860560219, 41.28010592184711669, -143.5033826244076067 ) ) ;
#8816=CARTESIAN_POINT ( 'NONE',  ( -29.76126909798818332, 38.07786601250845138, -139.7317159275528411 ) ) ;
#8820=CARTESIAN_POINT ( 'NONE',  ( -10.36675979729999852, 34.52853970540000006, -140.3392284379999921 ) ) ;
#8821=CARTESIAN_POINT ( 'NONE',  ( -18.22769797920763679, 36.96487028399435815, -148.6596776398734789 ) ) ;
#8822=CARTESIAN_POINT ( 'NONE',  ( -8.780084707271649691, 40.41048401779300292, -144.3937799371521180 ) ) ;
#8847=CARTESIAN_POINT ( 'NONE',  ( -12.28014746100000032, 36.97113097969999984, -148.4919582129999753 ) ) ;
#8850=( BOUNDED_CURVE ( )  B_SPLINE_CURVE ( 5, ( #23378, #5413, #19464, #3626, #23027, #6834 ),
 .UNSPECIFIED., .F., .F. ) 
 B_SPLINE_CURVE_WITH_KNOTS ( ( 6, 6 ),
 ( 1.570796326654102959, 3.141592653590000062 ),
 .UNSPECIFIED. ) 
 CURVE ( )  GEOMETRIC_REPRESENTATION_ITEM ( )  RATIONAL_B_SPLINE_CURVE ( ( 0.2500000000000000555, 0.2499999999820604335, 0.2999999999730906253, 0.3999999999641208337, 0.5999999999641207893, 1.000000000000000000 ) ) 
 REPRESENTATION_ITEM ( '' )  );
#8855=CARTESIAN_POINT ( 'NONE',  ( -16.01154825874916909, 36.06958384727375488, -148.5244474381624400 ) ) ;
#8862=CARTESIAN_POINT ( 'NONE',  ( -20.06155744032984956, 33.57530910074709141, -142.3227834883446121 ) ) ;
#8863=CARTESIAN_POINT ( 'NONE',  ( -11.83481770378323716, 38.37786124416315658, -147.4224916050285685 ) ) ;
#8864=PRODUCT_DEFINITION_FORMATION_WITH_SPECIFIED_SOURCE ( 'ANY', '', #21568, .NOT_KNOWN. ) ;
#8868=VERTEX_POINT ( 'NONE', #12656 ) ;
#8870=ADVANCED_FACE ( 'NONE', ( #62 ), #4907, .F. ) ;
#8876=CARTESIAN_POINT ( 'NONE',  ( -18.18930989820000121, 36.96028804430000037, -147.6841622079999752 ) ) ;
#8880=ORIENTED_EDGE ( 'NONE', *, *, #12655, .F. ) ;
#8886=ORIENTED_EDGE ( 'NONE', *, *, #12755, .T. ) ;
#8888=CARTESIAN_POINT ( 'NONE',  ( -27.13199227600000185, 40.71900643419999710, -144.3906906950000177 ) ) ;
#8896=AXIS2_PLACEMENT_3D ( 'NONE', #12144, #983, #1456 ) ;
#8901=CARTESIAN_POINT ( 'NONE',  ( -16.45586251408916922, 37.06757768449429591, -140.3467090679593525 ) ) ;
#8902=CARTESIAN_POINT ( 'NONE',  ( -29.36832786400000117, 38.86294434210000048, -140.8528603229999874 ) ) ;
#8913=CARTESIAN_POINT ( 'NONE',  ( -12.37691123100000112, 36.07411227369999551, -148.4862478850000116 ) ) ;
#8915=CARTESIAN_POINT ( 'NONE',  ( -5.453441311498944621, 40.82075019309078812, -146.2932936048981389 ) ) ;
#8918=CARTESIAN_POINT ( 'NONE',  ( -27.67795712710000089, 37.78351609900000341, -147.6208067679999942 ) ) ;
#8920=CARTESIAN_POINT ( 'NONE',  ( -16.16113997806631630, 37.07629171513328714, -147.8146678480565868 ) ) ;
#8932=SURFACE_STYLE_FILL_AREA ( #18001 ) ;
#8934=CARTESIAN_POINT ( 'NONE',  ( -19.72358824313251802, 32.72293528688742015, -141.8321840916795793 ) ) ;
#8936=CARTESIAN_POINT ( 'NONE',  ( -8.703280531730451131, 40.40219763566103239, -143.6646664510770393 ) ) ;
#8942=EDGE_LOOP ( 'NONE', ( #16208, #18758, #12148, #9972 ) ) ;
#8947=CARTESIAN_POINT ( 'NONE',  ( -4.839510985740364646, 37.75343476009111043, -140.5920901129109950 ) ) ;
#8956=CARTESIAN_POINT ( 'NONE',  ( -13.18072986969132288, 37.07863008620356027, -148.2345011165225799 ) ) ;
#8969=CARTESIAN_POINT ( 'NONE',  ( -16.37748838231915371, 35.24315528562843980, -148.0100301510570375 ) ) ;
#8986=ORIENTED_EDGE ( 'NONE', *, *, #7566, .F. ) ;
#8989=CARTESIAN_POINT ( 'NONE',  ( -20.55139866889999922, 40.46905695040000239, -146.1780460800000014 ) ) ;
#8992=ORIENTED_EDGE ( 'NONE', *, *, #344, .T. ) ;
#8995=CARTESIAN_POINT ( 'NONE',  ( -16.16113997806634472, 37.07629171513331556, -147.8146678480567004 ) ) ;
#9000=VERTEX_POINT ( 'NONE', #1421 ) ;
#9001=CARTESIAN_POINT ( 'NONE',  ( -26.90957831414080914, 39.30870637168261794, -140.7426796967767189 ) ) ;
#9010=EDGE_CURVE ( 'NONE', #20464, #1248, #3879, .T. ) ;
#9014=CARTESIAN_POINT ( 'NONE',  ( -16.75911775155306316, 38.89720175092567445, -139.8262345698500724 ) ) ;
#9028=CARTESIAN_POINT ( 'NONE',  ( -5.620151696350735193, 41.14699329952922824, -146.4569507367338588 ) ) ;
#9031=CARTESIAN_POINT ( 'NONE',  ( -14.11967125440000004, 36.98834135279999913, -140.5455248810000057 ) ) ;
#9039=CARTESIAN_POINT ( 'NONE',  ( -30.43411692010282010, 40.83884358021464323, -144.2352720013742555 ) ) ;
#9044=CARTESIAN_POINT ( 'NONE',  ( -20.18044358593063947, 35.97457350380363295, -139.5227774015246212 ) ) ;
#9045=CARTESIAN_POINT ( 'NONE',  ( -8.343166633029998280, 41.26425690090000131, -144.5268661329999986 ) ) ;
#9092=CARTESIAN_POINT ( 'NONE',  ( -19.68771884990000132, 32.54972883539999629, -143.8405663050000101 ) ) ;
#9094=CARTESIAN_POINT ( 'NONE',  ( -11.73808716551824638, 40.46300762661749673, -143.7953220469430562 ) ) ;
#9095=B_SPLINE_CURVE_WITH_KNOTS ( 'NONE', 5,
 ( #16084, #17868, #23453, #11062, #14540, #16545, #255, #20006, #12620, #9160, #8918, #5490 ),
 .UNSPECIFIED., .F., .F.,
 ( 6, 3, 3, 6 ),
 ( 0.000000000000000000, 4.469553974960000176, 8.969854531369998440, 13.50363095830000049 ),
 .UNSPECIFIED. ) ;
#9114=CARTESIAN_POINT ( 'NONE',  ( -26.49522641139999735, 37.71913029610000478, -140.3749603070000092 ) ) ;
#9116=CARTESIAN_POINT ( 'NONE',  ( -21.42839884788494231, 35.00147824449854994, -148.3972767829965562 ) ) ;
#9124=CARTESIAN_POINT ( 'NONE',  ( -26.69242357735191717, 41.76624275143136344, -143.5162967865278745 ) ) ;
#9126=CARTESIAN_POINT ( 'NONE',  ( -10.69115198329540561, 37.03949207291183399, -140.6562969416297051 ) ) ;
#9138=CARTESIAN_POINT ( 'NONE',  ( -17.69601676904985155, 41.72057493329485567, -143.4664273654990154 ) ) ;
#9147=ORIENTED_EDGE ( 'NONE', *, *, #16935, .F. ) ;
#9153=CARTESIAN_POINT ( 'NONE',  ( -5.400017929616782730, 41.25700937233216337, -141.5676830613712127 ) ) ;
#9160=CARTESIAN_POINT ( 'NONE',  ( -27.58120011020000106, 38.53525547130000461, -147.4183263870000076 ) ) ;
#9164=CARTESIAN_POINT ( 'NONE',  ( -24.40630853028789460, 37.68507504038083766, -147.3828018826562243 ) ) ;
#9165=CARTESIAN_POINT ( 'NONE',  ( -29.80549139627661148, 39.66955698335042513, -141.4168970351647943 ) ) ;
#9172=CARTESIAN_POINT ( 'NONE',  ( -19.92532084487941191, 37.01154022405600585, -139.3892291660192200 ) ) ;
#9184=CARTESIAN_POINT ( 'NONE',  ( -6.104854084327544506, 39.03903319827616514, -146.8405481461189197 ) ) ;
#9198=( BOUNDED_CURVE ( )  B_SPLINE_CURVE ( 5, ( #22415, #22535, #4441, #9895, #8231, #15280 ),
 .UNSPECIFIED., .F., .F. ) 
 B_SPLINE_CURVE_WITH_KNOTS ( ( 6, 6 ),
 ( 1.570796326521524344, 3.141592653590000062 ),
 .UNSPECIFIED. ) 
 CURVE ( )  GEOMETRIC_REPRESENTATION_ITEM ( )  RATIONAL_B_SPLINE_CURVE ( ( 0.2500000000000000000, 0.2499999999651800198, 0.2999999999477699908, 0.3999999999303600062, 0.5999999999303600173, 1.000000000000000000 ) ) 
 REPRESENTATION_ITEM ( '' )  );
#9208=CARTESIAN_POINT ( 'NONE',  ( -17.33409723696195215, 35.21621536416972731, -139.9717982390213251 ) ) ;
#9213=ORIENTED_EDGE ( 'NONE', *, *, #19279, .F. ) ;
#9215=CARTESIAN_POINT ( 'NONE',  ( -19.38605492662632201, 35.40602226195235858, -140.5130341973394081 ) ) ;
#9233=CARTESIAN_POINT ( 'NONE',  ( -26.37173218084349458, 38.40595776404164496, -140.8139459235259778 ) ) ;
#9235=CARTESIAN_POINT ( 'NONE',  ( -22.46720159712088716, 36.13856230159614569, -139.5983244477151857 ) ) ;
#9246=CARTESIAN_POINT ( 'NONE',  ( -6.938784185764151680, 37.04974994750941164, -148.5388410751211268 ) ) ;
#9247=CARTESIAN_POINT ( 'NONE',  ( -11.01939500368477454, 36.32079862139720206, -140.6910194413075033 ) ) ;
#9257=CARTESIAN_POINT ( 'NONE',  ( -16.64966033334543738, 38.59029664588182129, -140.5654869318181284 ) ) ;
#9267=CARTESIAN_POINT ( 'NONE',  ( -28.25100290369999811, 33.74243115720000219, -145.9160084049999853 ) ) ;
#9283=ORIENTED_EDGE ( 'NONE', *, *, #17841, .T. ) ;
#9285=CARTESIAN_POINT ( 'NONE',  ( -19.68771884990000132, 32.54972883539999629, -143.8405663050000101 ) ) ;
#9288=CARTESIAN_POINT ( 'NONE',  ( -22.92066848190323114, 37.01209555897660408, -139.3757315019973930 ) ) ;
#9301=CARTESIAN_POINT ( 'NONE',  ( -13.37265858230000148, 32.83955069500000690, -141.7941727500000013 ) ) ;
#9315=CARTESIAN_POINT ( 'NONE',  ( -9.072898850179999641, 36.94639249900000522, -148.2684494029999769 ) ) ;
#9323=CARTESIAN_POINT ( 'NONE',  ( -19.59255166816691940, 37.05126161860788159, -140.3061871180788103 ) ) ;
#9326=( BOUNDED_SURFACE ( )  B_SPLINE_SURFACE ( 5, 5, ( 
 ( #15503, #6338, #889, #6576, #8473, #4681 ),
 ( #10012, #5036, #6690, #1125, #19551, #6461 ),
 ( #15386, #21343, #13594, #4561, #11799, #17289 ),
 ( #4797, #2785, #15851, #1001, #13950, #19310 ),
 ( #12162, #8230, #21223, #22763, #13719, #19435 ),
 ( #3139, #2899, #10369, #20991, #23118, #11923 ),
 ( #19189, #10129, #17404, #10831, #15976, #10720 ),
 ( #23236, #21817, #10953, #12634, #155, #7398 ),
 ( #14305, #14659, #40, #7162, #14428, #8820 ),
 ( #5610, #1473, #21928, #14553, #21576, #1599 ),
 ( #5258, #12509, #6931, #12747, #3715, #19790 ),
 ( #23466, #5501, #23353, #14192, #16096, #21699 ) ),
 .UNSPECIFIED., .F., .F., .F. ) 
 B_SPLINE_SURFACE_WITH_KNOTS ( ( 6, 3, 3, 6 ),
 ( 6, 6 ),
 ( 0.000000000000000000, 4.570086947620000117, 8.869210483019999813, 12.91901055009999943 ),
 ( 1.570796326400424991, 3.141592653590000062 ),
 .UNSPECIFIED. ) 
 GEOMETRIC_REPRESENTATION_ITEM ( )  RATIONAL_B_SPLINE_SURFACE ( (
 ( 0.2500000000000000000, 0.2499999999497609926, 0.2999999999246414917, 0.3999999998995225070, 0.5999999998995220185, 1.000000000000000000),
 ( 0.2500000000000000000, 0.2499999999497609926, 0.2999999999246414917, 0.3999999998995225070, 0.5999999998995220185, 1.000000000000000000),
 ( 0.2500000000000000000, 0.2499999999497609926, 0.2999999999246414917, 0.3999999998995225070, 0.5999999998995220185, 1.000000000000000000),
 ( 0.2500000000000000000, 0.2499999999497609926, 0.2999999999246414917, 0.3999999998995225070, 0.5999999998995220185, 1.000000000000000000),
 ( 0.2500000000000000000, 0.2499999999497609926, 0.2999999999246414917, 0.3999999998995225070, 0.5999999998995220185, 1.000000000000000000),
 ( 0.2500000000000000000, 0.2499999999497609926, 0.2999999999246414917, 0.3999999998995225070, 0.5999999998995220185, 1.000000000000000000),
 ( 0.2500000000000000000, 0.2499999999497609926, 0.2999999999246414917, 0.3999999998995225070, 0.5999999998995220185, 1.000000000000000000),
 ( 0.2500000000000000000, 0.2499999999497609926, 0.2999999999246414917, 0.3999999998995225070, 0.5999999998995220185, 1.000000000000000000),
 ( 0.2500000000000000000, 0.2499999999497609926, 0.2999999999246414917, 0.3999999998995225070, 0.5999999998995220185, 1.000000000000000000),
 ( 0.2500000000000000000, 0.2499999999497609926, 0.2999999999246414917, 0.3999999998995225070, 0.5999999998995220185, 1.000000000000000000),
 ( 0.2500000000000000000, 0.2499999999497609926, 0.2999999999246414917, 0.3999999998995225070, 0.5999999998995220185, 1.000000000000000000),
 ( 0.2500000000000000000, 0.2499999999497609926, 0.2999999999246414917, 0.3999999998995225070, 0.5999999998995220185, 1.000000000000000000) ) ) 
 REPRESENTATION_ITEM ( '' )  SURFACE ( )  );
#9329=CARTESIAN_POINT ( 'NONE',  ( -24.10813950037725206, 36.95059904178096133, -147.5089432696950382 ) ) ;
#9336=CARTESIAN_POINT ( 'NONE',  ( -25.48612782046226144, 37.91366991941922748, -140.0433563333232314 ) ) ;
#9337=ORIENTED_EDGE ( 'NONE', *, *, #4059, .T. ) ;
#9345=CARTESIAN_POINT ( 'NONE',  ( -27.58120011020000106, 38.53525547130000461, -147.4183263870000076 ) ) ;
#9346=CARTESIAN_POINT ( 'NONE',  ( -23.81889237380000068, 39.38287674749999923, -140.7489234159999967 ) ) ;
#9358=ADVANCED_FACE ( 'NONE', ( #5424 ), #7339, .F. ) ;
#9362=CARTESIAN_POINT ( 'NONE',  ( -12.82596392966510379, 39.28888178912641393, -147.2049309481724038 ) ) ;
#9363=CARTESIAN_POINT ( 'NONE',  ( -16.55393100702923093, 37.83050752194322541, -140.3603090961101429 ) ) ;
#9373=CARTESIAN_POINT ( 'NONE',  ( -20.72654659758507378, 41.81248471335479877, -143.6178682002461926 ) ) ;
#9375=CARTESIAN_POINT ( 'NONE',  ( -27.26567793390747596, 36.96940380712532459, -148.4835048638151989 ) ) ;
#9390=CARTESIAN_POINT ( 'NONE',  ( -22.39162803485939079, 36.31163189668782820, -140.3928250950291101 ) ) ;
#9396=CARTESIAN_POINT ( 'NONE',  ( -19.21862483442529523, 34.19907101541957672, -140.3476381199748744 ) ) ;
#9400=CARTESIAN_POINT ( 'NONE',  ( -23.84605196395386884, 41.80962803837999786, -144.6368725230021255 ) ) ;
#9402=CARTESIAN_POINT ( 'NONE',  ( -15.90559286389999905, 34.15404988380000617, -147.7469703310000000 ) ) ;
#9403=CARTESIAN_POINT ( 'NONE',  ( -19.57725164000000007, 32.58775676329999271, -144.7853266960000269 ) ) ;
#9408=CARTESIAN_POINT ( 'NONE',  ( -5.024157003614323713, 39.12743904224282687, -141.1587107399263914 ) ) ;
#9414=CARTESIAN_POINT ( 'NONE',  ( -22.17914504452174640, 36.26149632490731989, -147.8500484283999299 ) ) ;
#9417=CARTESIAN_POINT ( 'NONE',  ( -12.34038114069202585, 33.41076594416544765, -146.1814057331143886 ) ) ;
#9428=CARTESIAN_POINT ( 'NONE',  ( -13.21931118272387984, 33.83281470431867888, -146.0365350581830057 ) ) ;
#9440=CARTESIAN_POINT ( 'NONE',  ( -20.07993885570694559, 39.12723785091482398, -141.2403607577224420 ) ) ;
#9452=CARTESIAN_POINT ( 'NONE',  ( -27.03718401022160478, 40.11783903597983425, -145.8300916363254203 ) ) ;
#9454=CARTESIAN_POINT ( 'NONE',  ( -22.04078958492209850, 33.03316129315219740, -141.6299626085071566 ) ) ;
#9461=CARTESIAN_POINT ( 'NONE',  ( -28.90798551740000022, 37.01360947639999921, -139.5686590450000040 ) ) ;
#9469=CARTESIAN_POINT ( 'NONE',  ( -7.107905118430739577, 36.22301459085688435, -148.1570340886389943 ) ) ;
#9480=CARTESIAN_POINT ( 'NONE',  ( -11.82391492285750090, 41.25980026458489647, -141.7018521871114558 ) ) ;
#9491=CARTESIAN_POINT ( 'NONE',  ( -27.87941100700000163, 36.27261185799999765, -147.6334388379999893 ) ) ;
#9495=CARTESIAN_POINT ( 'NONE',  ( -20.55139866887920164, 40.46905695053816743, -146.1780460796892100 ) ) ;
#9525=CARTESIAN_POINT ( 'NONE',  ( -23.33899886291975889, 41.64279904421267986, -143.6714135781022605 ) ) ;
#9530=CARTESIAN_POINT ( 'NONE',  ( -15.94523344361886075, 33.71216531385520199, -145.7766456663750034 ) ) ;
#9537=CARTESIAN_POINT ( 'NONE',  ( -6.882992773709530887, 38.62672044876698152, -147.5226783901907481 ) ) ;
#9541=CARTESIAN_POINT ( 'NONE',  ( -22.20363240416772399, 34.86754896295690997, -140.9631074518152332 ) ) ;
#9546=CARTESIAN_POINT ( 'NONE',  ( -11.95558717921827885, 36.12952356042787727, -147.9535135442314129 ) ) ;
#9554=CARTESIAN_POINT ( 'NONE',  ( -28.26195922703709229, 35.47171465400183621, -147.6105075849922059 ) ) ;
#9557=CARTESIAN_POINT ( 'NONE',  ( -14.19107797818078787, 33.22326183629838425, -142.1039242036714541 ) ) ;
#9567=CARTESIAN_POINT ( 'NONE',  ( -20.40768304764253216, 38.39967751248821770, -140.8966145518345456 ) ) ;
#9570=CARTESIAN_POINT ( 'NONE',  ( -28.06178240310348571, 37.06443177824644408, -147.7991814974818396 ) ) ;
#9580=CARTESIAN_POINT ( 'NONE',  ( -22.18841299866283379, 32.72156082663942556, -146.4695531048793953 ) ) ;
#9587=CARTESIAN_POINT ( 'NONE',  ( -14.31404048459999956, 38.45176613019999934, -140.7319883510000125 ) ) ;
#9592=CARTESIAN_POINT ( 'NONE',  ( -9.005502668621559792, 40.51905748780640693, -141.9284054814384035 ) ) ;
#9595=B_SPLINE_CURVE_WITH_KNOTS ( 'NONE', 5,
 ( #21247, #4940, #5163, #1625, #12187, #3164, #3268, #10394, #1376, #8603, #10501, #12412 ),
 .UNSPECIFIED., .F., .F.,
 ( 6, 3, 3, 6 ),
 ( 0.000000000000000000, 4.358589029760000066, 8.533830367689999363, 12.54112731390000057 ),
 .UNSPECIFIED. ) ;
#9599=CARTESIAN_POINT ( 'NONE',  ( -11.80427317207966098, 41.71109129671971516, -144.7115759666664303 ) ) ;
#9601=CARTESIAN_POINT ( 'NONE',  ( -18.28762386024642339, 39.85118522382028772, -147.8656472858100983 ) ) ;
#9602=CARTESIAN_POINT ( 'NONE',  ( -29.95441468910000182, 40.29796007080000209, -145.3430615500000158 ) ) ;
#9611=CARTESIAN_POINT ( 'NONE',  ( -21.73552493300723754, 38.87455327618756940, -148.2354957168025180 ) ) ;
#9613=( BOUNDED_SURFACE ( )  B_SPLINE_SURFACE ( 5, 5, ( 
 ( #15040, #22301, #5992, #10377, #20996, #17295 ),
 ( #15635, #14087, #6699, #1481, #8704, #12173 ),
 ( #13730, #4806, #15985, #15750, #8589, #23012 ),
 ( #17413, #23247, #14204, #10020, #6940, #2792 ),
 ( #4690, #3147, #8239, #15860, #21355, #21466 ),
 ( #19086, #1136, #1011, #19448, #10271, #11930 ),
 ( #5045, #19319, #22771, #5146, #19560, #17537 ),
 ( #15512, #6471, #21230, #8366, #2907, #23126 ),
 ( #17766, #19195, #10139, #4926, #13849, #1255 ),
 ( #17654, #13961, #22900, #1360, #6584, #21114 ),
 ( #12049, #3033, #6818, #12287, #3253, #8482 ),
 ( #10487, #14314, #14786, #48, #12642, #21586 ) ),
 .UNSPECIFIED., .F., .F., .F. ) 
 B_SPLINE_SURFACE_WITH_KNOTS ( ( 6, 3, 3, 6 ),
 ( 6, 6 ),
 ( 0.000000000000000000, 4.346865784160000246, 8.778337911509998648, 13.29702284770000098 ),
 ( 0.000000000000000000, 1.570796326891464867 ),
 .UNSPECIFIED. ) 
 GEOMETRIC_REPRESENTATION_ITEM ( )  RATIONAL_B_SPLINE_SURFACE ( (
 ( 1.000000000000000000, 0.5999999999754349611, 0.3999999999754355051, 0.2999999999815765039, 0.2499999999877174917, 0.2500000000000000000),
 ( 1.000000000000000000, 0.5999999999754349611, 0.3999999999754355051, 0.2999999999815765039, 0.2499999999877174917, 0.2500000000000000000),
 ( 1.000000000000000000, 0.5999999999754349611, 0.3999999999754355051, 0.2999999999815765039, 0.2499999999877174917, 0.2500000000000000000),
 ( 1.000000000000000000, 0.5999999999754349611, 0.3999999999754355051, 0.2999999999815765039, 0.2499999999877174917, 0.2500000000000000000),
 ( 1.000000000000000000, 0.5999999999754349611, 0.3999999999754355051, 0.2999999999815765039, 0.2499999999877174917, 0.2500000000000000000),
 ( 1.000000000000000000, 0.5999999999754349611, 0.3999999999754355051, 0.2999999999815765039, 0.2499999999877174917, 0.2500000000000000000),
 ( 1.000000000000000000, 0.5999999999754349611, 0.3999999999754355051, 0.2999999999815765039, 0.2499999999877174917, 0.2500000000000000000),
 ( 1.000000000000000000, 0.5999999999754349611, 0.3999999999754355051, 0.2999999999815765039, 0.2499999999877174917, 0.2500000000000000000),
 ( 1.000000000000000000, 0.5999999999754349611, 0.3999999999754355051, 0.2999999999815765039, 0.2499999999877174917, 0.2500000000000000000),
 ( 1.000000000000000000, 0.5999999999754349611, 0.3999999999754355051, 0.2999999999815765039, 0.2499999999877174917, 0.2500000000000000000),
 ( 1.000000000000000000, 0.5999999999754349611, 0.3999999999754355051, 0.2999999999815765039, 0.2499999999877174917, 0.2500000000000000000),
 ( 1.000000000000000000, 0.5999999999754349611, 0.3999999999754355051, 0.2999999999815765039, 0.2499999999877174917, 0.2500000000000000000) ) ) 
 REPRESENTATION_ITEM ( '' )  SURFACE ( )  );
#9614=CARTESIAN_POINT ( 'NONE',  ( -28.07061429630000049, 34.82490105569999628, -147.0351741510000068 ) ) ;
#9639=CARTESIAN_POINT ( 'NONE',  ( -17.55745234320254866, 36.93608508457231920, -140.4812394865591045 ) ) ;
#9645=CARTESIAN_POINT ( 'NONE',  ( -5.251527070960000820, 40.93408815870000694, -143.6492421949999994 ) ) ;
#9651=CARTESIAN_POINT ( 'NONE',  ( -22.31464002779999944, 34.51618902799999944, -147.4864127260000259 ) ) ;
#9654=CARTESIAN_POINT ( 'NONE',  ( -12.28742291280838650, 34.42299388273512761, -147.6510490011623631 ) ) ;
#9657=EDGE_CURVE ( 'NONE', #4528, #12438, #1319, .T. ) ;
#9659=CARTESIAN_POINT ( 'NONE',  ( -27.77832206610000298, 37.03059619289999915, -147.6270870419999710 ) ) ;
#9663=CARTESIAN_POINT ( 'NONE',  ( -27.87941100700000163, 36.27261185799999765, -147.6334388379999893 ) ) ;
#9666=CARTESIAN_POINT ( 'NONE',  ( -13.02237250279999969, 32.42872598539999274, -144.6889042450000034 ) ) ;
#9667=CARTESIAN_POINT ( 'NONE',  ( -10.65913935279999869, 37.04331329920000115, -139.7140392919999954 ) ) ;
#9675=CARTESIAN_POINT ( 'NONE',  ( -20.49955794677946130, 40.53802795458025088, -144.5257500491008500 ) ) ;
#9681=CARTESIAN_POINT ( 'NONE',  ( -22.52780672249999938, 37.05898997719999954, -140.0074087190000114 ) ) ;
#9689=CARTESIAN_POINT ( 'NONE',  ( -27.67795712710000089, 37.78351609900000341, -147.6208067679999942 ) ) ;
#9691=CARTESIAN_POINT ( 'NONE',  ( -22.82643395159999855, 32.86988923359999859, -143.6006525860000238 ) ) ;
#9702=CARTESIAN_POINT ( 'NONE',  ( -8.613431449137619822, 37.75849558873363776, -140.1079839314714093 ) ) ;
#9709=CARTESIAN_POINT ( 'NONE',  ( -12.30631862527572018, 40.23402543372416318, -145.9987124283284174 ) ) ;
#9721=CARTESIAN_POINT ( 'NONE',  ( -19.69393976299120297, 37.84845892289124691, -140.3168504268994070 ) ) ;
#9724=CARTESIAN_POINT ( 'NONE',  ( -27.36101731545187477, 33.42236680594814402, -145.9827244586238919 ) ) ;
#9745=( BOUNDED_CURVE ( )  B_SPLINE_CURVE ( 5, ( #8153, #11722, #13404, #12084, #10176, #6265 ),
 .UNSPECIFIED., .F., .F. ) 
 B_SPLINE_CURVE_WITH_KNOTS ( ( 6, 6 ),
 ( 0.000000000000000000, 1.570796326630344186 ),
 .UNSPECIFIED. ) 
 CURVE ( )  GEOMETRIC_REPRESENTATION_ITEM ( )  RATIONAL_B_SPLINE_CURVE ( ( 1.000000000000000000, 0.6000000000419293267, 0.4000000000419293156, 0.3000000000314470006, 0.2500000000209646744, 0.2500000000000000555 ) ) 
 REPRESENTATION_ITEM ( '' )  );
#9749=CARTESIAN_POINT ( 'NONE',  ( -15.47773836757839661, 32.88821176121729195, -146.1526184873809200 ) ) ;
#9757=CARTESIAN_POINT ( 'NONE',  ( -10.47418533556643894, 33.50012463686687880, -145.9259304112847815 ) ) ;
#9762=CARTESIAN_POINT ( 'NONE',  ( -21.83347610788520043, 32.92361448635804066, -143.4947777357014047 ) ) ;
#9765=CARTESIAN_POINT ( 'NONE',  ( -12.60451255900682277, 35.62527299504891687, -147.2474940801387788 ) ) ;
#9776=( NAMED_UNIT ( * ) SI_UNIT ( $, .STERADIAN. ) SOLID_ANGLE_UNIT ( ) );
#9779=CARTESIAN_POINT ( 'NONE',  ( -13.57921699037008523, 33.70180771155908417, -146.1646008835299995 ) ) ;
#9789=FACE_OUTER_BOUND ( 'NONE', #22742, .T. ) ;
#9790=CARTESIAN_POINT ( 'NONE',  ( -18.61313235484081829, 39.16608643220034480, -146.8838699807833450 ) ) ;
#9794=CARTESIAN_POINT ( 'NONE',  ( -25.73504040789999792, 33.16200571349999393, -143.7184748760000161 ) ) ;
#9803=ORIENTED_EDGE ( 'NONE', *, *, #19864, .F. ) ;
#9814=CARTESIAN_POINT ( 'NONE',  ( -28.18164916501774897, 37.07873981899407312, -148.1638686016682414 ) ) ;
#9816=CARTESIAN_POINT ( 'NONE',  ( -10.71787290739701781, 39.39257728183631002, -141.0168776336601582 ) ) ;
#9820=CARTESIAN_POINT ( 'NONE',  ( -8.664978901450041349, 37.83471353584230457, -139.7100943505009809 ) ) ;
#9841=CARTESIAN_POINT ( 'NONE',  ( -19.59255166827864159, 37.05126161859452338, -140.3061871182728169 ) ) ;
#9873=CARTESIAN_POINT ( 'NONE',  ( -23.24588518177116114, 41.24341284997103685, -143.7187626422519884 ) ) ;
#9875=CARTESIAN_POINT ( 'NONE',  ( -16.55827375301752014, 37.05535324331041380, -139.5705083843697594 ) ) ;
#9882=CARTESIAN_POINT ( 'NONE',  ( -9.751275928061490461, 32.90710057661718935, -143.3218945113347615 ) ) ;
#9883=CARTESIAN_POINT ( 'NONE',  ( -30.02199999990000023, 40.89711431700000333, -146.3052959529999839 ) ) ;
#9886=CARTESIAN_POINT ( 'NONE',  ( -22.00705883600000234, 37.05789963359999462, -148.1619053240000028 ) ) ;
#9889=CARTESIAN_POINT ( 'NONE',  ( -23.15277150037254827, 40.84402665608095617, -143.7661117063971972 ) ) ;
#9893=CARTESIAN_POINT ( 'NONE',  ( -27.11867290101618977, 36.95185637389148781, -147.5185143933870222 ) ) ;
#9895=CARTESIAN_POINT ( 'NONE',  ( -9.562013113444269408, 37.00477621355919666, -148.7272342975821005 ) ) ;
#9896=CARTESIAN_POINT ( 'NONE',  ( -9.005502668715839931, 40.51905748822048281, -141.9284054811836029 ) ) ;
#9905=CARTESIAN_POINT ( 'NONE',  ( -27.16475626499999763, 37.90277890280000150, -148.4897851379999736 ) ) ;
#9913=CARTESIAN_POINT ( 'NONE',  ( -22.07763076357013077, 37.06632353693575510, -147.8362371614070696 ) ) ;
#9914=CARTESIAN_POINT ( 'NONE',  ( -17.88596104465900183, 38.55815351507766309, -140.2676819153700762 ) ) ;
#9919=CARTESIAN_POINT ( 'NONE',  ( -25.11008055915115378, 33.57149262957015878, -144.4317693003656586 ) ) ;
#9941=CARTESIAN_POINT ( 'NONE',  ( -7.529689113779999943, 37.05876528330000497, -139.9906690790000141 ) ) ;
#9942=CARTESIAN_POINT ( 'NONE',  ( -9.747014461865537882, 38.96264327593980425, -148.3170967394802631 ) ) ;
#9944=CARTESIAN_POINT ( 'NONE',  ( -27.58110728279999790, 34.24318910290000417, -147.7245096240000066 ) ) ;
#9961=CARTESIAN_POINT ( 'NONE',  ( -15.32446908972706190, 41.39793051967586734, -143.4941841294994447 ) ) ;
#9962=CARTESIAN_POINT ( 'NONE',  ( -25.17849978636914443, 32.75955230985957201, -146.5550213843877998 ) ) ;
#9972=ORIENTED_EDGE ( 'NONE', *, *, #13240, .F. ) ;
#9977=EDGE_CURVE ( 'NONE', #2118, #20985, #11279, .T. ) ;
#9992=CARTESIAN_POINT ( 'NONE',  ( -16.50205712333324826, 33.47704857309710036, -144.2911601313269898 ) ) ;
#9993=CARTESIAN_POINT ( 'NONE',  ( -4.609334941132099850, 37.98062953722018875, -139.6349070798746936 ) ) ;
#9998=CARTESIAN_POINT ( 'NONE',  ( -9.394775000179999225, 34.25903911019999981, -147.4808749560000081 ) ) ;
#10008=CARTESIAN_POINT ( 'NONE',  ( -23.68366236538869174, 38.48614108665564970, -140.6202320859351573 ) ) ;
#10012=CARTESIAN_POINT ( 'NONE',  ( -10.07619956174958098, 36.21908991358723995, -147.8536995440399835 ) ) ;
#10014=CARTESIAN_POINT ( 'NONE',  ( -8.712023184228140593, 38.57885015678616014, -140.3122811006342090 ) ) ;
#10017=CARTESIAN_POINT ( 'NONE',  ( -21.93648690847360072, 37.04947573026750973, -148.4875734863011303 ) ) ;
#10020=CARTESIAN_POINT ( 'NONE',  ( -7.080966237668673280, 35.02109009467289980, -146.9136362634284012 ) ) ;
#10025=CARTESIAN_POINT ( 'NONE',  ( -15.26331651089999930, 39.75437292659999855, -147.8043400740000095 ) ) ;
#10030=CARTESIAN_POINT ( 'NONE',  ( -17.84118295813777522, 39.08206477522340805, -141.0250297803352453 ) ) ;
#10034=CARTESIAN_POINT ( 'NONE',  ( -25.91744746520000220, 33.58572460659999592, -142.1592104600000255 ) ) ;
#10039=CARTESIAN_POINT ( 'NONE',  ( -27.11867290101617556, 36.95185637389150912, -147.5185143933871075 ) ) ;
#10049=CARTESIAN_POINT ( 'NONE',  ( -18.95027878879999861, 36.16636532760000478, -148.4341920939999966 ) ) ;
#10052=CARTESIAN_POINT ( 'NONE',  ( -8.208807763331680718, 34.49436158495667826, -140.8229124834255970 ) ) ;
#10053=CARTESIAN_POINT ( 'NONE',  ( -8.869124888310000898, 38.72872035620000020, -148.0517159070000162 ) ) ;
#10071=CARTESIAN_POINT ( 'NONE',  ( -15.23014954472039939, 40.61563974024299029, -144.3756286147995809 ) ) ;
#10072=CARTESIAN_POINT ( 'NONE',  ( -24.16551117127903936, 36.07182940195683329, -148.2420083170896135 ) ) ;
#10087=ADVANCED_FACE ( 'NONE', ( #19740 ), #12194, .F. ) ;
#10088=CARTESIAN_POINT ( 'NONE',  ( -25.12153080219999879, 33.08100675569999538, -141.7696838820000096 ) ) ;
#10113=CARTESIAN_POINT ( 'NONE',  ( -4.510059210066960311, 37.06110843049349768, -139.6225057176258133 ) ) ;
#10115=EDGE_CURVE ( 'NONE', #20464, #6561, #19512, .T. ) ;
#10117=CARTESIAN_POINT ( 'NONE',  ( -8.931798216468004981, 36.92954985151560265, -147.9669232058148793 ) ) ;
#10124=ORIENTED_EDGE ( 'NONE', *, *, #19412, .T. ) ;
#10125=CARTESIAN_POINT ( 'NONE',  ( -13.91784526144543932, 35.46792342014339994, -140.7554205113700050 ) ) ;
#10129=CARTESIAN_POINT ( 'NONE',  ( -10.98352009339088653, 32.87162191921307652, -143.4565451244976657 ) ) ;
#10139=CARTESIAN_POINT ( 'NONE',  ( -7.404748324622609346, 34.90846072521996746, -141.2185729789256357 ) ) ;
#10141=CARTESIAN_POINT ( 'NONE',  ( -20.55310894649999653, 37.85259822169999921, -139.7937414779999870 ) ) ;
#10149=CARTESIAN_POINT ( 'NONE',  ( -17.53224077489999999, 39.64394931100000008, -140.2973660050000149 ) ) ;
#10154=CARTESIAN_POINT ( 'NONE',  ( -25.98284937189643529, 35.54018228806221913, -140.8314003423548968 ) ) ;
#10156=CARTESIAN_POINT ( 'NONE',  ( -11.59046614940708153, 39.86879823875771933, -140.2222977132334165 ) ) ;
#10163=CARTESIAN_POINT ( 'NONE',  ( -27.49486172903679204, 36.99676060752978657, -147.4549925864818931 ) ) ;
#10174=CARTESIAN_POINT ( 'NONE',  ( -19.29243665411954822, 35.40841497951669936, -148.0186320824420818 ) ) ;
#10175=CARTESIAN_POINT ( 'NONE',  ( -11.31333818511670408, 38.44169350299409160, -140.8806452754523093 ) ) ;
#10176=CARTESIAN_POINT ( 'NONE',  ( -12.41698512465752380, 36.98746477262142918, -147.4237781435811030 ) ) ;
#10178=CARTESIAN_POINT ( 'NONE',  ( -9.674592407111139991, 39.37273218265404040, -147.1879168908690190 ) ) ;
#10191=VERTEX_POINT ( 'NONE', #15780 ) ;
#10192=CARTESIAN_POINT ( 'NONE',  ( -22.92066848221891107, 37.01209555893892400, -139.3757315020603187 ) ) ;
#10195=CARTESIAN_POINT ( 'NONE',  ( -14.50908993386010870, 36.94185792196182661, -140.4668331870292377 ) ) ;
#10196=CARTESIAN_POINT ( 'NONE',  ( -25.42000568121191151, 32.21859392833894731, -144.6204194868284958 ) ) ;
#10220=CARTESIAN_POINT ( 'NONE',  ( -14.78241661194416068, 39.12140059992913166, -147.0349140006744904 ) ) ;
#10233=CARTESIAN_POINT ( 'NONE',  ( -16.63107678134597833, 35.60580843634807735, -140.6802342587363910 ) ) ;
#10239=CARTESIAN_POINT ( 'NONE',  ( -9.592967682888913217, 35.51842212454483416, -147.1736941271391004 ) ) ;
#10251=CARTESIAN_POINT ( 'NONE',  ( -28.94327676059999988, 35.53474617860000251, -140.7339624629999832 ) ) ;
#10254=CARTESIAN_POINT ( 'NONE',  ( -23.96059125624836028, 40.27687008288653203, -142.1584808468900860 ) ) ;
#10271=CARTESIAN_POINT ( 'NONE',  ( -7.724735339242877252, 33.29363753972616280, -144.6062484440719231 ) ) ;
#10276=CARTESIAN_POINT ( 'NONE',  ( -15.03885004549999849, 41.12207116019999376, -146.4108951270000034 ) ) ;
#10279=CARTESIAN_POINT ( 'NONE',  ( -17.55745234318444759, 36.93608508457451478, -140.4812394866132763 ) ) ;
#10284=CARTESIAN_POINT ( 'NONE',  ( -24.60351133389204392, 36.30534674873651824, -147.3819557762199963 ) ) ;
#10299=CARTESIAN_POINT ( 'NONE',  ( -19.28609856419999957, 34.66429844339999988, -140.9609051179999994 ) ) ;
#10300=CARTESIAN_POINT ( 'NONE',  ( -11.11377970773875923, 36.98904460433606545, -140.6889018750556772 ) ) ;
#10302=CARTESIAN_POINT ( 'NONE',  ( -7.687380149402162743, 32.47466110599622624, -144.7109350977037820 ) ) ;
#10303=CARTESIAN_POINT ( 'NONE',  ( -9.624908808166578567, 40.88242544008282664, -146.1844385046725279 ) ) ;
#10305=CARTESIAN_POINT ( 'NONE',  ( -28.70612892850000009, 35.15950212979999634, -139.8035036599999898 ) ) ;
#10307=CARTESIAN_POINT ( 'NONE',  ( -7.529689113779999943, 37.05876528330000497, -139.9906690790000141 ) ) ;
#10312=B_SPLINE_CURVE_WITH_KNOTS ( 'NONE', 5,
 ( #330, #20214, #1582, #9346, #21558, #5241, #4896, #10462, #19646, #3122, #5680, #20088 ),
 .UNSPECIFIED., .F., .F.,
 ( 6, 3, 3, 6 ),
 ( 0.000000000000000000, 4.509114667229999540, 8.972055907920001516, 13.39149027789999913 ),
 .UNSPECIFIED. ) ;
#10321=CARTESIAN_POINT ( 'NONE',  ( -15.00140173380579967, 40.20535686067439940, -145.8913236318788051 ) ) ;
#10322=CARTESIAN_POINT ( 'NONE',  ( -25.81549887252723252, 32.87029380595873818, -144.5911656381801151 ) ) ;
#10339=CARTESIAN_POINT ( 'NONE',  ( -15.36599175860845889, 37.73046438850320072, -147.5598381917453992 ) ) ;
#10340=CARTESIAN_POINT ( 'NONE',  ( -28.93111463330243893, 37.94265998448511823, -140.6213208041744736 ) ) ;
#10350=CARTESIAN_POINT ( 'NONE',  ( -16.04375348400463608, 33.06607696223074555, -141.5117709027480259 ) ) ;
#10360=CARTESIAN_POINT ( 'NONE',  ( -29.19553354363359077, 36.02155055457190969, -139.4833455107854832 ) ) ;
#10369=CARTESIAN_POINT ( 'NONE',  ( -10.75335342199438671, 32.39647868472179937, -144.3483278521977411 ) ) ;
#10370=CARTESIAN_POINT ( 'NONE',  ( -18.85469010170000459, 37.03971195569999963, -148.4264296979999926 ) ) ;
#10371=CARTESIAN_POINT ( 'NONE',  ( -8.730967964694192673, 38.58574671193542827, -147.7727093204715914 ) ) ;
#10377=CARTESIAN_POINT ( 'NONE',  ( -6.804059094871798052, 37.03366832437883716, -147.4295713064250890 ) ) ;
#10378=CARTESIAN_POINT ( 'NONE',  ( -29.18503926089999823, 39.40432144729999919, -139.9690405629999930 ) ) ;
#10379=CARTESIAN_POINT ( 'NONE',  ( -21.90852802850000103, 37.90475843469999973, -148.1502781210000137 ) ) ;
#10386=CARTESIAN_POINT ( 'NONE',  ( -21.70512920578378058, 38.46301180794304031, -147.3000385647142139 ) ) ;
#10394=CARTESIAN_POINT ( 'NONE',  ( -16.71251657190000017, 33.01037093000000766, -141.5651630139999781 ) ) ;
#10397=VERTEX_POINT ( 'NONE', #10517 ) ;
#10398=CARTESIAN_POINT ( 'NONE',  ( -23.32853373970706912, 36.96341023006314686, -139.4571126576171878 ) ) ;
#10410=CARTESIAN_POINT ( 'NONE',  ( -18.82091118379999983, 33.23810407359999886, -144.5979112940000277 ) ) ;
#10412=CARTESIAN_POINT ( 'NONE',  ( -11.69335150359915687, 39.46909266604216526, -147.6919637091589550 ) ) ;
#10414=CARTESIAN_POINT ( 'NONE',  ( -7.706057744140959898, 32.88414932316476325, -144.6585917708268028 ) ) ;
#10426=CARTESIAN_POINT ( 'NONE',  ( -10.76224745929999926, 37.97907322949999553, -139.7231730900000173 ) ) ;
#10428=CARTESIAN_POINT ( 'NONE',  ( -21.03694116389347712, 36.94210036640072303, -147.9486865818473973 ) ) ;
#10429=CARTESIAN_POINT ( 'NONE',  ( -25.64408091310000160, 33.16124342930000068, -144.5387451670000019 ) ) ;
#10430=ORIENTED_EDGE ( 'NONE', *, *, #374, .T. ) ;
#10434=CARTESIAN_POINT ( 'NONE',  ( -12.48399912370000031, 39.13586957980000136, -147.0556079069999953 ) ) ;
#10446=CARTESIAN_POINT ( 'NONE',  ( -14.16161598212295125, 40.91800955835415721, -144.5270132969140207 ) ) ;
#10461=CARTESIAN_POINT ( 'NONE',  ( -5.271986118780953134, 36.97016010513711848, -139.4665544805324089 ) ) ;
#10462=CARTESIAN_POINT ( 'NONE',  ( -24.49703822390000241, 40.50511125069999707, -146.0729279460000214 ) ) ;
#10470=CARTESIAN_POINT ( 'NONE',  ( -28.99748895112272251, 32.89468467962849729, -143.6350524796266654 ) ) ;
#10480=CARTESIAN_POINT ( 'NONE',  ( -8.151404454119415277, 40.91889870648304139, -143.6674959883383167 ) ) ;
#10487=CARTESIAN_POINT ( 'NONE',  ( -7.529689113779999943, 37.05876528330000497, -139.9906690790000141 ) ) ;
#10501=CARTESIAN_POINT ( 'NONE',  ( -17.13033207850000039, 36.08498863180000171, -139.6042211940000186 ) ) ;
#10508=( BOUNDED_CURVE ( )  B_SPLINE_CURVE ( 5, ( #13731, #8005, #10378, #4691, #6585, #21231, #2908, #6700, #17538 ),
 .UNSPECIFIED., .F., .F. ) 
 B_SPLINE_CURVE_WITH_KNOTS ( ( 6, 3, 6 ),
 ( 0.000000000000000000, 5.731822293570000504, 9.005131590149998644 ),
 .UNSPECIFIED. ) 
 CURVE ( )  GEOMETRIC_REPRESENTATION_ITEM ( )  RATIONAL_B_SPLINE_CURVE ( ( 0.2500000000000000000, 0.2500000000000000000, 0.2500000000000000000, 0.2500000000000000000, 0.2500000000000000000, 0.2500000000000000000, 0.2500000000000000000, 0.2500000000000000000, 0.2500000000000000000 ) ) 
 REPRESENTATION_ITEM ( '' )  );
#10517=CARTESIAN_POINT ( 'NONE',  ( -19.59255166829999695, 37.05126161860000167, -140.3061871179999969 ) ) ;
#10518=CARTESIAN_POINT ( 'NONE',  ( -9.292483939630001188, 40.96918990780000058, -144.3907905730000039 ) ) ;
#10543=CARTESIAN_POINT ( 'NONE',  ( -15.39869693353375268, 40.21355843083121329, -145.8451804845391280 ) ) ;
#10549=CARTESIAN_POINT ( 'NONE',  ( -25.64792992843672081, 37.04465132569895758, -139.7265440088568198 ) ) ;
#10562=CARTESIAN_POINT ( 'NONE',  ( -14.58162373624594110, 40.18882273015199758, -142.1871799654946074 ) ) ;
#10578=CARTESIAN_POINT ( 'NONE',  ( -5.974012367534657031, 36.93458879463069167, -148.2930816546209769 ) ) ;
#10599=CARTESIAN_POINT ( 'NONE',  ( -18.70471434392063514, 36.09242347422292596, -148.6518277728152100 ) ) ;
#10614=CARTESIAN_POINT ( 'NONE',  ( -4.584402860569999127, 37.05223431090000474, -140.2914745300000163 ) ) ;
#10630=CARTESIAN_POINT ( 'NONE',  ( -13.92432874550000044, 37.01165864720000087, -139.5650670249999905 ) ) ;
#10636=CARTESIAN_POINT ( 'NONE',  ( -16.16113997806470692, 37.07629171513308819, -147.8146678479332365 ) ) ;
#10637=CARTESIAN_POINT ( 'NONE',  ( -28.00933461728345009, 33.78802393297787177, -142.0848207868532711 ) ) ;
#10638=EDGE_LOOP ( 'NONE', ( #804, #5812, #2260, #12074 ) ) ;
#10642=CARTESIAN_POINT ( 'NONE',  ( -19.59255166816691940, 37.05126161860788159, -140.3061871180788103 ) ) ;
#10643=CARTESIAN_POINT ( 'NONE',  ( -12.08222824379999949, 38.77433534089999512, -148.2726881729999775 ) ) ;
#10658=ORIENTED_EDGE ( 'NONE', *, *, #17582, .T. ) ;
#10663=CARTESIAN_POINT ( 'NONE',  ( -12.28014746100000032, 36.97113097969999984, -148.4919582129999753 ) ) ;
#10665=CARTESIAN_POINT ( 'NONE',  ( -15.57415625657761282, 39.15353770086346685, -146.9238453625318925 ) ) ;
#10670=CARTESIAN_POINT ( 'NONE',  ( -26.16983372419520038, 40.98399646752800152, -141.7700373851359927 ) ) ;
#10676=CARTESIAN_POINT ( 'NONE',  ( -30.02199999990000023, 40.89711431700000333, -146.3052959529999839 ) ) ;
#10679=CARTESIAN_POINT ( 'NONE',  ( -16.36784392970000113, 33.86562477380000047, -142.0582287350000001 ) ) ;
#10685=CARTESIAN_POINT ( 'NONE',  ( -11.65594158659679458, 36.92432879710134586, -140.1042033534126290 ) ) ;
#10687=CARTESIAN_POINT ( 'NONE',  ( -14.31404048469557999, 38.45176613018656298, -140.7319883511174226 ) ) ;
#10703=CARTESIAN_POINT ( 'NONE',  ( -5.169538687456003423, 39.83360900324895937, -140.1488912727290881 ) ) ;
#10715=CARTESIAN_POINT ( 'NONE',  ( -23.96729089107739696, 37.81249143161688409, -148.2640374884782091 ) ) ;
#10716=CARTESIAN_POINT ( 'NONE',  ( -29.32937220831407643, 40.41939957101111958, -140.7656299762568040 ) ) ;
#10720=CARTESIAN_POINT ( 'NONE',  ( -9.944031889410000602, 32.62729151690000151, -143.2983400859999961 ) ) ;
#10721=CARTESIAN_POINT ( 'NONE',  ( -18.99012760142337441, 32.85953695965795873, -141.8126290792370696 ) ) ;
#10722=CARTESIAN_POINT ( 'NONE',  ( -9.174907861666381947, 40.57495297524849320, -144.3653690793416615 ) ) ;
#10729=CARTESIAN_POINT ( 'NONE',  ( -6.288682381900000173, 41.28368337119999865, -144.4167712529999790 ) ) ;
#10760=CARTESIAN_POINT ( 'NONE',  ( -11.53909816450000037, 41.50279269539999660, -144.7127947380000137 ) ) ;
#10779=CARTESIAN_POINT ( 'NONE',  ( -21.93648690846499605, 37.04947573026642971, -148.4875734863409775 ) ) ;
#10784=CARTESIAN_POINT ( 'NONE',  ( -26.81858241934068943, 38.72415308318589666, -139.9577798820823489 ) ) ;
#10789=CARTESIAN_POINT ( 'NONE',  ( -10.33840623949446424, 36.25694129130458521, -139.9440796118479398 ) ) ;
#10792=CARTESIAN_POINT ( 'NONE',  ( -15.76532943049999780, 34.76918918230000344, -146.9254579969999952 ) ) ;
#10797=CARTESIAN_POINT ( 'NONE',  ( -15.46613156839596037, 36.99333119720399310, -147.5584717933712113 ) ) ;
#10815=CARTESIAN_POINT ( 'NONE',  ( -6.010199571182928580, 41.30249798234603986, -146.4953287552840777 ) ) ;
#10822=CARTESIAN_POINT ( 'NONE',  ( -25.10891061333512653, 37.07005729393354443, -148.1636427046708491 ) ) ;
#10826=CARTESIAN_POINT ( 'NONE',  ( -29.55850978546380148, 41.47329217817320313, -142.4456950392549857 ) ) ;
#10827=CARTESIAN_POINT ( 'NONE',  ( -22.23138069770000058, 34.62558912630000663, -140.6296127990000002 ) ) ;
#10831=CARTESIAN_POINT ( 'NONE',  ( -10.50749457979810586, 32.24767484617476754, -143.3007931252695073 ) ) ;
#10833=CARTESIAN_POINT ( 'NONE',  ( -19.14968637899999848, 34.49201595030000078, -147.7870032629999741 ) ) ;
#10834=ADVANCED_FACE ( 'NONE', ( #16113 ), #21943, .F. ) ;
#10835=CARTESIAN_POINT ( 'NONE',  ( -8.932337917339909339, 37.68960189247532355, -147.6085193066813304 ) ) ;
#10847=CARTESIAN_POINT ( 'NONE',  ( -5.746192911800908298, 37.73100506242058572, -140.1565350977006119 ) ) ;
#10853=B_SPLINE_CURVE_WITH_KNOTS ( 'NONE', 5,
 ( #13212, #20487, #13562, #20834, #18706, #2415, #16906, #22386, #4303, #11533, #22729, #23207 ),
 .UNSPECIFIED., .F., .F.,
 ( 6, 3, 3, 6 ),
 ( 0.000000000000000000, 4.371092480729999785, 8.745625541600000830, 13.12578902609999965 ),
 .UNSPECIFIED. ) ;
#10862=( BOUNDED_SURFACE ( )  B_SPLINE_SURFACE ( 5, 5, ( 
 ( #7868, #13230, #2434, #4080, #758, #9886 ),
 ( #14915, #4322, #18725, #2660, #9414, #4207 ),
 ( #11552, #17160, #4431, #882, #2539, #15143 ),
 ( #11201, #22526, #18828, #13115, #6102, #9651 ),
 ( #16923, #635, #22406, #7642, #20508, #13354 ),
 ( #15379, #16813, #20627, #16691, #13467, #3969 ),
 ( #9762, #17039, #6329, #7988, #22286, #18476 ),
 ( #6219, #406, #11667, #11441, #20388, #11318 ),
 ( #18599, #9541, #525, #7757, #15021, #2169 ),
 ( #22150, #7734, #21924, #4181, #16900, #18569 ),
 ( #6078, #9390, #20256, #20599, #5951, #13092 ),
 ( #22377, #5836, #20363, #5605, #16444, #4058 ) ),
 .UNSPECIFIED., .F., .F., .F. ) 
 B_SPLINE_SURFACE_WITH_KNOTS ( ( 6, 3, 3, 6 ),
 ( 6, 6 ),
 ( 0.000000000000000000, 4.463483057499999518, 8.880954762089999122, 13.25426345570000031 ),
 ( 1.570796326503985041, 3.141592653590000062 ),
 .UNSPECIFIED. ) 
 GEOMETRIC_REPRESENTATION_ITEM ( )  RATIONAL_B_SPLINE_SURFACE ( (
 ( 0.2500000000000000000, 0.2499999999629470004, 0.2999999999444205034, 0.3999999999258939676, 0.5999999999258940342, 1.000000000000000000),
 ( 0.2500000000000000000, 0.2499999999629470004, 0.2999999999444205034, 0.3999999999258939676, 0.5999999999258940342, 1.000000000000000000),
 ( 0.2500000000000000000, 0.2499999999629470004, 0.2999999999444205034, 0.3999999999258939676, 0.5999999999258940342, 1.000000000000000000),
 ( 0.2500000000000000000, 0.2499999999629470004, 0.2999999999444205034, 0.3999999999258939676, 0.5999999999258940342, 1.000000000000000000),
 ( 0.2500000000000000000, 0.2499999999629470004, 0.2999999999444205034, 0.3999999999258939676, 0.5999999999258940342, 1.000000000000000000),
 ( 0.2500000000000000000, 0.2499999999629470004, 0.2999999999444205034, 0.3999999999258939676, 0.5999999999258940342, 1.000000000000000000),
 ( 0.2500000000000000000, 0.2499999999629470004, 0.2999999999444205034, 0.3999999999258939676, 0.5999999999258940342, 1.000000000000000000),
 ( 0.2500000000000000000, 0.2499999999629470004, 0.2999999999444205034, 0.3999999999258939676, 0.5999999999258940342, 1.000000000000000000),
 ( 0.2500000000000000000, 0.2499999999629470004, 0.2999999999444205034, 0.3999999999258939676, 0.5999999999258940342, 1.000000000000000000),
 ( 0.2500000000000000000, 0.2499999999629470004, 0.2999999999444205034, 0.3999999999258939676, 0.5999999999258940342, 1.000000000000000000),
 ( 0.2500000000000000000, 0.2499999999629470004, 0.2999999999444205034, 0.3999999999258939676, 0.5999999999258940342, 1.000000000000000000),
 ( 0.2500000000000000000, 0.2499999999629470004, 0.2999999999444205034, 0.3999999999258939676, 0.5999999999258940342, 1.000000000000000000) ) ) 
 REPRESENTATION_ITEM ( '' )  SURFACE ( )  );
#10873=CARTESIAN_POINT ( 'NONE',  ( -13.47473365134610290, 34.60989327097050250, -147.6241178362156745 ) ) ;
#10878=CARTESIAN_POINT ( 'NONE',  ( -19.17479249162562027, 35.04308797501523287, -146.9876367767126908 ) ) ;
#10879=CARTESIAN_POINT ( 'NONE',  ( -12.76385253892641991, 37.02886902030763849, -147.6186336935359975 ) ) ;
#10889=ADVANCED_FACE ( 'NONE', ( #19296 ), #13733, .F. ) ;
#10897=CARTESIAN_POINT ( 'NONE',  ( -26.87491139698960652, 40.50028737762694675, -144.3978882166674396 ) ) ;
#10899=CARTESIAN_POINT ( 'NONE',  ( -15.47708384459999920, 37.95279615419999431, -148.5507537150000132 ) ) ;
#10904=CARTESIAN_POINT ( 'NONE',  ( -27.29484193126405600, 40.93981164352350532, -143.5422035504862208 ) ) ;
#10918=CARTESIAN_POINT ( 'NONE',  ( -17.01025018545970013, 38.48180121062596015, -140.7067500820750183 ) ) ;
#10919=CARTESIAN_POINT ( 'NONE',  ( -29.49311769368501857, 40.53847605628178741, -144.3259011655036375 ) ) ;
#10936=CARTESIAN_POINT ( 'NONE',  ( -6.064688046277384004, 37.92358258467430687, -148.6337691084673338 ) ) ;
#10941=ORIENTED_EDGE ( 'NONE', *, *, #1084, .T. ) ;
#10945=CARTESIAN_POINT ( 'NONE',  ( -24.06602356380263785, 36.94557182218072455, -148.2530914613568029 ) ) ;
#10953=CARTESIAN_POINT ( 'NONE',  ( -11.08944297849076399, 33.05461395872589492, -141.6094732493307617 ) ) ;
#10955=CARTESIAN_POINT ( 'NONE',  ( -19.10658510145665900, 32.20893999946100195, -143.7553378037570155 ) ) ;
#10959=CARTESIAN_POINT ( 'NONE',  ( -23.54789306461707810, 36.93722613941657329, -139.7713821669954370 ) ) ;
#10968=CARTESIAN_POINT ( 'NONE',  ( -6.705189174517019346, 39.56570632389819764, -147.4373625594447788 ) ) ;
#10987=CARTESIAN_POINT ( 'NONE',  ( -14.11967125440000004, 36.98834135279999913, -140.5455248810000057 ) ) ;
#10996=CARTESIAN_POINT ( 'NONE',  ( -17.28155659539766731, 34.85587989530459652, -141.0407616605357930 ) ) ;
#11002=CARTESIAN_POINT ( 'NONE',  ( -19.58178540279576652, 33.51645733664073390, -143.8848924971558176 ) ) ;
#11010=( BOUNDED_SURFACE ( )  B_SPLINE_SURFACE ( 5, 5, ( 
 ( #15079, #22338, #3915, #4367, #20331, #2370 ),
 ( #9702, #9820, #16978, #6033, #4134, #11604 ),
 ( #16746, #459, #7696, #11376, #14965, #18881 ),
 ( #22226, #7922, #15204, #18655, #14727, #5915 ),
 ( #9592, #21995, #18421, #13288, #20558, #22458 ),
 ( #6154, #2592, #223, #5686, #2131, #16624 ),
 ( #3070, #2944, #1046, #8275, #17214, #19360 ),
 ( #815, #10303, #8042, #2715, #11724, #4722 ),
 ( #10178, #8405, #17579, #1294, #17099, #22686 ),
 ( #11967, #17330, #9942, #19231, #6620, #10053 ),
 ( #15321, #12086, #15548, #20791, #22578, #4483 ),
 ( #6381, #15678, #6267, #13518, #8155, #11847 ) ),
 .UNSPECIFIED., .F., .F., .F. ) 
 B_SPLINE_SURFACE_WITH_KNOTS ( ( 6, 3, 3, 6 ),
 ( 6, 6 ),
 ( 0.000000000000000000, 4.371092480729999785, 8.745625541600000830, 13.12578902609999965 ),
 ( 1.570796326521529895, 3.141592653590000062 ),
 .UNSPECIFIED. ) 
 GEOMETRIC_REPRESENTATION_ITEM ( )  RATIONAL_B_SPLINE_SURFACE ( (
 ( 0.2500000000000000000, 0.2499999999651804916, 0.2999999999477704904, 0.3999999999303610054, 0.5999999999303610165, 1.000000000000000000),
 ( 0.2500000000000000000, 0.2499999999651804916, 0.2999999999477704904, 0.3999999999303610054, 0.5999999999303610165, 1.000000000000000000),
 ( 0.2500000000000000000, 0.2499999999651804916, 0.2999999999477704904, 0.3999999999303610054, 0.5999999999303610165, 1.000000000000000000),
 ( 0.2500000000000000000, 0.2499999999651804916, 0.2999999999477704904, 0.3999999999303610054, 0.5999999999303610165, 1.000000000000000000),
 ( 0.2500000000000000000, 0.2499999999651804916, 0.2999999999477704904, 0.3999999999303610054, 0.5999999999303610165, 1.000000000000000000),
 ( 0.2500000000000000000, 0.2499999999651804916, 0.2999999999477704904, 0.3999999999303610054, 0.5999999999303610165, 1.000000000000000000),
 ( 0.2500000000000000000, 0.2499999999651804916, 0.2999999999477704904, 0.3999999999303610054, 0.5999999999303610165, 1.000000000000000000),
 ( 0.2500000000000000000, 0.2499999999651804916, 0.2999999999477704904, 0.3999999999303610054, 0.5999999999303610165, 1.000000000000000000),
 ( 0.2500000000000000000, 0.2499999999651804916, 0.2999999999477704904, 0.3999999999303610054, 0.5999999999303610165, 1.000000000000000000),
 ( 0.2500000000000000000, 0.2499999999651804916, 0.2999999999477704904, 0.3999999999303610054, 0.5999999999303610165, 1.000000000000000000),
 ( 0.2500000000000000000, 0.2499999999651804916, 0.2999999999477704904, 0.3999999999303610054, 0.5999999999303610165, 1.000000000000000000),
 ( 0.2500000000000000000, 0.2499999999651804916, 0.2999999999477704904, 0.3999999999303610054, 0.5999999999303610165, 1.000000000000000000) ) ) 
 REPRESENTATION_ITEM ( '' )  SURFACE ( )  );
#11015=CARTESIAN_POINT ( 'NONE',  ( -28.18164916493977756, 37.07873981898478633, -148.1638686014308632 ) ) ;
#11021=CARTESIAN_POINT ( 'NONE',  ( -25.80099178304097762, 37.02638091262101483, -140.6905788942604261 ) ) ;
#11023=CARTESIAN_POINT ( 'NONE',  ( -23.01788799736533875, 34.20869732335551561, -140.2024652167382328 ) ) ;
#11024=CARTESIAN_POINT ( 'NONE',  ( -29.95441468910000182, 40.29796007080000209, -145.3430615500000158 ) ) ;
#11030=CARTESIAN_POINT ( 'NONE',  ( -25.90907760989742670, 37.01347911741230945, -139.4251635482865765 ) ) ;
#11044=CARTESIAN_POINT ( 'NONE',  ( -16.92892821565927974, 40.42700121177570338, -142.0839162034752121 ) ) ;
#11045=CARTESIAN_POINT ( 'NONE',  ( -29.31903837101844346, 40.46341529379842683, -142.8387304625044010 ) ) ;
#11047=CARTESIAN_POINT ( 'NONE',  ( -6.812760379890000273, 32.88798608609999974, -143.6676051400000063 ) ) ;
#11054=CARTESIAN_POINT ( 'NONE',  ( -27.58110728285923940, 34.24318910288427986, -147.7245096245594027 ) ) ;
#11057=CARTESIAN_POINT ( 'NONE',  ( -5.872912812989576459, 37.83051333333958155, -148.3065483569547780 ) ) ;
#11062=CARTESIAN_POINT ( 'NONE',  ( -26.68542098469999857, 39.18140699330000132, -140.9632721460000084 ) ) ;
#11075=CARTESIAN_POINT ( 'NONE',  ( -19.39325354300213533, 37.07505107993059568, -139.9601895477539131 ) ) ;
#11086=CARTESIAN_POINT ( 'NONE',  ( -6.389646268321180322, 36.98420143700543861, -147.3954793911336481 ) ) ;
#11095=CARTESIAN_POINT ( 'NONE',  ( -13.05391057859098325, 32.94097121706953857, -141.8088358606670454 ) ) ;
#11107=ADVANCED_FACE ( 'NONE', ( #11491 ), #818, .F. ) ;
#11114=VERTEX_POINT ( 'NONE', #4607 ) ;
#11117=CARTESIAN_POINT ( 'NONE',  ( -20.10690122708593108, 36.24603085032271110, -140.7204002581620728 ) ) ;
#11122=CARTESIAN_POINT ( 'NONE',  ( -17.89449577229859401, 36.92509720026601627, -147.9522036891449943 ) ) ;
#11130=CARTESIAN_POINT ( 'NONE',  ( -25.93177281299394465, 40.35538820219090894, -142.1683974516384410 ) ) ;
#11133=CARTESIAN_POINT ( 'NONE',  ( -22.56584646715587539, 37.05444931714286838, -139.6092474954658940 ) ) ;
#11146=( BOUNDED_CURVE ( )  B_SPLINE_CURVE ( 5, ( #7676, #9570, #11015, #2003, #16846, #18292 ),
 .UNSPECIFIED., .F., .F. ) 
 B_SPLINE_CURVE_WITH_KNOTS ( ( 6, 6 ),
 ( 0.000000000000000000, 1.570796326695737877 ),
 .UNSPECIFIED. ) 
 CURVE ( )  GEOMETRIC_REPRESENTATION_ITEM ( )  RATIONAL_B_SPLINE_CURVE ( ( 1.000000000000000000, 0.6000000000252768695, 0.4000000000252768584, 0.3000000000189576577, 0.2500000000126384458, 0.2500000000000000000 ) ) 
 REPRESENTATION_ITEM ( '' )  );
#11147=CARTESIAN_POINT ( 'NONE',  ( -10.43323856990612875, 37.07027821888497954, -139.9576636760149313 ) ) ;
#11154=CARTESIAN_POINT ( 'NONE',  ( -11.19806794730000021, 41.07225940149999843, -141.8826665010000170 ) ) ;
#11156=CARTESIAN_POINT ( 'NONE',  ( -16.54806230416816959, 38.77190534598552318, -140.1780706808168588 ) ) ;
#11157=CARTESIAN_POINT ( 'NONE',  ( -29.62343099156833759, 40.28042712731500785, -145.3785591165033679 ) ) ;
#11160=CARTESIAN_POINT ( 'NONE',  ( -25.80099178328665488, 37.02638091259170494, -140.6905788942244158 ) ) ;
#11167=CARTESIAN_POINT ( 'NONE',  ( -19.59722155829454593, 38.81238647146790299, -140.2173786323916715 ) ) ;
#11169=CARTESIAN_POINT ( 'NONE',  ( -27.78250035523632988, 34.89932656597451199, -146.8789310658169427 ) ) ;
#11174=ORIENTED_EDGE ( 'NONE', *, *, #2702, .T. ) ;
#11181=CARTESIAN_POINT ( 'NONE',  ( -29.29455083632570123, 36.96746664035849506, -139.4767999530270117 ) ) ;
#11186=CARTESIAN_POINT ( 'NONE',  ( -18.42369010557010967, 35.12722143684463560, -148.4184552812508571 ) ) ;
#11190=CARTESIAN_POINT ( 'NONE',  ( -24.53283754947133488, 37.97921577274999549, -148.7308746522571141 ) ) ;
#11198=CARTESIAN_POINT ( 'NONE',  ( -5.659867863817344080, 38.70771930248351822, -140.0293976191753984 ) ) ;
#11201=CARTESIAN_POINT ( 'NONE',  ( -21.33871772388139831, 34.54066873246879510, -147.2646375964223751 ) ) ;
#11205=CARTESIAN_POINT ( 'NONE',  ( -13.20169807812806084, 35.46390522416190549, -140.5417041917768302 ) ) ;
#11211=ORIENTED_EDGE ( 'NONE', *, *, #6762, .F. ) ;
#11227=CARTESIAN_POINT ( 'NONE',  ( -21.40986708713248632, 40.96636350904213231, -144.4750854696517877 ) ) ;
#11230=CARTESIAN_POINT ( 'NONE',  ( -7.010349701930000066, 37.05829245179999987, -148.1453878979999956 ) ) ;
#11239=CARTESIAN_POINT ( 'NONE',  ( -26.95224972473072000, 39.68365438105159626, -147.7577323695496148 ) ) ;
#11241=CARTESIAN_POINT ( 'NONE',  ( -23.03288344411683752, 33.05775148879286718, -141.7732690776623485 ) ) ;
#11245=SHAPE_DEFINITION_REPRESENTATION ( #12416, #2821 ) ;
#11247=CARTESIAN_POINT ( 'NONE',  ( -29.62827070406144969, 36.92763176543196124, -139.7399851634201582 ) ) ;
#11265=CARTESIAN_POINT ( 'NONE',  ( -13.08363943609140989, 37.92745778430769121, -148.2189490109368535 ) ) ;
#11266=ADVANCED_FACE ( 'NONE', ( #9789 ), #2348, .F. ) ;
#11267=CARTESIAN_POINT ( 'NONE',  ( -16.35051094564224172, 37.08015310165124134, -139.9332297720636973 ) ) ;
#11268=CARTESIAN_POINT ( 'NONE',  ( -29.38682351424920114, 41.54928687793172060, -144.4052646031983898 ) ) ;
#11277=CARTESIAN_POINT ( 'NONE',  ( -21.50444101780000139, 40.78041997809999941, -146.2395182369999986 ) ) ;
#11279=( BOUNDED_CURVE ( )  B_SPLINE_CURVE ( 5, ( #21178, #22960, #13799, #19257, #6644, #2970, #13905, #3200, #10434, #21294, #3091, #23073 ),
 .UNSPECIFIED., .F., .F. ) 
 B_SPLINE_CURVE_WITH_KNOTS ( ( 6, 3, 3, 6 ),
 ( 0.000000000000000000, 4.398006073320000375, 8.633600727160001043, 12.71824907600000110 ),
 .UNSPECIFIED. ) 
 CURVE ( )  GEOMETRIC_REPRESENTATION_ITEM ( )  RATIONAL_B_SPLINE_CURVE ( ( 0.2500000000000000000, 0.2500000000000000000, 0.2500000000000000000, 0.2500000000000000000, 0.2500000000000000000, 0.2500000000000000000, 0.2500000000000000000, 0.2500000000000000000, 0.2500000000000000000, 0.2500000000000000000, 0.2500000000000000000, 0.2500000000000000000 ) ) 
 REPRESENTATION_ITEM ( '' )  );
#11304=CARTESIAN_POINT ( 'NONE',  ( -23.45607911474452933, 41.63247930368797967, -144.6595350281507706 ) ) ;
#11306=CARTESIAN_POINT ( 'NONE',  ( -15.27594358124297536, 35.39499320739097499, -147.3719605119253799 ) ) ;
#11307=CARTESIAN_POINT ( 'NONE',  ( -19.04867772230000256, 35.29145880730000329, -148.2212826610000036 ) ) ;
#11311=CARTESIAN_POINT ( 'NONE',  ( -6.414293125256102179, 40.89447441809702610, -144.3648767483412598 ) ) ;
#11318=CARTESIAN_POINT ( 'NONE',  ( -23.02519999780000148, 33.35976406540000028, -141.9520978260000277 ) ) ;
#11321=CARTESIAN_POINT ( 'NONE',  ( -12.84285234542676690, 33.24967124346566294, -141.9488202108821326 ) ) ;
#11328=CARTESIAN_POINT ( 'NONE',  ( -28.54444076201625435, 32.93521038166499437, -146.4073461492294541 ) ) ;
#11333=CARTESIAN_POINT ( 'NONE',  ( -14.02654126840723592, 33.59767434680839671, -142.2851935300912771 ) ) ;
#11357=CARTESIAN_POINT ( 'NONE',  ( -26.40742642360234882, 40.79449254541880521, -146.2962172200168993 ) ) ;
#11359=CARTESIAN_POINT ( 'NONE',  ( -22.72559961389999827, 32.84666773589999877, -144.4841142160000231 ) ) ;
#11374=CARTESIAN_POINT ( 'NONE',  ( -6.171158540472589493, 35.20721382762360463, -148.0504213054279887 ) ) ;
#11376=CARTESIAN_POINT ( 'NONE',  ( -8.060394343138106876, 38.95025308942626907, -139.6606609314920604 ) ) ;
#11383=CARTESIAN_POINT ( 'NONE',  ( -11.53909816450000037, 41.50279269539999660, -144.7127947380000137 ) ) ;
#11385=CARTESIAN_POINT ( 'NONE',  ( -18.53945141080000170, 39.74065879090000664, -147.6687609889999919 ) ) ;
#11386=CARTESIAN_POINT ( 'NONE',  ( -29.69101630266833425, 40.01133477889813861, -145.8395111173366558 ) ) ;
#11388=CARTESIAN_POINT ( 'NONE',  ( -6.323999170589999608, 34.61896835509999448, -147.3311432729999808 ) ) ;
#11397=CARTESIAN_POINT ( 'NONE',  ( -20.74418227175951657, 39.28578094477872185, -147.3492911867232067 ) ) ;
#11399=CARTESIAN_POINT ( 'NONE',  ( -27.31614846892880166, 35.48399733451186933, -147.3070584612585208 ) ) ;
#11403=CARTESIAN_POINT ( 'NONE',  ( -13.82058007329999860, 36.03909227049999942, -139.5626078809999910 ) ) ;
#11426=CARTESIAN_POINT ( 'NONE',  ( -22.83308877298548012, 39.55027303327759824, -140.7145628016388059 ) ) ;
#11431=CARTESIAN_POINT ( 'NONE',  ( -17.59435718368114721, 36.12650549322601989, -140.0997835545947794 ) ) ;
#11432=EDGE_CURVE ( 'NONE', #10191, #2371, #16171, .T. ) ;
#11437=CARTESIAN_POINT ( 'NONE',  ( -5.376163642574164570, 39.00480445835521692, -141.2592359520692753 ) ) ;
#11441=CARTESIAN_POINT ( 'NONE',  ( -22.76238589975820048, 33.93499072747687251, -142.2605165499471696 ) ) ;
#11454=CARTESIAN_POINT ( 'NONE',  ( -28.10506494415270140, 36.10535006841108441, -148.5541524927092780 ) ) ;
#11457=CARTESIAN_POINT ( 'NONE',  ( -14.14505183392335930, 35.98615714182410130, -139.5052020486566562 ) ) ;
#11467=CARTESIAN_POINT ( 'NONE',  ( -21.11951001670777472, 40.57477398628559939, -141.9750481070400951 ) ) ;
#11481=CARTESIAN_POINT ( 'NONE',  ( -22.60791700490179323, 34.20506515043313556, -140.1155385156617115 ) ) ;
#11490=CARTESIAN_POINT ( 'NONE',  ( -6.033650297970000409, 36.94170754819999303, -147.9652040070000112 ) ) ;
#11491=FACE_OUTER_BOUND ( 'NONE', #14434, .T. ) ;
#11498=CARTESIAN_POINT ( 'NONE',  ( -12.66714788113077894, 37.75265353613255570, -147.6129237411522013 ) ) ;
#11507=CARTESIAN_POINT ( 'NONE',  ( -29.03767587600000155, 36.26045984259999955, -140.5446710220000170 ) ) ;
#11510=CARTESIAN_POINT ( 'NONE',  ( -20.55310894649999653, 37.85259822169999921, -139.7937414779999870 ) ) ;
#11514=CARTESIAN_POINT ( 'NONE',  ( -26.92552552937697996, 36.92880110468703947, -148.2769915172784181 ) ) ;
#11521=CARTESIAN_POINT ( 'NONE',  ( -19.59255166829999695, 37.05126161860000167, -140.3061871179999969 ) ) ;
#11528=CARTESIAN_POINT ( 'NONE',  ( -29.94412816097619867, 41.23953273984808021, -145.7122098475038001 ) ) ;
#11533=CARTESIAN_POINT ( 'NONE',  ( -8.869124888310000898, 38.72872035620000020, -148.0517159070000162 ) ) ;
#11537=CARTESIAN_POINT ( 'NONE',  ( -24.87949572109999963, 37.83967983510000010, -147.8465544160000036 ) ) ;
#11539=CARTESIAN_POINT ( 'NONE',  ( -15.80977837879197878, 32.72809527743532954, -146.2784451626665998 ) ) ;
#11541=CARTESIAN_POINT ( 'NONE',  ( -16.99460745035325004, 35.63018681495184126, -140.8504752325732738 ) ) ;
#11542=CARTESIAN_POINT ( 'NONE',  ( -20.45144833149999997, 36.94873838139999833, -139.8044047869999815 ) ) ;
#11546=CARTESIAN_POINT ( 'NONE',  ( -9.335232969524987823, 34.68189297890224765, -146.9285082157170450 ) ) ;
#11547=CARTESIAN_POINT ( 'NONE',  ( -29.40140556766587920, 40.21055626232655555, -145.9944493861164858 ) ) ;
#11552=CARTESIAN_POINT ( 'NONE',  ( -21.23917607303755872, 35.28761490568743397, -147.7082871199631882 ) ) ;
#11555=CARTESIAN_POINT ( 'NONE',  ( -12.41698512488694028, 36.98746477264878507, -147.4237781434867713 ) ) ;
#11565=CARTESIAN_POINT ( 'NONE',  ( -8.100541861814468447, 36.99062475582145737, -140.7379126119401178 ) ) ;
#11567=CARTESIAN_POINT ( 'NONE',  ( -28.21080904470232653, 35.15062816310292959, -148.3093627672952834 ) ) ;
#11569=CARTESIAN_POINT ( 'NONE',  ( -13.92432874550000044, 37.01165864720000087, -139.5650670249999905 ) ) ;
#11577=CARTESIAN_POINT ( 'NONE',  ( -20.25327657862008479, 40.16659554823041844, -142.3141480157923411 ) ) ;
#11579=CARTESIAN_POINT ( 'NONE',  ( -17.42663577349999926, 38.80963643279999786, -139.8270276149999916 ) ) ;
#11583=CARTESIAN_POINT ( 'NONE',  ( -25.89229443138020414, 34.88584362729995547, -141.2126295570188859 ) ) ;
#11599=CARTESIAN_POINT ( 'NONE',  ( -26.81377270494896337, 41.77330197855063432, -144.5318660586409862 ) ) ;
#11604=CARTESIAN_POINT ( 'NONE',  ( -7.628878236750000319, 37.90286001179999431, -140.0026079769999683 ) ) ;
#11619=( BOUNDED_SURFACE ( )  B_SPLINE_SURFACE ( 5, 5, ( 
 ( #562, #21979, #2356, #11021, #18299, #16852 ),
 ( #18176, #9336, #5669, #20080, #12805, #9114 ),
 ( #3900, #2012, #7795, #5558, #9233, #3661 ),
 ( #15063, #12925, #5448, #16499, #206, #12693 ),
 ( #1891, #16610, #11130, #3779, #7450, #16395 ),
 ( #18406, #2115, #14712, #321, #7682, #19960 ),
 ( #5899, #7564, #2232, #4010, #10897, #7346 ),
 ( #14840, #11357, #5786, #13045, #9452, #20314 ),
 ( #11239, #18511, #16730, #445, #14951, #13155 ),
 ( #18639, #20424, #4118, #6017, #15188, #16964 ),
 ( #22443, #15414, #13505, #675, #22673, #9689 ),
 ( #801, #6368, #19106, #10039, #10163, #18757 ) ),
 .UNSPECIFIED., .F., .F., .F. ) 
 B_SPLINE_SURFACE_WITH_KNOTS ( ( 6, 3, 3, 6 ),
 ( 6, 6 ),
 ( 0.000000000000000000, 4.469553974960000176, 8.969854531369998440, 13.50363095830000049 ),
 ( 1.570796326695754974, 3.141592653590000062 ),
 .UNSPECIFIED. ) 
 GEOMETRIC_REPRESENTATION_ITEM ( )  RATIONAL_B_SPLINE_SURFACE ( (
 ( 0.2500000000000000000, 0.2499999999873634970, 0.2999999999810455398, 0.3999999999747270163, 0.5999999999747269719, 1.000000000000000000),
 ( 0.2500000000000000000, 0.2499999999873634970, 0.2999999999810455398, 0.3999999999747270163, 0.5999999999747269719, 1.000000000000000000),
 ( 0.2500000000000000000, 0.2499999999873634970, 0.2999999999810455398, 0.3999999999747270163, 0.5999999999747269719, 1.000000000000000000),
 ( 0.2500000000000000000, 0.2499999999873634970, 0.2999999999810455398, 0.3999999999747270163, 0.5999999999747269719, 1.000000000000000000),
 ( 0.2500000000000000000, 0.2499999999873634970, 0.2999999999810455398, 0.3999999999747270163, 0.5999999999747269719, 1.000000000000000000),
 ( 0.2500000000000000000, 0.2499999999873634970, 0.2999999999810455398, 0.3999999999747270163, 0.5999999999747269719, 1.000000000000000000),
 ( 0.2500000000000000000, 0.2499999999873634970, 0.2999999999810455398, 0.3999999999747270163, 0.5999999999747269719, 1.000000000000000000),
 ( 0.2500000000000000000, 0.2499999999873634970, 0.2999999999810455398, 0.3999999999747270163, 0.5999999999747269719, 1.000000000000000000),
 ( 0.2500000000000000000, 0.2499999999873634970, 0.2999999999810455398, 0.3999999999747270163, 0.5999999999747269719, 1.000000000000000000),
 ( 0.2500000000000000000, 0.2499999999873634970, 0.2999999999810455398, 0.3999999999747270163, 0.5999999999747269719, 1.000000000000000000),
 ( 0.2500000000000000000, 0.2499999999873634970, 0.2999999999810455398, 0.3999999999747270163, 0.5999999999747269719, 1.000000000000000000),
 ( 0.2500000000000000000, 0.2499999999873634970, 0.2999999999810455398, 0.3999999999747270163, 0.5999999999747269719, 1.000000000000000000) ) ) 
 REPRESENTATION_ITEM ( '' )  SURFACE ( )  );
#11624=CARTESIAN_POINT ( 'NONE',  ( -13.92432874550000044, 37.01165864720000087, -139.5650670249999905 ) ) ;
#11627=CARTESIAN_POINT ( 'NONE',  ( -29.03767587600000155, 36.26045984259999955, -140.5446710220000170 ) ) ;
#11633=CARTESIAN_POINT ( 'NONE',  ( -11.10890527109999937, 34.84141842859999372, -140.9538660569999990 ) ) ;
#11644=CARTESIAN_POINT ( 'NONE',  ( -30.35298369712678124, 40.05084304751723323, -145.7710807886656994 ) ) ;
#11645=CARTESIAN_POINT ( 'NONE',  ( -13.36469768600054131, 37.07845968427642447, -139.9331372610152187 ) ) ;
#11652=CARTESIAN_POINT ( 'NONE',  ( -24.01715389780000010, 40.57582142210000598, -141.9832779239999923 ) ) ;
#11653=CARTESIAN_POINT ( 'NONE',  ( -16.35051094559660001, 37.08015310165674805, -139.9332297721434770 ) ) ;
#11662=CARTESIAN_POINT ( 'NONE',  ( -10.66194399686184013, 33.15920395727439995, -144.2988335297578146 ) ) ;
#11667=CARTESIAN_POINT ( 'NONE',  ( -22.34741274029249425, 33.98766409949738687, -142.2380615103167543 ) ) ;
#11670=EDGE_LOOP ( 'NONE', ( #9283, #20603 ) ) ;
#11671=CARTESIAN_POINT ( 'NONE',  ( -22.78427419138386867, 39.31013640214133176, -141.0476221778322667 ) ) ;
#11679=CARTESIAN_POINT ( 'NONE',  ( -8.150249107171578800, 40.14823067250430455, -142.2562647667796512 ) ) ;
#11682=CARTESIAN_POINT ( 'NONE',  ( -28.54685876571991798, 33.62064205115557058, -146.0221638278284786 ) ) ;
#11684=CARTESIAN_POINT ( 'NONE',  ( -13.69140658673902600, 32.73813017274896708, -141.7795096389974105 ) ) ;
#11686=FACE_OUTER_BOUND ( 'NONE', #11670, .T. ) ;
#11698=CARTESIAN_POINT ( 'NONE',  ( -18.17958360501333459, 40.51113216957658381, -141.8712026623171312 ) ) ;
#11701=CARTESIAN_POINT ( 'NONE',  ( -25.17490547269999723, 35.46855981759999565, -147.6699473629999773 ) ) ;
#11720=ADVANCED_FACE ( 'NONE', ( #22881 ), #21038, .F. ) ;
#11721=CARTESIAN_POINT ( 'NONE',  ( -11.15746551791342256, 40.20079968431886641, -142.3617349190212451 ) ) ;
#11722=CARTESIAN_POINT ( 'NONE',  ( -11.99109128271716607, 36.93662743998936548, -148.3295785880283688 ) ) ;
#11724=CARTESIAN_POINT ( 'NONE',  ( -8.672768080054304107, 41.10012672573470383, -146.4297548272103882 ) ) ;
#11732=CARTESIAN_POINT ( 'NONE',  ( -17.98964812796958057, 38.50830570030355915, -147.4920370692187817 ) ) ;
#11735=CARTESIAN_POINT ( 'NONE',  ( -30.35298369712675637, 40.05084304751726165, -145.7710807886656141 ) ) ;
#11740=ORIENTED_EDGE ( 'NONE', *, *, #4594, .F. ) ;
#11741=CARTESIAN_POINT ( 'NONE',  ( -15.14642988953127123, 40.61711729829275441, -143.6018754827553039 ) ) ;
#11743=CARTESIAN_POINT ( 'NONE',  ( -26.12537298186485302, 35.02184044444919664, -139.7119552129821898 ) ) ;
#11752=EDGE_LOOP ( 'NONE', ( #19633, #12812, #13940, #13486 ) ) ;
#11760=( BOUNDED_CURVE ( )  B_SPLINE_CURVE ( 5, ( #8876, #1655, #14366, #5326, #12690, #7105 ),
 .UNSPECIFIED., .F., .F. ) 
 B_SPLINE_CURVE_WITH_KNOTS ( ( 6, 6 ),
 ( 1.570796326683616906, 3.141592653590000062 ),
 .UNSPECIFIED. ) 
 CURVE ( )  GEOMETRIC_REPRESENTATION_ITEM ( )  RATIONAL_B_SPLINE_CURVE ( ( 0.2499999999999999722, 0.2499999999858182609, 0.2999999999787273941, 0.3999999999716365440, 0.5999999999716365551, 1.000000000000000000 ) ) 
 REPRESENTATION_ITEM ( '' )  );
#11763=CARTESIAN_POINT ( 'NONE',  ( -21.21916986627255852, 36.96385231547830585, -148.6710958206780333 ) ) ;
#11767=ORIENTED_EDGE ( 'NONE', *, *, #741, .T. ) ;
#11776=CARTESIAN_POINT ( 'NONE',  ( -16.82851227082468171, 36.09362984996642609, -139.4602078708371948 ) ) ;
#11778=CARTESIAN_POINT ( 'NONE',  ( -15.90559286389999905, 34.15404988380000617, -147.7469703310000000 ) ) ;
#11779=CARTESIAN_POINT ( 'NONE',  ( -5.647208160064898230, 36.92537127315613787, -140.1716802709670731 ) ) ;
#11791=CARTESIAN_POINT ( 'NONE',  ( -28.14969746246292104, 32.41805236246676003, -143.4814202872532007 ) ) ;
#11794=CARTESIAN_POINT ( 'NONE',  ( -13.36469768600054131, 37.07845968427642447, -139.9331372610152187 ) ) ;
#11795=CARTESIAN_POINT ( 'NONE',  ( -17.22605506639999717, 36.97564272059999979, -139.5994799229999899 ) ) ;
#11799=CARTESIAN_POINT ( 'NONE',  ( -9.429756658493721133, 34.97621497276782065, -148.2829651374544540 ) ) ;
#11808=CARTESIAN_POINT ( 'NONE',  ( -13.64404366343704034, 33.71937897323879696, -142.3027892630092026 ) ) ;
#11809=CARTESIAN_POINT ( 'NONE',  ( -22.52780672249999938, 37.05898997719999954, -140.0074087190000114 ) ) ;
#11814=CARTESIAN_POINT ( 'NONE',  ( -13.92432874550000044, 37.01165864720000087, -139.5650670249999905 ) ) ;
#11821=CARTESIAN_POINT ( 'NONE',  ( -16.91592704275090142, 37.75347730504772414, -140.5160138912785897 ) ) ;
#11824=CARTESIAN_POINT ( 'NONE',  ( -25.36170170592352235, 36.30663503025585470, -140.4342969991932364 ) ) ;
#11838=ORIENTED_EDGE ( 'NONE', *, *, #23033, .F. ) ;
#11843=CARTESIAN_POINT ( 'NONE',  ( -18.28451977759775815, 36.23520409079904425, -147.6763998120985946 ) ) ;
#11844=CARTESIAN_POINT ( 'NONE',  ( -10.69115198329542160, 37.03949207291182688, -140.6562969416297335 ) ) ;
#11847=CARTESIAN_POINT ( 'NONE',  ( -9.072898850179999641, 36.94639249900000522, -148.2684494029999769 ) ) ;
#11851=MECHANICAL_DESIGN_GEOMETRIC_PRESENTATION_REPRESENTATION('',(#18346),#6565);
#11860=CARTESIAN_POINT ( 'NONE',  ( -17.71126569026348108, 40.30718541991128490, -145.9389846959304009 ) ) ;
#11870=CARTESIAN_POINT ( 'NONE',  ( -14.97611052781801533, 40.21187687468054861, -142.1229170966665833 ) ) ;
#11871=CARTESIAN_POINT ( 'NONE',  ( -25.73504040789999792, 33.16200571349999393, -143.7184748760000161 ) ) ;
#11907=CARTESIAN_POINT ( 'NONE',  ( -9.494338074862545440, 36.25121439520489730, -147.3777826702195739 ) ) ;
#11910=CARTESIAN_POINT ( 'NONE',  ( -26.19803085470000070, 35.41001212129999942, -140.6029839040000127 ) ) ;
#11912=( BOUNDED_SURFACE ( )  B_SPLINE_SURFACE ( 5, 5, ( 
 ( #22035, #5723, #20257, #7157, #11181, #14301 ),
 ( #1595, #5497, #21695, #8816, #16092, #23348 ),
 ( #18232, #3710, #7038, #21572, #3478, #5253 ),
 ( #12504, #9165, #19786, #16445, #151, #10716 ),
 ( #1707, #14423, #12630, #19900, #3600, #10826 ),
 ( #18110, #1821, #9039, #16328, #36, #22151 ),
 ( #7965, #4524, #16901, #18805, #5952, #16666 ),
 ( #15001, #13442, #6079, #857, #8086, #11528 ),
 ( #15244, #11644, #7619, #15357, #18571, #22380 ) ),
 .UNSPECIFIED., .F., .F., .F. ) 
 B_SPLINE_SURFACE_WITH_KNOTS ( ( 6, 3, 6 ),
 ( 6, 6 ),
 ( 0.000000000000000000, 5.731822293570000504, 9.005131590149998644 ),
 ( 0.000000000000000000, 1.570796326823719946 ),
 .UNSPECIFIED. ) 
 GEOMETRIC_REPRESENTATION_ITEM ( )  RATIONAL_B_SPLINE_SURFACE ( (
 ( 1.000000000000000000, 0.5999999999926870498, 0.3999999999926869831, 0.2999999999945155427, 0.2499999999963435082, 0.2500000000000000000),
 ( 1.000000000000000000, 0.5999999999926870498, 0.3999999999926869831, 0.2999999999945155427, 0.2499999999963435082, 0.2500000000000000000),
 ( 1.000000000000000000, 0.5999999999926870498, 0.3999999999926869831, 0.2999999999945155427, 0.2499999999963435082, 0.2500000000000000000),
 ( 1.000000000000000000, 0.5999999999926870498, 0.3999999999926869831, 0.2999999999945155427, 0.2499999999963435082, 0.2500000000000000000),
 ( 1.000000000000000000, 0.5999999999926870498, 0.3999999999926869831, 0.2999999999945155427, 0.2499999999963435082, 0.2500000000000000000),
 ( 1.000000000000000000, 0.5999999999926870498, 0.3999999999926869831, 0.2999999999945155427, 0.2499999999963435082, 0.2500000000000000000),
 ( 1.000000000000000000, 0.5999999999926870498, 0.3999999999926869831, 0.2999999999945155427, 0.2499999999963435082, 0.2500000000000000000),
 ( 1.000000000000000000, 0.5999999999926870498, 0.3999999999926869831, 0.2999999999945155427, 0.2499999999963435082, 0.2500000000000000000),
 ( 1.000000000000000000, 0.5999999999926870498, 0.3999999999926869831, 0.2999999999945155427, 0.2499999999963435082, 0.2500000000000000000) ) ) 
 REPRESENTATION_ITEM ( '' )  SURFACE ( )  );
#11914=CARTESIAN_POINT ( 'NONE',  ( -29.48665300989436844, 35.31333379408754780, -140.3895235765232030 ) ) ;
#11918=CARTESIAN_POINT ( 'NONE',  ( -13.62721142606643276, 36.29159090319166836, -140.6168710240230268 ) ) ;
#11921=CARTESIAN_POINT ( 'NONE',  ( -15.07147389515269431, 36.94622240755793996, -147.6034838243276681 ) ) ;
#11923=CARTESIAN_POINT ( 'NONE',  ( -9.834719431799998191, 32.58365614919999587, -144.2353630830000100 ) ) ;
#11925=CARTESIAN_POINT ( 'NONE',  ( -8.380324466120532279, 38.99863161821663482, -141.2713831690983568 ) ) ;
#11930=CARTESIAN_POINT ( 'NONE',  ( -7.706057744118020025, 32.88414932266176294, -144.6585917708909790 ) ) ;
#11931=CARTESIAN_POINT ( 'NONE',  ( -25.95437585259999835, 39.65968214939999825, -140.4458241780000094 ) ) ;
#11939=CARTESIAN_POINT ( 'NONE',  ( -17.10091063371594089, 39.14571640553532461, -141.0837638240496119 ) ) ;
#11943=CARTESIAN_POINT ( 'NONE',  ( -24.68545039255907625, 32.95552305825756889, -143.5792614360848347 ) ) ;
#11946=CARTESIAN_POINT ( 'NONE',  ( -11.48759298120159933, 37.74537190000896203, -140.3874188151567921 ) ) ;
#11963=CARTESIAN_POINT ( 'NONE',  ( -10.62000911041278783, 38.66961726526942300, -140.5822234582898886 ) ) ;
#11967=CARTESIAN_POINT ( 'NONE',  ( -9.771488485039439453, 38.65068379608815974, -147.6127673910835938 ) ) ;
#11973=ADVANCED_FACE ( 'NONE', ( #22272 ), #23460, .F. ) ;
#11975=EDGE_LOOP ( 'NONE', ( #2586, #18078, #5546, #13182 ) ) ;
#11977=CARTESIAN_POINT ( 'NONE',  ( -23.51619327739999932, 36.94101002280000046, -140.1031831869999849 ) ) ;
#11981=ORIENTED_EDGE ( 'NONE', *, *, #19279, .T. ) ;
#11986=CARTESIAN_POINT ( 'NONE',  ( -24.57863953938383972, 33.12365566000271855, -146.2648171788414118 ) ) ;
#12009=CARTESIAN_POINT ( 'NONE',  ( -14.40871421779729111, 40.88007763208802459, -146.3531009209950469 ) ) ;
#12020=CARTESIAN_POINT ( 'NONE',  ( -16.25499370519659692, 36.25618878915210530, -139.9176275600604242 ) ) ;
#12025=CARTESIAN_POINT ( 'NONE',  ( -9.141321705204468628, 35.20952963915718215, -147.7046101278156129 ) ) ;
#12035=CARTESIAN_POINT ( 'NONE',  ( -23.49616868971058281, 39.04951233234732655, -141.2607385382614495 ) ) ;
#12040=CARTESIAN_POINT ( 'NONE',  ( -6.033650297970000409, 36.94170754819999303, -147.9652040070000112 ) ) ;
#12047=CARTESIAN_POINT ( 'NONE',  ( -21.21916986627257273, 36.96385231547829164, -148.6710958206780617 ) ) ;
#12049=CARTESIAN_POINT ( 'NONE',  ( -7.427142538590000065, 36.18616221519999954, -139.9783837409999876 ) ) ;
#12057=CARTESIAN_POINT ( 'NONE',  ( -20.92934595191639957, 38.39978090212863293, -147.3875924135098217 ) ) ;
#12059=CARTESIAN_POINT ( 'NONE',  ( -17.53569647173340229, 40.68917497052807875, -144.4123951040356246 ) ) ;
#12064=CARTESIAN_POINT ( 'NONE',  ( -24.26662447760775976, 35.20109951628700173, -148.0073960933498256 ) ) ;
#12074=ORIENTED_EDGE ( 'NONE', *, *, #4059, .F. ) ;
#12076=CARTESIAN_POINT ( 'NONE',  ( -28.67645553090000021, 33.79622934780000065, -142.1760638819999940 ) ) ;
#12081=CARTESIAN_POINT ( 'NONE',  ( -19.24427237058737106, 36.32221599350456387, -147.8366771256798131 ) ) ;
#12084=CARTESIAN_POINT ( 'NONE',  ( -12.02450515616398086, 36.94061592733338983, -147.5849826168277730 ) ) ;
#12086=CARTESIAN_POINT ( 'NONE',  ( -10.03947840059807817, 37.95006096691596298, -148.1887910594758750 ) ) ;
#12088=CARTESIAN_POINT ( 'NONE',  ( -28.03429568389999815, 32.40695676820000415, -144.4586890250000124 ) ) ;
#12104=CARTESIAN_POINT ( 'NONE',  ( -15.13725729890880878, 41.64066907640037130, -144.4902128453323655 ) ) ;
#12105=CARTESIAN_POINT ( 'NONE',  ( -25.19866427022423494, 35.19115820926130311, -148.3071468095327816 ) ) ;
#12123=CARTESIAN_POINT ( 'NONE',  ( -21.93648690847361138, 37.04947573026748131, -148.4875734863013008 ) ) ;
#12124=CARTESIAN_POINT ( 'NONE',  ( -13.66607852796262357, 39.56920417019204450, -140.6329893835133475 ) ) ;
#12126=ORIENTED_EDGE ( 'NONE', *, *, #9010, .F. ) ;
#12138=CARTESIAN_POINT ( 'NONE',  ( -16.20147620265711907, 33.40528963980359833, -143.4816615022452027 ) ) ;
#12142=CARTESIAN_POINT ( 'NONE',  ( -5.459597139290000456, 36.94776568910000236, -139.8191173760000083 ) ) ;
#12143=CARTESIAN_POINT ( 'NONE',  ( -7.706057744120000663, 32.88414932280000613, -144.6585917709999762 ) ) ;
#12144=CARTESIAN_POINT ( 'NONE',  ( 7.935413903360000631, 38.54667735430000164, -117.9621819409999972 ) ) ;
#12148=ORIENTED_EDGE ( 'NONE', *, *, #3436, .T. ) ;
#12153=CARTESIAN_POINT ( 'NONE',  ( -29.26469713025206687, 35.46669211296976698, -140.6743228978359923 ) ) ;
#12157=CARTESIAN_POINT ( 'NONE',  ( -24.05878554920779777, 40.01929703906174751, -145.8416302223327818 ) ) ;
#12162=CARTESIAN_POINT ( 'NONE',  ( -10.47418533528157880, 33.50012463732112167, -145.9259304110134110 ) ) ;
#12165=CARTESIAN_POINT ( 'NONE',  ( -9.389499115902607329, 36.98418387199379254, -147.3811924090304046 ) ) ;
#12173=CARTESIAN_POINT ( 'NONE',  ( -7.107905118343079920, 36.22301459074771657, -148.1570340891202022 ) ) ;
#12187=CARTESIAN_POINT ( 'NONE',  ( -16.13502618060000060, 32.80445174449999968, -146.2787800969999807 ) ) ;
#12194=( BOUNDED_SURFACE ( )  B_SPLINE_SURFACE ( 5, 5, ( 
 ( #14377, #18306, #3788, #21882, #11030, #10549 ),
 ( #17830, #3557, #12701, #7241, #8770, #5341 ),
 ( #1551, #16048, #10784, #21769, #12583, #19858 ),
 ( #16167, #9001, #3435, #23307, #7000, #14261 ),
 ( #114, #5456, #21526, #12460, #19968, #10670 ),
 ( #1666, #10904, #3670, #1899, #9124, #17953 ),
 ( #8888, #21988, #22333, #16741, #11599, #22452 ),
 ( #686, #18874, #18764, #5678, #20433, #6025 ),
 ( #2123, #22220, #7916, #20669, #14850, #3907 ),
 ( #9345, #22106, #4362, #5910, #2587, #13399 ),
 ( #454, #5794, #13279, #15195, #2475, #6148 ),
 ( #15073, #13054, #9814, #18521, #4251, #16859 ) ),
 .UNSPECIFIED., .F., .F., .F. ) 
 B_SPLINE_SURFACE_WITH_KNOTS ( ( 6, 3, 3, 6 ),
 ( 6, 6 ),
 ( 0.000000000000000000, 4.469553974960000176, 8.969854531369998440, 13.50363095830000049 ),
 ( 0.000000000000000000, 1.570796327036555029 ),
 .UNSPECIFIED. ) 
 GEOMETRIC_REPRESENTATION_ITEM ( )  RATIONAL_B_SPLINE_SURFACE ( (
 ( 1.000000000000000000, 0.5999999999384889593, 0.3999999999384890037, 0.2999999999538665030, 0.2499999999692444907, 0.2500000000000000000),
 ( 1.000000000000000000, 0.5999999999384889593, 0.3999999999384890037, 0.2999999999538665030, 0.2499999999692444907, 0.2500000000000000000),
 ( 1.000000000000000000, 0.5999999999384889593, 0.3999999999384890037, 0.2999999999538665030, 0.2499999999692444907, 0.2500000000000000000),
 ( 1.000000000000000000, 0.5999999999384889593, 0.3999999999384890037, 0.2999999999538665030, 0.2499999999692444907, 0.2500000000000000000),
 ( 1.000000000000000000, 0.5999999999384889593, 0.3999999999384890037, 0.2999999999538665030, 0.2499999999692444907, 0.2500000000000000000),
 ( 1.000000000000000000, 0.5999999999384889593, 0.3999999999384890037, 0.2999999999538665030, 0.2499999999692444907, 0.2500000000000000000),
 ( 1.000000000000000000, 0.5999999999384889593, 0.3999999999384890037, 0.2999999999538665030, 0.2499999999692444907, 0.2500000000000000000),
 ( 1.000000000000000000, 0.5999999999384889593, 0.3999999999384890037, 0.2999999999538665030, 0.2499999999692444907, 0.2500000000000000000),
 ( 1.000000000000000000, 0.5999999999384889593, 0.3999999999384890037, 0.2999999999538665030, 0.2499999999692444907, 0.2500000000000000000),
 ( 1.000000000000000000, 0.5999999999384889593, 0.3999999999384890037, 0.2999999999538665030, 0.2499999999692444907, 0.2500000000000000000),
 ( 1.000000000000000000, 0.5999999999384889593, 0.3999999999384890037, 0.2999999999538665030, 0.2499999999692444907, 0.2500000000000000000),
 ( 1.000000000000000000, 0.5999999999384889593, 0.3999999999384890037, 0.2999999999538665030, 0.2499999999692444907, 0.2500000000000000000) ) ) 
 REPRESENTATION_ITEM ( '' )  SURFACE ( )  );
#12199=CARTESIAN_POINT ( 'NONE',  ( -28.53262905876626121, 34.95472962840860021, -141.1599551600052109 ) ) ;
#12206=CARTESIAN_POINT ( 'NONE',  ( -18.18930989820000121, 36.96028804430000037, -147.6841622079999752 ) ) ;
#12209=CARTESIAN_POINT ( 'NONE',  ( -6.932379827013399165, 32.27029367454267827, -144.6524339332874263 ) ) ;
#12221=CARTESIAN_POINT ( 'NONE',  ( -20.84101097270000125, 38.55092845019999714, -147.7610021339999946 ) ) ;
#12226=EDGE_LOOP ( 'NONE', ( #17923, #16083, #15944, #11740 ) ) ;
#12227=CARTESIAN_POINT ( 'NONE',  ( -15.26331651089999930, 39.75437292659999855, -147.8043400740000095 ) ) ;
#12243=CARTESIAN_POINT ( 'NONE',  ( -14.45813593939999997, 41.09907220950000095, -141.6721478100000127 ) ) ;
#12244=FACE_OUTER_BOUND ( 'NONE', #11975, .T. ) ;
#12259=ADVANCED_FACE ( 'NONE', ( #7721 ), #4766, .F. ) ;
#12261=CARTESIAN_POINT ( 'NONE',  ( -7.010349701930000066, 37.05829245179999987, -148.1453878979999956 ) ) ;
#12277=FACE_OUTER_BOUND ( 'NONE', #20806, .T. ) ;
#12287=CARTESIAN_POINT ( 'NONE',  ( -7.998490025638652412, 36.27838346975144646, -140.7398725790258993 ) ) ;
#12288=CARTESIAN_POINT ( 'NONE',  ( -22.83308877300000006, 39.55027303330000166, -140.7145628009999996 ) ) ;
#12315=ORIENTED_EDGE ( 'NONE', *, *, #3948, .T. ) ;
#12321=CARTESIAN_POINT ( 'NONE',  ( -6.697834181631886707, 32.57753539646190433, -144.5849521621801443 ) ) ;
#12327=ORIENTED_EDGE ( 'NONE', *, *, #7015, .T. ) ;
#12336=CARTESIAN_POINT ( 'NONE',  ( -15.36992937847549001, 41.12890580218349612, -146.3724425043323834 ) ) ;
#12354=CARTESIAN_POINT ( 'NONE',  ( -14.60410653414054316, 40.19715529047051916, -145.9374667791834099 ) ) ;
#12360=CARTESIAN_POINT ( 'NONE',  ( -28.52142019844059107, 37.05975231236454448, -139.6605181376032476 ) ) ;
#12369=CARTESIAN_POINT ( 'NONE',  ( -6.565507373470476082, 37.00519331014221081, -148.7410818962694066 ) ) ;
#12375=CARTESIAN_POINT ( 'NONE',  ( -12.28014746100000032, 36.97113097969999984, -148.4919582129999753 ) ) ;
#12383=CARTESIAN_POINT ( 'NONE',  ( -24.97797643630000053, 37.05442817780000553, -147.8575004449999994 ) ) ;
#12412=CARTESIAN_POINT ( 'NONE',  ( -17.22605506639999717, 36.97564272059999979, -139.5994799229999899 ) ) ;
#12416=PRODUCT_DEFINITION_SHAPE ( 'NONE', 'NONE',  #20119 ) ;
#12421=ADVANCED_FACE ( 'NONE', ( #5763 ), #7196, .F. ) ;
#12424=CARTESIAN_POINT ( 'NONE',  ( -28.32042446336400232, 35.24116700710558092, -139.8750711406415235 ) ) ;
#12425=ORIENTED_EDGE ( 'NONE', *, *, #20029, .F. ) ;
#12432=CARTESIAN_POINT ( 'NONE',  ( -18.82091118356679971, 33.23810407333031947, -144.5979112941420226 ) ) ;
#12434=CARTESIAN_POINT ( 'NONE',  ( -11.89394129276558232, 37.80475929424586923, -148.3421129316571125 ) ) ;
#12436=ORIENTED_EDGE ( 'NONE', *, *, #1474, .F. ) ;
#12438=VERTEX_POINT ( 'NONE', #13133 ) ;
#12447=ADVANCED_FACE ( 'NONE', ( #20404 ), #9613, .F. ) ;
#12452=CARTESIAN_POINT ( 'NONE',  ( -10.86836323999999898, 38.91206754959999614, -139.9811931129999891 ) ) ;
#12454=CARTESIAN_POINT ( 'NONE',  ( -15.65026171697591018, 40.90570753890175837, -146.2089035856170369 ) ) ;
#12456=CARTESIAN_POINT ( 'NONE',  ( -29.25462571399999590, 37.92445966660000778, -140.5403777589999947 ) ) ;
#12460=CARTESIAN_POINT ( 'NONE',  ( -26.87389185232229138, 41.15523227550784924, -141.5790970697422892 ) ) ;
#12472=FACE_OUTER_BOUND ( 'NONE', #2599, .T. ) ;
#12473=CARTESIAN_POINT ( 'NONE',  ( -13.46422577752552563, 37.93715959768575630, -139.9491268735157519 ) ) ;
#12474=CARTESIAN_POINT ( 'NONE',  ( -28.65584425188693984, 38.23101052054714444, -139.6673458017931750 ) ) ;
#12492=CARTESIAN_POINT ( 'NONE',  ( -8.309953467249998837, 35.25464643879999471, -140.3668538350000006 ) ) ;
#12503=CARTESIAN_POINT ( 'NONE',  ( -23.81040386161897260, 37.71789450755535711, -147.9004385756058753 ) ) ;
#12504=CARTESIAN_POINT ( 'NONE',  ( -29.47785954729999958, 39.65718555499999809, -141.4786507110000287 ) ) ;
#12509=CARTESIAN_POINT ( 'NONE',  ( -11.56119896032659256, 36.14006801961227922, -140.1188298284611449 ) ) ;
#12510=CARTESIAN_POINT ( 'NONE',  ( -18.64329452426891365, 32.49620444683537102, -144.6932856329320884 ) ) ;
#12511=CARTESIAN_POINT ( 'NONE',  ( -9.105481712864866850, 39.02735606833573456, -146.8299818849519340 ) ) ;
#12533=CARTESIAN_POINT ( 'NONE',  ( -25.80099178304864793, 37.02638091262011955, -140.6905788942592608 ) ) ;
#12545=CARTESIAN_POINT ( 'NONE',  ( -16.36776575232984143, 35.42538575923208555, -147.6161688091087569 ) ) ;
#12546=CARTESIAN_POINT ( 'NONE',  ( -13.20713333982466509, 36.31039189040361492, -147.8273893801373902 ) ) ;
#12549=EDGE_LOOP ( 'NONE', ( #4005, #6993, #7685, #5347 ) ) ;
#12552=CARTESIAN_POINT ( 'NONE',  ( -20.00879305376257022, 35.51518944883265760, -140.9236936935650135 ) ) ;
#12575=CARTESIAN_POINT ( 'NONE',  ( -11.42599417689999974, 41.52668172479999953, -143.7505393120000292 ) ) ;
#12583=CARTESIAN_POINT ( 'NONE',  ( -26.11358249223754413, 38.93857572900594022, -139.6801797896497703 ) ) ;
#12602=CARTESIAN_POINT ( 'NONE',  ( -16.86519360499094233, 39.73476227100517377, -140.3032793073522555 ) ) ;
#12611=ORIENTED_EDGE ( 'NONE', *, *, #8513, .T. ) ;
#12617=CARTESIAN_POINT ( 'NONE',  ( -6.288682382039059604, 41.28368337079415085, -144.4167712528175969 ) ) ;
#12619=VERTEX_POINT ( 'NONE', #2647 ) ;
#12620=CARTESIAN_POINT ( 'NONE',  ( -27.48801997220000004, 39.21796412529999998, -147.0196846460000017 ) ) ;
#12625=COLOUR_RGB ( '', 0.09019608, 0.27058824, 0.51372549) ;
#12629=CARTESIAN_POINT ( 'NONE',  ( -23.82650726623105086, 39.03244537584987484, -146.9745935326799895 ) ) ;
#12630=CARTESIAN_POINT ( 'NONE',  ( -30.24492469408960105, 40.76033517006445805, -142.6215232399929960 ) ) ;
#12634=CARTESIAN_POINT ( 'NONE',  ( -10.74201573257056630, 32.87128505482456120, -141.4462505804974057 ) ) ;
#12635=CARTESIAN_POINT ( 'NONE',  ( -19.59223779464246817, 34.04810666035614730, -140.2228890206432652 ) ) ;
#12636=CARTESIAN_POINT ( 'NONE',  ( -8.971913342289999704, 37.83624783359999810, -148.2794752869999968 ) ) ;
#12641=ORIENTED_EDGE ( 'NONE', *, *, #8433, .F. ) ;
#12642=CARTESIAN_POINT ( 'NONE',  ( -8.462973826026347623, 36.94736262684725858, -140.5165674475847766 ) ) ;
#12643=CARTESIAN_POINT ( 'NONE',  ( -23.86695901000000219, 38.68196870779999585, -148.0474502900000005 ) ) ;
#12655=EDGE_CURVE ( 'NONE', #7237, #12619, #6580, .T. ) ;
#12656=CARTESIAN_POINT ( 'NONE',  ( -23.51619327739999932, 36.94101002280000046, -140.1031831869999849 ) ) ;
#12668=CARTESIAN_POINT ( 'NONE',  ( -15.57039528521051963, 36.22627288621195873, -147.5570433397655847 ) ) ;
#12669=CARTESIAN_POINT ( 'NONE',  ( -13.39436545728456451, 34.84914659774037204, -147.2640033608687702 ) ) ;
#12676=CARTESIAN_POINT ( 'NONE',  ( -12.02450515625771210, 36.94061592734458088, -147.5849826166100627 ) ) ;
#12683=( BOUNDED_SURFACE ( )  B_SPLINE_SURFACE ( 5, 5, ( 
 ( #3452, #10685, #17966, #1679, #19873, #3568 ),
 ( #11946, #1155, #2142, #19214, #22123, #2379 ),
 ( #7589, #22469, #22006, #22348, #4146, #15086 ),
 ( #18428, #16634, #469, #10156, #5692, #4705 ),
 ( #7706, #20451, #14863, #9480, #17428, #11154 ),
 ( #8388, #16756, #21013, #3921, #22233, #18775 ),
 ( #13750, #15214, #2924, #20567, #9599, #11383 ),
 ( #9709, #6045, #5809, #582, #18666, #12951 ),
 ( #16873, #9362, #20228, #7818, #347, #14972 ),
 ( #13177, #13066, #13296, #4268, #20338, #4031 ),
 ( #11498, #2488, #11265, #18538, #2256, #16985 ),
 ( #699, #7931, #6491, #5923, #23029, #8847 ) ),
 .UNSPECIFIED., .F., .F., .F. ) 
 B_SPLINE_SURFACE_WITH_KNOTS ( ( 6, 3, 3, 6 ),
 ( 6, 6 ),
 ( 0.000000000000000000, 4.398006073320000375, 8.633600727160001043, 12.71824907600000110 ),
 ( 1.570796326630355066, 3.141592653590000062 ),
 .UNSPECIFIED. ) 
 GEOMETRIC_REPRESENTATION_ITEM ( )  RATIONAL_B_SPLINE_SURFACE ( (
 ( 0.2500000000000000000, 0.2499999999790369909, 0.2999999999685555307, 0.3999999999580740040, 0.5999999999580739596, 1.000000000000000000),
 ( 0.2500000000000000000, 0.2499999999790369909, 0.2999999999685555307, 0.3999999999580740040, 0.5999999999580739596, 1.000000000000000000),
 ( 0.2500000000000000000, 0.2499999999790369909, 0.2999999999685555307, 0.3999999999580740040, 0.5999999999580739596, 1.000000000000000000),
 ( 0.2500000000000000000, 0.2499999999790369909, 0.2999999999685555307, 0.3999999999580740040, 0.5999999999580739596, 1.000000000000000000),
 ( 0.2500000000000000000, 0.2499999999790369909, 0.2999999999685555307, 0.3999999999580740040, 0.5999999999580739596, 1.000000000000000000),
 ( 0.2500000000000000000, 0.2499999999790369909, 0.2999999999685555307, 0.3999999999580740040, 0.5999999999580739596, 1.000000000000000000),
 ( 0.2500000000000000000, 0.2499999999790369909, 0.2999999999685555307, 0.3999999999580740040, 0.5999999999580739596, 1.000000000000000000),
 ( 0.2500000000000000000, 0.2499999999790369909, 0.2999999999685555307, 0.3999999999580740040, 0.5999999999580739596, 1.000000000000000000),
 ( 0.2500000000000000000, 0.2499999999790369909, 0.2999999999685555307, 0.3999999999580740040, 0.5999999999580739596, 1.000000000000000000),
 ( 0.2500000000000000000, 0.2499999999790369909, 0.2999999999685555307, 0.3999999999580740040, 0.5999999999580739596, 1.000000000000000000),
 ( 0.2500000000000000000, 0.2499999999790369909, 0.2999999999685555307, 0.3999999999580740040, 0.5999999999580739596, 1.000000000000000000),
 ( 0.2500000000000000000, 0.2499999999790369909, 0.2999999999685555307, 0.3999999999580740040, 0.5999999999580739596, 1.000000000000000000) ) ) 
 REPRESENTATION_ITEM ( '' )  SURFACE ( )  );
#12690=CARTESIAN_POINT ( 'NONE',  ( -19.10036853996236772, 37.06903765908678849, -148.2030617969735715 ) ) ;
#12693=CARTESIAN_POINT ( 'NONE',  ( -26.68542098469999857, 39.18140699330000132, -140.9632721460000084 ) ) ;
#12696=CARTESIAN_POINT ( 'NONE',  ( -15.76067864000701668, 37.76810578663741325, -147.5051738567275379 ) ) ;
#12701=CARTESIAN_POINT ( 'NONE',  ( -26.71657219920165005, 37.82487237221160825, -139.7343082328227410 ) ) ;
#12705=CARTESIAN_POINT ( 'NONE',  ( -10.92974397189781222, 35.65249901646877362, -140.8582538894084735 ) ) ;
#12715=CARTESIAN_POINT ( 'NONE',  ( -17.45987344088444360, 41.16328378089777829, -141.5750803238402398 ) ) ;
#12717=ORIENTED_EDGE ( 'NONE', *, *, #195, .T. ) ;
#12719=CARTESIAN_POINT ( 'NONE',  ( -25.64792992860000354, 37.04465132570000208, -139.7265440090000084 ) ) ;
#12731=CARTESIAN_POINT ( 'NONE',  ( -5.664837119873038951, 39.54185838768819394, -147.6076384376017927 ) ) ;
#12742=CARTESIAN_POINT ( 'NONE',  ( -23.91604154053268161, 38.38020865605560772, -147.3412701355220520 ) ) ;
#12747=CARTESIAN_POINT ( 'NONE',  ( -11.16897700298565077, 36.05264020273449432, -139.4334584778495412 ) ) ;
#12749=CARTESIAN_POINT ( 'NONE',  ( -19.54668701385130447, 37.05673630843254784, -139.5622637237151196 ) ) ;
#12755=EDGE_CURVE ( 'NONE', #16477, #598, #14509, .T. ) ;
#12759=ORIENTED_EDGE ( 'NONE', *, *, #387, .T. ) ;
#12760=CARTESIAN_POINT ( 'NONE',  ( -5.733381482170000432, 39.34803470290000149, -147.3316303149999840 ) ) ;
#12769=CARTESIAN_POINT ( 'NONE',  ( -25.09512484594771209, 36.12507003254601301, -148.5419237647928981 ) ) ;
#12783=CARTESIAN_POINT ( 'NONE',  ( -16.33553080621575404, 33.80379307428399471, -145.7770475876280329 ) ) ;
#12789=CARTESIAN_POINT ( 'NONE',  ( -19.57725164000000007, 32.58775676329999271, -144.7853266960000269 ) ) ;
#12805=CARTESIAN_POINT ( 'NONE',  ( -26.27746988921043680, 37.69287412588059993, -140.6313975853602756 ) ) ;
#12808=CARTESIAN_POINT ( 'NONE',  ( -21.53618355987887867, 33.35162261426351904, -146.0341402268610125 ) ) ;
#12809=MECHANICAL_DESIGN_GEOMETRIC_PRESENTATION_REPRESENTATION('',(#18141),#4461);
#12812=ORIENTED_EDGE ( 'NONE', *, *, #8504, .T. ) ;
#12819=( BOUNDED_CURVE ( )  B_SPLINE_CURVE ( 5, ( #11809, #15861, #18012, #12288, #5147, #3494, #21711, #8705, #19801, #12643, #6941, #3614 ),
 .UNSPECIFIED., .F., .F. ) 
 B_SPLINE_CURVE_WITH_KNOTS ( ( 6, 3, 3, 6 ),
 ( 0.000000000000000000, 4.509114667229999540, 8.972055907920001516, 13.39149027789999913 ),
 .UNSPECIFIED. ) 
 CURVE ( )  GEOMETRIC_REPRESENTATION_ITEM ( )  RATIONAL_B_SPLINE_CURVE ( ( 0.2500000000000000000, 0.2500000000000000000, 0.2500000000000000000, 0.2500000000000000000, 0.2500000000000000000, 0.2500000000000000000, 0.2500000000000000000, 0.2500000000000000000, 0.2500000000000000000, 0.2500000000000000000, 0.2500000000000000000, 0.2500000000000000000 ) ) 
 REPRESENTATION_ITEM ( '' )  );
#12823=CARTESIAN_POINT ( 'NONE',  ( -14.01657753870000001, 36.22806874879999839, -140.5479840249999768 ) ) ;
#12831=CARTESIAN_POINT ( 'NONE',  ( -17.08670351461686820, 41.11123597602360746, -141.6546470616082161 ) ) ;
#12832=CARTESIAN_POINT ( 'NONE',  ( -29.47785954729999958, 39.65718555499999809, -141.4786507110000287 ) ) ;
#12836=CARTESIAN_POINT ( 'NONE',  ( -17.75130813170000366, 41.00325609940000504, -141.6328284839999867 ) ) ;
#12840=CARTESIAN_POINT ( 'NONE',  ( -27.40802390352900630, 34.81902089894730778, -146.9145522347566839 ) ) ;
#12845=CARTESIAN_POINT ( 'NONE',  ( -6.732165765376294075, 38.94235323983919272, -148.2714551560809753 ) ) ;
#12863=( NAMED_UNIT ( * ) SI_UNIT ( $, .STERADIAN. ) SOLID_ANGLE_UNIT ( ) );
#12864=CARTESIAN_POINT ( 'NONE',  ( -19.57725164000000007, 32.58775676329999271, -144.7853266960000269 ) ) ;
#12865=ADVANCED_FACE ( 'NONE', ( #17627 ), #16922, .F. ) ;
#12877=CARTESIAN_POINT ( 'NONE',  ( -6.981168498894938956, 37.84839353770540527, -147.7381749008708312 ) ) ;
#12886=CARTESIAN_POINT ( 'NONE',  ( -12.28014746100000032, 36.97113097969999984, -148.4919582129999753 ) ) ;
#12902=CARTESIAN_POINT ( 'NONE',  ( -13.18072986969131932, 37.07863008620352474, -148.2345011165226651 ) ) ;
#12907=CARTESIAN_POINT ( 'NONE',  ( -20.10082943595380911, 33.21594955552029660, -142.1386041078769154 ) ) ;
#12910=CARTESIAN_POINT ( 'NONE',  ( -20.54812748657687038, 36.93719815735425271, -140.4704715740689949 ) ) ;
#12919=CARTESIAN_POINT ( 'NONE',  ( -24.06602356369428009, 36.94557182216776425, -148.2530914611035939 ) ) ;
#12925=CARTESIAN_POINT ( 'NONE',  ( -25.68538705770549058, 39.50692289490424258, -140.7105351162441877 ) ) ;
#12927=CARTESIAN_POINT ( 'NONE',  ( -22.81311670109966272, 32.52853389434195464, -143.5568795629989722 ) ) ;
#12929=CARTESIAN_POINT ( 'NONE',  ( -29.82391180389999619, 40.55477172079999804, -144.2881336360000262 ) ) ;
#12936=CARTESIAN_POINT ( 'NONE',  ( -7.506111428109999650, 33.37436714639999735, -146.3147224710000387 ) ) ;
#12939=CARTESIAN_POINT ( 'NONE',  ( -10.13972653286922565, 34.91672950339960835, -140.8637739126610313 ) ) ;
#12951=CARTESIAN_POINT ( 'NONE',  ( -11.76172848620000089, 40.95326072219999958, -146.5101368410000191 ) ) ;
#12952=CARTESIAN_POINT ( 'NONE',  ( -17.43685409200564251, 41.68787803771047606, -144.5118622863669202 ) ) ;
#12961=CARTESIAN_POINT ( 'NONE',  ( -20.09055976259235266, 41.19265711152617371, -141.7594002370568944 ) ) ;
#12963=( BOUNDED_SURFACE ( )  B_SPLINE_SURFACE ( 5, 5, ( 
 ( #6377, #4604, #15543, #1170, #21264, #8400 ),
 ( #11843, #2818, #6616, #12081, #19355, #10049 ),
 ( #22809, #6505, #13770, #21030, #10174, #19227 ),
 ( #15673, #7328, #10878, #5304, #18282, #8742 ),
 ( #14696, #3401, #3529, #5182, #18157, #20061 ),
 ( #12432, #16020, #1870, #1996, #16485, #12789 ),
 ( #5651, #14589, #11002, #3644, #20188, #9092 ),
 ( #191, #14473, #6972, #8862, #12907, #3759 ),
 ( #14237, #21857, #84, #23282, #16378, #5541 ),
 ( #9215, #19707, #12552, #7434, #21965, #16141 ),
 ( #3883, #14348, #11117, #23395, #18389, #21501 ),
 ( #10642, #17925, #1641, #7091, #18042, #19943 ) ),
 .UNSPECIFIED., .F., .F., .F. ) 
 B_SPLINE_SURFACE_WITH_KNOTS ( ( 6, 3, 3, 6 ),
 ( 6, 6 ),
 ( 0.000000000000000000, 4.059123295939999210, 8.340116530639999581, 12.86134770560000007 ),
 ( 1.570796326526080033, 3.141592653590000062 ),
 .UNSPECIFIED. ) 
 GEOMETRIC_REPRESENTATION_ITEM ( )  RATIONAL_B_SPLINE_SURFACE ( (
 ( 0.2500000000000000000, 0.2499999999657600003, 0.2999999999486395175, 0.3999999999315194676, 0.5999999999315199783, 1.000000000000000000),
 ( 0.2500000000000000000, 0.2499999999657600003, 0.2999999999486395175, 0.3999999999315194676, 0.5999999999315199783, 1.000000000000000000),
 ( 0.2500000000000000000, 0.2499999999657600003, 0.2999999999486395175, 0.3999999999315194676, 0.5999999999315199783, 1.000000000000000000),
 ( 0.2500000000000000000, 0.2499999999657600003, 0.2999999999486395175, 0.3999999999315194676, 0.5999999999315199783, 1.000000000000000000),
 ( 0.2500000000000000000, 0.2499999999657600003, 0.2999999999486395175, 0.3999999999315194676, 0.5999999999315199783, 1.000000000000000000),
 ( 0.2500000000000000000, 0.2499999999657600003, 0.2999999999486395175, 0.3999999999315194676, 0.5999999999315199783, 1.000000000000000000),
 ( 0.2500000000000000000, 0.2499999999657600003, 0.2999999999486395175, 0.3999999999315194676, 0.5999999999315199783, 1.000000000000000000),
 ( 0.2500000000000000000, 0.2499999999657600003, 0.2999999999486395175, 0.3999999999315194676, 0.5999999999315199783, 1.000000000000000000),
 ( 0.2500000000000000000, 0.2499999999657600003, 0.2999999999486395175, 0.3999999999315194676, 0.5999999999315199783, 1.000000000000000000),
 ( 0.2500000000000000000, 0.2499999999657600003, 0.2999999999486395175, 0.3999999999315194676, 0.5999999999315199783, 1.000000000000000000),
 ( 0.2500000000000000000, 0.2499999999657600003, 0.2999999999486395175, 0.3999999999315194676, 0.5999999999315199783, 1.000000000000000000),
 ( 0.2500000000000000000, 0.2499999999657600003, 0.2999999999486395175, 0.3999999999315194676, 0.5999999999315199783, 1.000000000000000000) ) ) 
 REPRESENTATION_ITEM ( '' )  SURFACE ( )  );
#12964=CARTESIAN_POINT ( 'NONE',  ( -27.13030197561320733, 35.14114750801761033, -148.0149677930219525 ) ) ;
#12966=CARTESIAN_POINT ( 'NONE',  ( -12.28014746100000032, 36.97113097969999984, -148.4919582129999753 ) ) ;
#12969=CARTESIAN_POINT ( 'NONE',  ( -11.38486064709999823, 36.95668670079999885, -140.3965526140000009 ) ) ;
#12987=CARTESIAN_POINT ( 'NONE',  ( -18.01531055826208672, 36.06437412970446132, -148.3642685968914634 ) ) ;
#12991=CARTESIAN_POINT ( 'NONE',  ( -24.91068290195174129, 38.76331891718528766, -147.9212516401705386 ) ) ;
#12993=CARTESIAN_POINT ( 'NONE',  ( -15.56194485763432134, 32.85813890014918570, -144.2218690930858145 ) ) ;
#12999=CARTESIAN_POINT ( 'NONE',  ( -5.345822467930000599, 40.94956462150000220, -144.4907973060000188 ) ) ;
#13009=CARTESIAN_POINT ( 'NONE',  ( -13.15660544825068712, 35.28848928018297926, -140.1477172601388190 ) ) ;
#13020=CARTESIAN_POINT ( 'NONE',  ( -27.81458217780672726, 35.04316096251904611, -148.4325824290839364 ) ) ;
#13023=CARTESIAN_POINT ( 'NONE',  ( -12.47706116150000000, 35.17890886639999337, -148.2557368829999973 ) ) ;
#13033=CARTESIAN_POINT ( 'NONE',  ( -21.31444489898548866, 40.98951650670894509, -143.6265206826709004 ) ) ;
#13036=CARTESIAN_POINT ( 'NONE',  ( -16.81794493320086303, 37.02435727938927812, -140.5111119822732064 ) ) ;
#13045=CARTESIAN_POINT ( 'NONE',  ( -26.65693523154040534, 40.12876521656455964, -145.8849180162604000 ) ) ;
#13047=CARTESIAN_POINT ( 'NONE',  ( -21.48110840330020466, 32.98389871696830511, -146.2328788545872271 ) ) ;
#13054=CARTESIAN_POINT ( 'NONE',  ( -28.06178240320601347, 37.06443177825870094, -147.7991814975441685 ) ) ;
#13055=CARTESIAN_POINT ( 'NONE',  ( -14.58162373620000096, 40.18882273020000184, -142.1871799649999843 ) ) ;
#13066=CARTESIAN_POINT ( 'NONE',  ( -12.91895806490169996, 38.59375950464521310, -147.5965526133004460 ) ) ;
#13069=CARTESIAN_POINT ( 'NONE',  ( -29.88845675159999971, 40.47687533140000227, -144.8298193859999969 ) ) ;
#13071=CARTESIAN_POINT ( 'NONE',  ( -7.220568065030000149, 34.52259161599999970, -140.6708207100000152 ) ) ;
#13077=CARTESIAN_POINT ( 'NONE',  ( -20.13480534186356508, 38.99445981612083045, -139.6568722183936018 ) ) ;
#13085=CARTESIAN_POINT ( 'NONE',  ( -10.66194399679999982, 33.15920395730000081, -144.2988335299999960 ) ) ;
#13088=CARTESIAN_POINT ( 'NONE',  ( -20.21101409811914706, 36.97743810397754771, -140.7155889590011952 ) ) ;
#13092=CARTESIAN_POINT ( 'NONE',  ( -23.41786221899999987, 36.12684018730000446, -140.1150171360000058 ) ) ;
#13094=CARTESIAN_POINT ( 'NONE',  ( -22.42941481619999777, 36.22509709909999742, -139.9955747719999692 ) ) ;
#13101=CARTESIAN_POINT ( 'NONE',  ( -24.97797643630000053, 37.05442817780000553, -147.8575004449999994 ) ) ;
#13103=CARTESIAN_POINT ( 'NONE',  ( -16.17059658477510808, 32.32997518586915220, -143.3112915338346909 ) ) ;
#13110=CARTESIAN_POINT ( 'NONE',  ( -5.777804233054069094, 40.42495531994817526, -144.3912056291562180 ) ) ;
#13115=CARTESIAN_POINT ( 'NONE',  ( -22.18638062229441132, 34.91229655975453028, -146.9294338459641551 ) ) ;
#13120=CARTESIAN_POINT ( 'NONE',  ( -13.43635516220704318, 34.87491094518600931, -141.2152170337695622 ) ) ;
#13129=CARTESIAN_POINT ( 'NONE',  ( -27.58110728279703849, 34.24318910290035944, -147.7245096245254103 ) ) ;
#13133=CARTESIAN_POINT ( 'NONE',  ( -13.92432874550000044, 37.01165864720000087, -139.5650670249999905 ) ) ;
#13155=CARTESIAN_POINT ( 'NONE',  ( -27.48801997220000004, 39.21796412529999998, -147.0196846460000017 ) ) ;
#13169=CARTESIAN_POINT ( 'NONE',  ( -7.206173031983939659, 35.38491483748016009, -147.9515367334090001 ) ) ;
#13177=CARTESIAN_POINT ( 'NONE',  ( -12.57385931471914198, 38.47543513197548037, -147.4253642441603915 ) ) ;
#13179=CARTESIAN_POINT ( 'NONE',  ( -18.75277607359999976, 37.97046254950000588, -148.4181951110000171 ) ) ;
#13180=CARTESIAN_POINT ( 'NONE',  ( -29.55751743908506413, 40.46053532644847195, -144.8661948876702752 ) ) ;
#13182=ORIENTED_EDGE ( 'NONE', *, *, #13727, .F. ) ;
#13183=CARTESIAN_POINT ( 'NONE',  ( -6.033650297970000409, 36.94170754819999303, -147.9652040070000112 ) ) ;
#13190=CARTESIAN_POINT ( 'NONE',  ( -20.90770409063893354, 39.73774297846755843, -147.9490349955885620 ) ) ;
#13192=CARTESIAN_POINT ( 'NONE',  ( -27.07034204102121322, 35.31393907231532125, -147.6133383737439431 ) ) ;
#13212=CARTESIAN_POINT ( 'NONE',  ( -7.529689113779999943, 37.05876528330000497, -139.9906690790000141 ) ) ;
#13216=CARTESIAN_POINT ( 'NONE',  ( -23.76507348473139913, 39.47303768189023998, -147.6024660349875717 ) ) ;
#13218=CARTESIAN_POINT ( 'NONE',  ( -15.14562011634022731, 35.04295422807219040, -148.0905764885102371 ) ) ;
#13219=CARTESIAN_POINT ( 'NONE',  ( -16.92867099909999595, 34.38083942290000294, -140.2753207150000208 ) ) ;
#13224=CARTESIAN_POINT ( 'NONE',  ( -6.787442408928496818, 39.33311790174365541, -147.1061528123235860 ) ) ;
#13230=CARTESIAN_POINT ( 'NONE',  ( -21.12162747660223872, 36.95220905035969139, -147.5578847871684900 ) ) ;
#13236=CARTESIAN_POINT ( 'NONE',  ( -16.92431971702843541, 37.01165972487795131, -139.4624774945204422 ) ) ;
#13240=EDGE_CURVE ( 'NONE', #16530, #2118, #19365, .T. ) ;
#13243=ORIENTED_EDGE ( 'NONE', *, *, #8513, .F. ) ;
#13244=CARTESIAN_POINT ( 'NONE',  ( -28.77360867277181811, 32.46091987502819620, -144.5371065550806975 ) ) ;
#13248=CARTESIAN_POINT ( 'NONE',  ( -14.21072043115257699, 34.69090590940501784, -141.1210154221530786 ) ) ;
#13279=CARTESIAN_POINT ( 'NONE',  ( -28.08093528158016383, 37.94476457440455164, -148.1477062081667668 ) ) ;
#13288=CARTESIAN_POINT ( 'NONE',  ( -8.400427469268855418, 41.24693708775285472, -141.5795910977944061 ) ) ;
#13294=CARTESIAN_POINT ( 'NONE',  ( -25.64792992860000354, 37.04465132570000208, -139.7265440090000084 ) ) ;
#13296=CARTESIAN_POINT ( 'NONE',  ( -12.98514687064261963, 38.77227581979464333, -147.9931195024429087 ) ) ;
#13303=( BOUNDED_CURVE ( )  B_SPLINE_CURVE ( 5, ( #22237, #3808, #16878, #7822, #474, #20572 ),
 .UNSPECIFIED., .F., .F. ) 
 B_SPLINE_CURVE_WITH_KNOTS ( ( 6, 6 ),
 ( 1.570796326891506167, 3.141592653590000062 ),
 .UNSPECIFIED. ) 
 CURVE ( )  GEOMETRIC_REPRESENTATION_ITEM ( )  RATIONAL_B_SPLINE_CURVE ( ( 0.2500000000000000000, 0.2500000000122875043, 0.3000000000184313009, 0.4000000000245750864, 0.6000000000245750975, 1.000000000000000000 ) ) 
 REPRESENTATION_ITEM ( '' )  );
#13311=CARTESIAN_POINT ( 'NONE',  ( -20.84101097272391812, 38.55092845023212078, -147.7610021333602219 ) ) ;
#13314=CARTESIAN_POINT ( 'NONE',  ( -27.23537055383044247, 34.33249971486813479, -147.5370179225575953 ) ) ;
#13319=CARTESIAN_POINT ( 'NONE',  ( -9.971101149720000834, 37.05360750090000721, -147.8421425029999909 ) ) ;
#13342=CARTESIAN_POINT ( 'NONE',  ( -15.67014142460604020, 35.45905754580739710, -147.3461856841272208 ) ) ;
#13343=CARTESIAN_POINT ( 'NONE',  ( -15.94523344347496163, 33.71216531382139436, -145.7766456663748045 ) ) ;
#13349=CARTESIAN_POINT ( 'NONE',  ( -9.906675138925947977, 36.27859082920983980, -147.4875108566695303 ) ) ;
#13354=CARTESIAN_POINT ( 'NONE',  ( -22.52056272209999932, 33.27763168300000274, -146.2006519230000094 ) ) ;
#13360=CARTESIAN_POINT ( 'NONE',  ( -13.47165290135673921, 33.35876621941304165, -143.8174469061277989 ) ) ;
#13369=CARTESIAN_POINT ( 'NONE',  ( -13.38748872343123963, 33.38537881997591228, -144.5933708984670147 ) ) ;
#13382=CARTESIAN_POINT ( 'NONE',  ( -20.21101409811915772, 36.97743810397759745, -140.7155889590012237 ) ) ;
#13385=CARTESIAN_POINT ( 'NONE',  ( -22.79386933271688420, 37.02723109250344891, -140.7029355817511771 ) ) ;
#13386=CARTESIAN_POINT ( 'NONE',  ( -25.12153080232964086, 33.08100675563860449, -141.7696838823344194 ) ) ;
#13389=ORIENTED_EDGE ( 'NONE', *, *, #4849, .T. ) ;
#13399=CARTESIAN_POINT ( 'NONE',  ( -27.06022691627751797, 38.83733237962867690, -148.2479545111105779 ) ) ;
#13404=CARTESIAN_POINT ( 'NONE',  ( -11.85909339612901015, 36.92087135289245481, -147.9691652863633067 ) ) ;
#13408=CARTESIAN_POINT ( 'NONE',  ( -13.92432874550000044, 37.01165864720000087, -139.5650670249999905 ) ) ;
#13424=CARTESIAN_POINT ( 'NONE',  ( -20.76253627919999900, 39.57534689110000414, -140.5049880910000013 ) ) ;
#13426=CARTESIAN_POINT ( 'NONE',  ( -27.65087262191089224, 32.98947248583699832, -143.4940380741495289 ) ) ;
#13435=CARTESIAN_POINT ( 'NONE',  ( -8.514310886080000529, 36.94123471670000214, -140.1199228270000106 ) ) ;
#13442=CARTESIAN_POINT ( 'NONE',  ( -30.28539838652671179, 40.31549301428387366, -145.3075639834989090 ) ) ;
#13443=CARTESIAN_POINT ( 'NONE',  ( -13.92432874550000044, 37.01165864720000087, -139.5650670249999905 ) ) ;
#13462=CARTESIAN_POINT ( 'NONE',  ( -9.801780389369936231, 37.03339632395869074, -147.4803110669174657 ) ) ;
#13467=CARTESIAN_POINT ( 'NONE',  ( -22.75008518894089704, 33.18911177007243651, -144.4560875053247457 ) ) ;
#13476=CARTESIAN_POINT ( 'NONE',  ( -8.810109936767679173, 39.32487244797151504, -140.7337397743969802 ) ) ;
#13479=CARTESIAN_POINT ( 'NONE',  ( -28.32050416868494125, 34.28824206719405510, -147.8072173032999217 ) ) ;
#13482=CARTESIAN_POINT ( 'NONE',  ( -14.39443208618090253, 34.43246107294096703, -140.8168812543075603 ) ) ;
#13486=ORIENTED_EDGE ( 'NONE', *, *, #16428, .F. ) ;
#13492=CARTESIAN_POINT ( 'NONE',  ( -18.27025349466079973, 40.59684088653609280, -144.3213525969109128 ) ) ;
#13495=CARTESIAN_POINT ( 'NONE',  ( -24.56649898262948994, 33.80095595918812990, -145.8672865390101663 ) ) ;
#13505=CARTESIAN_POINT ( 'NONE',  ( -26.76912629117864739, 37.72282967552698807, -147.8698271774196371 ) ) ;
#13514=CARTESIAN_POINT ( 'NONE',  ( -10.51976837306068191, 37.87277224112855123, -140.3566920414173467 ) ) ;
#13518=CARTESIAN_POINT ( 'NONE',  ( -9.562013113444260526, 37.00477621355918245, -148.7272342975820436 ) ) ;
#13527=CARTESIAN_POINT ( 'NONE',  ( -18.05676631878100125, 41.24287485562951616, -146.4171244423180838 ) ) ;
#13537=( BOUNDED_CURVE ( )  B_SPLINE_CURVE ( 5, ( #15077, #9246, #7463, #18310, #20438, #11490 ),
 .UNSPECIFIED., .F., .F. ) 
 B_SPLINE_CURVE_WITH_KNOTS ( ( 6, 6 ),
 ( 1.570796326505558893, 3.141592653590000062 ),
 .UNSPECIFIED. ) 
 CURVE ( )  GEOMETRIC_REPRESENTATION_ITEM ( )  RATIONAL_B_SPLINE_CURVE ( ( 0.2500000000000000000, 0.2499999999631472292, 0.2999999999447208188, 0.3999999999262944250, 0.5999999999262943806, 1.000000000000000000 ) ) 
 REPRESENTATION_ITEM ( '' )  );
#13538=CARTESIAN_POINT ( 'NONE',  ( -14.58162373618102059, 40.18882273014816064, -142.1871799655052087 ) ) ;
#13540=CARTESIAN_POINT ( 'NONE',  ( -24.26662447743907691, 35.20109951642859869, -148.0073960929780128 ) ) ;
#13553=ADVANCED_FACE ( 'NONE', ( #1171 ), #20752, .F. ) ;
#13562=CARTESIAN_POINT ( 'NONE',  ( -7.728596210859999260, 38.74386132360000090, -140.2295773360000055 ) ) ;
#13567=CARTESIAN_POINT ( 'NONE',  ( -16.71251657190000017, 33.01037093000000766, -141.5651630139999781 ) ) ;
#13569=CARTESIAN_POINT ( 'NONE',  ( -15.76532943033608092, 34.76918918225535293, -146.9254579970084080 ) ) ;
#13571=CARTESIAN_POINT ( 'NONE',  ( -4.584402860569999127, 37.05223431090000474, -140.2914745300000163 ) ) ;
#13575=CARTESIAN_POINT ( 'NONE',  ( -10.15741051819999896, 33.19655140199999721, -141.5761258080000005 ) ) ;
#13586=CARTESIAN_POINT ( 'NONE',  ( -23.34997301947807813, 41.23575095046039962, -144.6233831889099974 ) ) ;
#13591=CARTESIAN_POINT ( 'NONE',  ( -14.84561440076392813, 36.91926241633399997, -147.9647079511927643 ) ) ;
#13594=CARTESIAN_POINT ( 'NONE',  ( -10.16983759159231049, 35.05179278799776199, -148.3304041598011622 ) ) ;
#13602=CARTESIAN_POINT ( 'NONE',  ( -13.60030749279999895, 34.19157895370000233, -140.3499153360000093 ) ) ;
#13611=CARTESIAN_POINT ( 'NONE',  ( -21.03694116381500123, 36.94210036639135808, -147.9486865822096036 ) ) ;
#13613=CARTESIAN_POINT ( 'NONE',  ( -18.70477357766290183, 38.50421286460694148, -147.2749284916807824 ) ) ;
#13618=CARTESIAN_POINT ( 'NONE',  ( -25.60593271316125197, 35.60614443581115296, -140.8684412788813063 ) ) ;
#13651=CARTESIAN_POINT ( 'NONE',  ( -18.85469010170000459, 37.03971195569999963, -148.4264296979999926 ) ) ;
#13657=CARTESIAN_POINT ( 'NONE',  ( -22.07763076355694665, 37.06632353693416349, -147.8362371614679489 ) ) ;
#13660=CARTESIAN_POINT ( 'NONE',  ( -15.10539350069024067, 40.90753194052741293, -141.7004951165038449 ) ) ;
#13662=CARTESIAN_POINT ( 'NONE',  ( -26.33255611194164558, 36.96293009473756541, -139.4434112040622153 ) ) ;
#13696=CARTESIAN_POINT ( 'NONE',  ( -16.46253290489252663, 36.15891006124687834, -139.5597335927451752 ) ) ;
#13699=CARTESIAN_POINT ( 'NONE',  ( -4.584402860569999127, 37.05223431090000474, -140.2914745300000163 ) ) ;
#13704=CARTESIAN_POINT ( 'NONE',  ( -9.958372260283605115, 33.77808441015003638, -141.9208523075240009 ) ) ;
#13713=CARTESIAN_POINT ( 'NONE',  ( -24.30767937719999949, 40.97374044589999897, -144.4830919949999952 ) ) ;
#13717=CARTESIAN_POINT ( 'NONE',  ( -15.24898703719208193, 36.96741147810104877, -148.5896301378323301 ) ) ;
#13719=CARTESIAN_POINT ( 'NONE',  ( -9.776657394585679839, 32.72643639172331120, -146.2409476793991416 ) ) ;
#13727=EDGE_CURVE ( 'NONE', #14370, #1248, #8568, .T. ) ;
#13730=CARTESIAN_POINT ( 'NONE',  ( -6.227860603739999945, 35.34754625490000279, -147.7419925389999946 ) ) ;
#13731=CARTESIAN_POINT ( 'NONE',  ( -28.90798551740000022, 37.01360947639999921, -139.5686590450000040 ) ) ;
#13733=( BOUNDED_SURFACE ( )  B_SPLINE_SURFACE ( 5, 5, ( 
 ( #20849, #10117, #22398, #21091, #13462, #4318 ),
 ( #22743, #17033, #19061, #11907, #13349, #20728 ),
 ( #6562, #12025, #20978, #10239, #4543, #17510 ),
 ( #9998, #1233, #11546, #986, #6098, #8217 ),
 ( #18823, #19175, #2535, #6444, #8101, #9757 ),
 ( #2883, #7984, #15262, #22519, #4423, #11662 ),
 ( #2652, #9882, #17155, #875, #6321, #15374 ),
 ( #13575, #15485, #13704, #4667, #17391, #18187 ),
 ( #23426, #5570, #12939, #14726, #19746, #18311 ),
 ( #2026, #2130, #5460, #1905, #12705, #20217 ),
 ( #15727, #10789, #5684, #16515, #9247, #221 ),
 ( #3441, #11147, #6674, #14382, #17959, #18420 ) ),
 .UNSPECIFIED., .F., .F., .F. ) 
 B_SPLINE_SURFACE_WITH_KNOTS ( ( 6, 3, 3, 6 ),
 ( 6, 6 ),
 ( 0.000000000000000000, 4.570086947620000117, 8.869210483019999813, 12.91901055009999943 ),
 ( 0.000000000000000000, 1.570796326852889946 ),
 .UNSPECIFIED. ) 
 GEOMETRIC_REPRESENTATION_ITEM ( )  RATIONAL_B_SPLINE_SURFACE ( (
 ( 1.000000000000000000, 0.5999999999852579924, 0.3999999999852579813, 0.2999999999889434998, 0.2499999999926290073, 0.2500000000000000000),
 ( 1.000000000000000000, 0.5999999999852579924, 0.3999999999852579813, 0.2999999999889434998, 0.2499999999926290073, 0.2500000000000000000),
 ( 1.000000000000000000, 0.5999999999852579924, 0.3999999999852579813, 0.2999999999889434998, 0.2499999999926290073, 0.2500000000000000000),
 ( 1.000000000000000000, 0.5999999999852579924, 0.3999999999852579813, 0.2999999999889434998, 0.2499999999926290073, 0.2500000000000000000),
 ( 1.000000000000000000, 0.5999999999852579924, 0.3999999999852579813, 0.2999999999889434998, 0.2499999999926290073, 0.2500000000000000000),
 ( 1.000000000000000000, 0.5999999999852579924, 0.3999999999852579813, 0.2999999999889434998, 0.2499999999926290073, 0.2500000000000000000),
 ( 1.000000000000000000, 0.5999999999852579924, 0.3999999999852579813, 0.2999999999889434998, 0.2499999999926290073, 0.2500000000000000000),
 ( 1.000000000000000000, 0.5999999999852579924, 0.3999999999852579813, 0.2999999999889434998, 0.2499999999926290073, 0.2500000000000000000),
 ( 1.000000000000000000, 0.5999999999852579924, 0.3999999999852579813, 0.2999999999889434998, 0.2499999999926290073, 0.2500000000000000000),
 ( 1.000000000000000000, 0.5999999999852579924, 0.3999999999852579813, 0.2999999999889434998, 0.2499999999926290073, 0.2500000000000000000),
 ( 1.000000000000000000, 0.5999999999852579924, 0.3999999999852579813, 0.2999999999889434998, 0.2499999999926290073, 0.2500000000000000000),
 ( 1.000000000000000000, 0.5999999999852579924, 0.3999999999852579813, 0.2999999999889434998, 0.2499999999926290073, 0.2500000000000000000) ) ) 
 REPRESENTATION_ITEM ( '' )  SURFACE ( )  );
#13741=CARTESIAN_POINT ( 'NONE',  ( -21.78779062148921497, 39.33326857531331910, -147.2076583194208013 ) ) ;
#13742=CARTESIAN_POINT ( 'NONE',  ( -18.75277607359999976, 37.97046254950000588, -148.4181951110000171 ) ) ;
#13747=CARTESIAN_POINT ( 'NONE',  ( -25.18773796597552916, 33.56545492220686100, -143.6970596393699964 ) ) ;
#13750=CARTESIAN_POINT ( 'NONE',  ( -12.13467478867948124, 40.69160539494399842, -144.5327625260007665 ) ) ;
#13770=CARTESIAN_POINT ( 'NONE',  ( -19.08835673601252836, 35.67218568070619966, -147.3285224709407260 ) ) ;
#13771=CARTESIAN_POINT ( 'NONE',  ( -10.86836323999999898, 38.91206754959999614, -139.9811931129999891 ) ) ;
#13776=CARTESIAN_POINT ( 'NONE',  ( -27.80359210600000353, 32.89696731220000459, -146.3345487529999787 ) ) ;
#13784=ORIENTED_EDGE ( 'NONE', *, *, #15631, .F. ) ;
#13791=CARTESIAN_POINT ( 'NONE',  ( -14.24884431174197452, 36.97292245484901230, -139.4994906131649088 ) ) ;
#13793=CARTESIAN_POINT ( 'NONE',  ( -25.54709891099935959, 36.13246793449779659, -139.7173810944768206 ) ) ;
#13799=CARTESIAN_POINT ( 'NONE',  ( -11.58731752079999922, 38.53682247849999953, -140.5940415739999878 ) ) ;
#13811=CARTESIAN_POINT ( 'NONE',  ( -14.21887350778302128, 37.71951061619743939, -140.5431489171175770 ) ) ;
#13822=CARTESIAN_POINT ( 'NONE',  ( -16.72278394149610037, 36.31586521337584372, -140.5063707124861878 ) ) ;
#13825=CARTESIAN_POINT ( 'NONE',  ( -5.271986118780927377, 36.97016010513713979, -139.4665544805324657 ) ) ;
#13833=CARTESIAN_POINT ( 'NONE',  ( -28.88704352681202536, 32.48182513811993744, -143.5726213976734584 ) ) ;
#13836=CARTESIAN_POINT ( 'NONE',  ( -23.48449349015638887, 36.94479390616790937, -140.4349842069408112 ) ) ;
#13840=CARTESIAN_POINT ( 'NONE',  ( -5.064279449469999861, 40.47653686799999662, -142.0698957560000224 ) ) ;
#13844=AXIS2_PLACEMENT_3D ( 'NONE', #6350, #18965, #545 ) ;
#13849=CARTESIAN_POINT ( 'NONE',  ( -8.168564777796522236, 34.74583461989782052, -141.1491392514008680 ) ) ;
#13850=CARTESIAN_POINT ( 'NONE',  ( -26.50527565049999978, 41.51083911109999747, -144.5405030839999938 ) ) ;
#13857=CARTESIAN_POINT ( 'NONE',  ( -18.04274282227677872, 40.84322841768359780, -141.6905766441785488 ) ) ;
#13862=CARTESIAN_POINT ( 'NONE',  ( -25.44349950041027952, 35.21826511839348228, -139.9516901547978023 ) ) ;
#13878=CARTESIAN_POINT ( 'NONE',  ( -8.712023184210000437, 38.57885015669999973, -140.3122811009999964 ) ) ;
#13881=CARTESIAN_POINT ( 'NONE',  ( -8.565647946495506204, 36.93510680650897626, -139.7232782068719530 ) ) ;
#13899=CARTESIAN_POINT ( 'NONE',  ( -18.85469010170000459, 37.03971195569999963, -148.4264296979999926 ) ) ;
#13902=CARTESIAN_POINT ( 'NONE',  ( -26.31398817765400011, 34.53172810853797614, -140.8131697956154653 ) ) ;
#13905=CARTESIAN_POINT ( 'NONE',  ( -12.13467478879999994, 40.69160539509999808, -144.5327625259999706 ) ) ;
#13908=VERTEX_POINT ( 'NONE', #9031 ) ;
#13919=CARTESIAN_POINT ( 'NONE',  ( -14.83261257093395180, 37.83839852817070692, -148.3884378576142922 ) ) ;
#13940=ORIENTED_EDGE ( 'NONE', *, *, #20145, .T. ) ;
#13942=CARTESIAN_POINT ( 'NONE',  ( -28.50747929780000334, 33.37084171139999711, -143.6371486329999811 ) ) ;
#13945=CARTESIAN_POINT ( 'NONE',  ( -23.55797472143900251, 40.74841938861488444, -146.3388075608100110 ) ) ;
#13950=CARTESIAN_POINT ( 'NONE',  ( -9.544641620896076262, 34.08278316542619990, -147.7344509276062752 ) ) ;
#13957=CARTESIAN_POINT ( 'NONE',  ( -20.85361110351559333, 37.81545827817836170, -148.3531455720921031 ) ) ;
#13961=CARTESIAN_POINT ( 'NONE',  ( -7.284577139200968610, 35.45677114639833150, -140.5143805028650377 ) ) ;
#13970=CARTESIAN_POINT ( 'NONE',  ( -18.31895680040000229, 41.06933176500000116, -146.2870363079999834 ) ) ;
#13972=CARTESIAN_POINT ( 'NONE',  ( -25.64792992860000354, 37.04465132570000208, -139.7265440090000084 ) ) ;
#13987=CARTESIAN_POINT ( 'NONE',  ( -27.77884619099882713, 32.57034656671790174, -143.4578452901890273 ) ) ;
#13991=CARTESIAN_POINT ( 'NONE',  ( -9.005502668700000157, 40.51905748810000318, -141.9284054809999986 ) ) ;
#13992=CARTESIAN_POINT ( 'NONE',  ( -11.86981903014650008, 40.35288497626832083, -142.1893091612195974 ) ) ;
#13994=CARTESIAN_POINT ( 'NONE',  ( -7.644488704951585945, 35.02206480932151322, -139.6643986246225779 ) ) ;
#13996=CARTESIAN_POINT ( 'NONE',  ( -28.59946202389999925, 34.31616424880000693, -140.2812573680000128 ) ) ;
#14006=EDGE_CURVE ( 'NONE', #22397, #9000, #9095, .T. ) ;
#14012=CARTESIAN_POINT ( 'NONE',  ( -19.54668701403429054, 37.05673630841071287, -139.5622637236315029 ) ) ;
#14016=CARTESIAN_POINT ( 'NONE',  ( -25.78373889329461122, 32.73831349156768056, -141.6589310348909123 ) ) ;
#14031=CARTESIAN_POINT ( 'NONE',  ( -24.36912841290000031, 34.40976477760000307, -147.5507798129999912 ) ) ;
#14038=CARTESIAN_POINT ( 'NONE',  ( -13.82941295814141647, 37.74960637515216177, -140.6313136556216250 ) ) ;
#14040=ORIENTED_EDGE ( 'NONE', *, *, #17358, .T. ) ;
#14052=CARTESIAN_POINT ( 'NONE',  ( -15.82146356845421131, 32.49419957915463186, -143.2970122493755127 ) ) ;
#14057=CARTESIAN_POINT ( 'NONE',  ( -7.206173031919999694, 35.38491483730000198, -147.9515367340000012 ) ) ;
#14062=CARTESIAN_POINT ( 'NONE',  ( -26.10314130450000292, 34.70878586860000325, -141.0128996759999893 ) ) ;
#14071=CARTESIAN_POINT ( 'NONE',  ( -23.61748844584506557, 39.23591355021475380, -147.3005354435039749 ) ) ;
#14084=CARTESIAN_POINT ( 'NONE',  ( -21.63220705389141685, 37.01315499805642162, -148.7192284428339519 ) ) ;
#14087=CARTESIAN_POINT ( 'NONE',  ( -6.190578628962761343, 36.21727375469096444, -147.6271024187999501 ) ) ;
#14105=FACE_OUTER_BOUND ( 'NONE', #20859, .T. ) ;
#14110=CARTESIAN_POINT ( 'NONE',  ( -15.90674982588249975, 37.04592612750588643, -148.5146100863278491 ) ) ;
#14120=CARTESIAN_POINT ( 'NONE',  ( -18.28451977779999993, 36.23520409090000527, -147.6763998119999997 ) ) ;
#14121=CARTESIAN_POINT ( 'NONE',  ( -12.18289575740000075, 37.87223172089999679, -148.4976681630000144 ) ) ;
#14123=CARTESIAN_POINT ( 'NONE',  ( -8.029216439717911769, 32.92480140023701551, -141.8798076613048522 ) ) ;
#14142=CARTESIAN_POINT ( 'NONE',  ( -21.23917607311824085, 35.28761490586239802, -147.7082871195992197 ) ) ;
#14144=EDGE_CURVE ( 'NONE', #10397, #12619, #5398, .T. ) ;
#14149=CARTESIAN_POINT ( 'NONE',  ( -11.11377970773875212, 36.98904460433607255, -140.6889018750557341 ) ) ;
#14150=VERTEX_POINT ( 'NONE', #13435 ) ;
#14156=CARTESIAN_POINT ( 'NONE',  ( -13.82353779670000193, 34.78290842719999887, -141.1681162280000308 ) ) ;
#14160=CARTESIAN_POINT ( 'NONE',  ( -22.00705883600000234, 37.05789963359999462, -148.1619053240000028 ) ) ;
#14161=CARTESIAN_POINT ( 'NONE',  ( -15.26331651089999930, 39.75437292659999855, -147.8043400740000095 ) ) ;
#14162=CARTESIAN_POINT ( 'NONE',  ( -29.32937220846275750, 40.41939957101679681, -140.7656299762288086 ) ) ;
#14172=EDGE_LOOP ( 'NONE', ( #18568, #17450, #2406, #18968 ) ) ;
#14176=CARTESIAN_POINT ( 'NONE',  ( -5.769798041881806228, 38.72966034773180866, -148.0785409402818118 ) ) ;
#14192=CARTESIAN_POINT ( 'NONE',  ( -11.26413364454818122, 36.97109742514091124, -139.4278719022179018 ) ) ;
#14202=B_SPLINE_CURVE_WITH_KNOTS ( 'NONE', 5,
 ( #2794, #10141, #17656, #19197, #8240, #3149, #2910, #17415, #15514, #21232, #10379, #15753 ),
 .UNSPECIFIED., .F., .F.,
 ( 6, 3, 3, 6 ),
 ( 0.000000000000000000, 4.390059406679999832, 8.746277600790000051, 13.07048654050000103 ),
 .UNSPECIFIED. ) ;
#14204=CARTESIAN_POINT ( 'NONE',  ( -6.665693515917223699, 34.99563620361987404, -146.8660724163397333 ) ) ;
#14208=CARTESIAN_POINT ( 'NONE',  ( -5.579327536678420074, 37.66950319827602556, -140.5530665557081704 ) ) ;
#14218=CARTESIAN_POINT ( 'NONE',  ( -26.17844700321287377, 36.98132551455246642, -140.6351982806903607 ) ) ;
#14222=( BOUNDED_CURVE ( )  B_SPLINE_CURVE ( 5, ( #19765, #21316, #19528, #3333, #15950, #7019 ),
 .UNSPECIFIED., .F., .F. ) 
 B_SPLINE_CURVE_WITH_KNOTS ( ( 6, 6 ),
 ( 1.570796326807921472, 3.141592653590000062 ),
 .UNSPECIFIED. ) 
 CURVE ( )  GEOMETRIC_REPRESENTATION_ITEM ( )  RATIONAL_B_SPLINE_CURVE ( ( 0.2500000000000000000, 0.2500000000016452395, 0.3000000000024678481, 0.4000000000032904457, 0.6000000000032904568, 1.000000000000000000 ) ) 
 REPRESENTATION_ITEM ( '' )  );
#14231=CARTESIAN_POINT ( 'NONE',  ( -28.14233742207320788, 35.42069160767093194, -140.2329357297371359 ) ) ;
#14237=CARTESIAN_POINT ( 'NONE',  ( -19.28609856400827738, 34.66429844319404197, -140.9609051181238044 ) ) ;
#14254=CARTESIAN_POINT ( 'NONE',  ( -11.19806794730000021, 41.07225940149999843, -141.8826665010000170 ) ) ;
#14256=CARTESIAN_POINT ( 'NONE',  ( -15.86060558933779419, 39.62525409245568397, -147.5113276022380830 ) ) ;
#14261=CARTESIAN_POINT ( 'NONE',  ( -25.95437585238067868, 39.65968214927003288, -140.4458241779535967 ) ) ;
#14274=CARTESIAN_POINT ( 'NONE',  ( -15.00140173387118026, 40.20535686067567838, -145.8913236318710176 ) ) ;
#14275=CARTESIAN_POINT ( 'NONE',  ( -29.13601448249999848, 36.98639052360000079, -140.5419328609999923 ) ) ;
#14289=CARTESIAN_POINT ( 'NONE',  ( -6.033650297970000409, 36.94170754819999303, -147.9652040070000112 ) ) ;
#14301=CARTESIAN_POINT ( 'NONE',  ( -28.90798551733967869, 37.01360947636671739, -139.5686590453834128 ) ) ;
#14305=CARTESIAN_POINT ( 'NONE',  ( -11.10890527080962009, 34.84141842887415663, -140.9538660576732241 ) ) ;
#14307=CARTESIAN_POINT ( 'NONE',  ( -8.396783337457932817, 40.57449494537098644, -144.4531261594902958 ) ) ;
#14314=CARTESIAN_POINT ( 'NONE',  ( -7.486908230310626244, 37.06387187510053849, -140.3212062627006560 ) ) ;
#14340=CARTESIAN_POINT ( 'NONE',  ( -16.06433926788437461, 35.52312188426208905, -147.3204108562227646 ) ) ;
#14348=CARTESIAN_POINT ( 'NONE',  ( -19.68769410165050715, 36.28218526682968559, -140.6463262768891127 ) ) ;
#14351=CARTESIAN_POINT ( 'NONE',  ( -12.32040252380945589, 37.67168662422751169, -147.4262574636698844 ) ) ;
#14366=CARTESIAN_POINT ( 'NONE',  ( -18.90246017573007720, 37.04541408823331494, -147.4848489023210050 ) ) ;
#14368=ORIENTED_EDGE ( 'NONE', *, *, #22815, .F. ) ;
#14370=VERTEX_POINT ( 'NONE', #10676 ) ;
#14377=CARTESIAN_POINT ( 'NONE',  ( -26.39607007120000048, 36.95534867429999792, -140.3840478969999879 ) ) ;
#14382=CARTESIAN_POINT ( 'NONE',  ( -10.69115198329542160, 37.03949207291182688, -140.6562969416297335 ) ) ;
#14387=CARTESIAN_POINT ( 'NONE',  ( -16.72278394150000125, 36.31586521340000218, -140.5063707120000061 ) ) ;
#14392=CARTESIAN_POINT ( 'NONE',  ( -29.04280990185221967, 38.86145750698325685, -140.9282040248405110 ) ) ;
#14395=CARTESIAN_POINT ( 'NONE',  ( -25.38678224712056775, 37.07582353396835373, -140.0279244692600855 ) ) ;
#14409=CARTESIAN_POINT ( 'NONE',  ( -13.71246964740000074, 35.06639867129999999, -139.8243480419999685 ) ) ;
#14410=CARTESIAN_POINT ( 'NONE',  ( -5.059418532210888664, 38.95414396229264042, -139.6466485215420619 ) ) ;
#14423=CARTESIAN_POINT ( 'NONE',  ( -29.97886196652672197, 40.49728245963383699, -142.7481031354987238 ) ) ;
#14428=CARTESIAN_POINT ( 'NONE',  ( -10.58679693489213491, 34.36322230824750079, -140.1414225335838921 ) ) ;
#14429=CARTESIAN_POINT ( 'NONE',  ( -18.90938373568686259, 34.33541876391318226, -147.9661085319850713 ) ) ;
#14430=CARTESIAN_POINT ( 'NONE',  ( -9.771488485234659294, 38.65068379629019546, -147.6127673914778029 ) ) ;
#14434=EDGE_LOOP ( 'NONE', ( #2392, #12315, #15025, #9803 ) ) ;
#14473=CARTESIAN_POINT ( 'NONE',  ( -19.32129348605712593, 33.83991419265531420, -142.3697286030541704 ) ) ;
#14474=CARTESIAN_POINT ( 'NONE',  ( -12.66714788137640113, 37.75265353618991782, -147.6129237412843906 ) ) ;
#14499=CARTESIAN_POINT ( 'NONE',  ( -15.36599175854349930, 37.73046438849700479, -147.5598381917543804 ) ) ;
#14509=( BOUNDED_CURVE ( )  B_SPLINE_CURVE ( 5, ( #6317, #22740, #8213, #6670, #11779, #12142 ),
 .UNSPECIFIED., .F., .F. ) 
 B_SPLINE_CURVE_WITH_KNOTS ( ( 6, 6 ),
 ( 0.000000000000000000, 1.570796326447242430 ),
 .UNSPECIFIED. ) 
 CURVE ( )  GEOMETRIC_REPRESENTATION_ITEM ( )  RATIONAL_B_SPLINE_CURVE ( ( 1.000000000000000000, 0.6000000000885556961, 0.4000000000885557405, 0.3000000000664168054, 0.2500000000442779147, 0.2500000000000000000 ) ) 
 REPRESENTATION_ITEM ( '' )  );
#14513=CARTESIAN_POINT ( 'NONE',  ( -16.20147620269999678, 33.40528963979999588, -143.4816615020000086 ) ) ;
#14519=CARTESIAN_POINT ( 'NONE',  ( -10.65913935279999869, 37.04331329920000115, -139.7140392919999954 ) ) ;
#14521=CARTESIAN_POINT ( 'NONE',  ( -16.74301326758274300, 39.28355396474279360, -140.9617246865330173 ) ) ;
#14537=CARTESIAN_POINT ( 'NONE',  ( -4.929500267440261041, 40.76073806058817439, -141.9202204794446232 ) ) ;
#14540=CARTESIAN_POINT ( 'NONE',  ( -26.86882954950000268, 40.29793777999999804, -142.0811670120000088 ) ) ;
#14553=CARTESIAN_POINT ( 'NONE',  ( -11.06913245161039860, 35.13609156430476332, -139.6650812237304820 ) ) ;
#14554=CARTESIAN_POINT ( 'NONE',  ( -19.91220883949999987, 32.96944242089999477, -141.9853941000000077 ) ) ;
#14567=ORIENTED_EDGE ( 'NONE', *, *, #12655, .T. ) ;
#14583=CARTESIAN_POINT ( 'NONE',  ( -16.71251657190000017, 33.01037093000000766, -141.5651630139999781 ) ) ;
#14589=CARTESIAN_POINT ( 'NONE',  ( -19.15756699511638317, 33.51755048520087854, -143.8372150283107374 ) ) ;
#14593=ADVANCED_FACE ( 'NONE', ( #20441 ), #11010, .F. ) ;
#14607=FACE_OUTER_BOUND ( 'NONE', #8419, .T. ) ;
#14622=CARTESIAN_POINT ( 'NONE',  ( -13.38748872360000064, 33.38537881989999789, -144.5933708990000071 ) ) ;
#14629=CARTESIAN_POINT ( 'NONE',  ( -16.44879669585063908, 37.92811585471407199, -139.9493606072290390 ) ) ;
#14630=CARTESIAN_POINT ( 'NONE',  ( -22.82643395159999855, 32.86988923359999859, -143.6006525860000238 ) ) ;
#14640=( BOUNDED_SURFACE ( )  B_SPLINE_SURFACE ( 5, 5, ( 
 ( #12919, #2107, #9329, #14832, #15654, #17310 ),
 ( #1152, #15526, #19335, #10284, #2572, #18980 ),
 ( #12064, #22791, #911, #21011, #8253, #11701 ),
 ( #8135, #15407, #6131, #3047, #6489, #15301 ),
 ( #1025, #4703, #13495, #22914, #22666, #20654 ),
 ( #6598, #2922, #17072, #9919, #20770, #1272 ),
 ( #6362, #11943, #17556, #13747, #15178, #9794 ),
 ( #13386, #4464, #794, #22436, #2804, #10034 ),
 ( #8385, #20895, #19211, #4349, #11583, #2692 ),
 ( #13862, #17426, #17192, #13618, #10154, #4584 ),
 ( #21129, #4822, #11824, #18861, #8017, #22557 ),
 ( #6246, #19099, #16122, #12533, #14218, #7073 ) ),
 .UNSPECIFIED., .F., .F., .F. ) 
 B_SPLINE_SURFACE_WITH_KNOTS ( ( 6, 3, 3, 6 ),
 ( 6, 6 ),
 ( 0.000000000000000000, 4.454241660750000165, 8.943513424000000711, 13.47090878500000066 ),
 ( 1.570796326706449975, 3.141592653590000062 ),
 .UNSPECIFIED. ) 
 GEOMETRIC_REPRESENTATION_ITEM ( )  RATIONAL_B_SPLINE_SURFACE ( (
 ( 0.2500000000000000000, 0.2499999999887249913, 0.2999999999830880171, 0.3999999999774505044, 0.5999999999774500159, 1.000000000000000000),
 ( 0.2500000000000000000, 0.2499999999887249913, 0.2999999999830880171, 0.3999999999774505044, 0.5999999999774500159, 1.000000000000000000),
 ( 0.2500000000000000000, 0.2499999999887249913, 0.2999999999830880171, 0.3999999999774505044, 0.5999999999774500159, 1.000000000000000000),
 ( 0.2500000000000000000, 0.2499999999887249913, 0.2999999999830880171, 0.3999999999774505044, 0.5999999999774500159, 1.000000000000000000),
 ( 0.2500000000000000000, 0.2499999999887249913, 0.2999999999830880171, 0.3999999999774505044, 0.5999999999774500159, 1.000000000000000000),
 ( 0.2500000000000000000, 0.2499999999887249913, 0.2999999999830880171, 0.3999999999774505044, 0.5999999999774500159, 1.000000000000000000),
 ( 0.2500000000000000000, 0.2499999999887249913, 0.2999999999830880171, 0.3999999999774505044, 0.5999999999774500159, 1.000000000000000000),
 ( 0.2500000000000000000, 0.2499999999887249913, 0.2999999999830880171, 0.3999999999774505044, 0.5999999999774500159, 1.000000000000000000),
 ( 0.2500000000000000000, 0.2499999999887249913, 0.2999999999830880171, 0.3999999999774505044, 0.5999999999774500159, 1.000000000000000000),
 ( 0.2500000000000000000, 0.2499999999887249913, 0.2999999999830880171, 0.3999999999774505044, 0.5999999999774500159, 1.000000000000000000),
 ( 0.2500000000000000000, 0.2499999999887249913, 0.2999999999830880171, 0.3999999999774505044, 0.5999999999774500159, 1.000000000000000000),
 ( 0.2500000000000000000, 0.2499999999887249913, 0.2999999999830880171, 0.3999999999774505044, 0.5999999999774500159, 1.000000000000000000) ) ) 
 REPRESENTATION_ITEM ( '' )  SURFACE ( )  );
#14644=CARTESIAN_POINT ( 'NONE',  ( -4.818372690434668648, 39.73127005685628177, -140.3607218662884009 ) ) ;
#14655=CARTESIAN_POINT ( 'NONE',  ( -22.03156944979999921, 33.39557638549999297, -141.8445571070000142 ) ) ;
#14659=CARTESIAN_POINT ( 'NONE',  ( -11.37294983628254208, 34.64303755342024971, -140.7164989729878641 ) ) ;
#14661=CARTESIAN_POINT ( 'NONE',  ( -18.80491877122047129, 35.17450263849315917, -148.4239332058163825 ) ) ;
#14671=CARTESIAN_POINT ( 'NONE',  ( -6.289131962756090211, 37.69042679468366686, -147.3987319627627812 ) ) ;
#14696=CARTESIAN_POINT ( 'NONE',  ( -18.64600821060120239, 33.72696025750419579, -146.0724859999907892 ) ) ;
#14697=ADVANCED_FACE ( 'NONE', ( #18736 ), #16507, .F. ) ;
#14712=CARTESIAN_POINT ( 'NONE',  ( -26.11027262183172226, 40.79568045835033274, -143.6926091179167315 ) ) ;
#14726=CARTESIAN_POINT ( 'NONE',  ( -10.42144917147403227, 35.06776031302221952, -141.1445986588747132 ) ) ;
#14727=CARTESIAN_POINT ( 'NONE',  ( -7.880169906864895601, 39.70507027285627544, -140.3906468505855685 ) ) ;
#14738=CARTESIAN_POINT ( 'NONE',  ( -17.81604679228244237, 41.73690735279433994, -144.4734149966611199 ) ) ;
#14739=CARTESIAN_POINT ( 'NONE',  ( -29.15022769660199131, 39.64481412623220535, -141.5404043871726287 ) ) ;
#14748=CARTESIAN_POINT ( 'NONE',  ( -19.75449977488149855, 38.96382659270718563, -139.8356432587078189 ) ) ;
#14750=CARTESIAN_POINT ( 'NONE',  ( -27.87941100700000163, 36.27261185799999765, -147.6334388379999893 ) ) ;
#14760=CARTESIAN_POINT ( 'NONE',  ( -16.16658683009994490, 37.07694188521399070, -148.2333767341115447 ) ) ;
#14769=CARTESIAN_POINT ( 'NONE',  ( -24.06602356359999817, 36.94557182220000158, -148.2530914610000252 ) ) ;
#14775=CARTESIAN_POINT ( 'NONE',  ( -19.09494877088048170, 33.54410563151299840, -142.1858765933287998 ) ) ;
#14781=CARTESIAN_POINT ( 'NONE',  ( -24.60556451751816454, 40.79665324755396227, -146.2317373473354394 ) ) ;
#14783=CARTESIAN_POINT ( 'NONE',  ( -15.03800142071511914, 35.98415342847451370, -148.3589868715107229 ) ) ;
#14786=CARTESIAN_POINT ( 'NONE',  ( -7.695630400395947923, 37.03895750127035313, -140.6427397355593030 ) ) ;
#14791=CARTESIAN_POINT ( 'NONE',  ( -5.543976733014329028, 40.02318592805595188, -142.2744635965945008 ) ) ;
#14802=CARTESIAN_POINT ( 'NONE',  ( -13.82353779674532035, 34.78290842721720111, -141.1681162278709962 ) ) ;
#14815=CARTESIAN_POINT ( 'NONE',  ( -28.35872823665358666, 34.75047554562008401, -147.1914172358262931 ) ) ;
#14819=CARTESIAN_POINT ( 'NONE',  ( -12.76754407576741990, 35.14623324252765002, -148.4212001205290221 ) ) ;
#14820=CARTESIAN_POINT ( 'NONE',  ( -10.36675979729999852, 34.52853970540000006, -140.3392284379999921 ) ) ;
#14827=CARTESIAN_POINT ( 'NONE',  ( -20.55310894649999653, 37.85259822169999921, -139.7937414779999870 ) ) ;
#14832=CARTESIAN_POINT ( 'NONE',  ( -24.50448663614206168, 36.99790949615556457, -147.3823814620965038 ) ) ;
#14840=CARTESIAN_POINT ( 'NONE',  ( -26.73151279747740006, 41.02465574082271615, -146.3859699704034085 ) ) ;
#14842=CARTESIAN_POINT ( 'NONE',  ( -22.37814652455998043, 32.77961379161537536, -141.5227465161630107 ) ) ;
#14850=CARTESIAN_POINT ( 'NONE',  ( -27.28682787397352172, 39.84701410126417898, -147.9146130286543439 ) ) ;
#14854=CARTESIAN_POINT ( 'NONE',  ( -7.010349701995939320, 37.05829245175783626, -148.1453878980124159 ) ) ;
#14863=CARTESIAN_POINT ( 'NONE',  ( -12.13433848750514166, 40.98455321840125976, -141.8124549635463438 ) ) ;
#14865=CARTESIAN_POINT ( 'NONE',  ( -17.97686571119999854, 41.53571570570000659, -143.4577736070000071 ) ) ;
#14868=CARTESIAN_POINT ( 'NONE',  ( -6.227860603739999945, 35.34754625490000279, -147.7419925389999946 ) ) ;
#14873=CARTESIAN_POINT ( 'NONE',  ( -28.07061429630000049, 34.82490105569999628, -147.0351741510000068 ) ) ;
#14875=CARTESIAN_POINT ( 'NONE',  ( -20.84895621120898923, 41.79397058805413678, -144.6400553131143170 ) ) ;
#14877=CARTESIAN_POINT ( 'NONE',  ( -28.42317279839999955, 33.35748734759999934, -144.4144508710000139 ) ) ;
#14897=CARTESIAN_POINT ( 'NONE',  ( -18.52830673193259514, 34.28760034481967978, -147.9573921617513577 ) ) ;
#14901=CARTESIAN_POINT ( 'NONE',  ( -23.55797472130712222, 40.74841938826056520, -146.3388075606171981 ) ) ;
#14902=CARTESIAN_POINT ( 'NONE',  ( -15.35800208497430930, 33.25688119014312605, -145.9433539410966887 ) ) ;
#14905=CARTESIAN_POINT ( 'NONE',  ( -19.68771884990000132, 32.54972883539999629, -143.8405663050000101 ) ) ;
#14909=CARTESIAN_POINT ( 'NONE',  ( -5.895487218599030577, 38.46663302055699774, -147.4545603117625205 ) ) ;
#14915=CARTESIAN_POINT ( 'NONE',  ( -21.13851658203423867, 36.11334442967607572, -147.9366295169849934 ) ) ;
#14918=CARTESIAN_POINT ( 'NONE',  ( -13.26154605881311532, 33.84108359974723612, -142.3203849960127627 ) ) ;
#14927=CARTESIAN_POINT ( 'NONE',  ( -27.36723106709627729, 36.02973761862455859, -148.4771530685292191 ) ) ;
#14931=CARTESIAN_POINT ( 'NONE',  ( -9.944031889410000602, 32.62729151690000151, -143.2983400859999961 ) ) ;
#14939=CARTESIAN_POINT ( 'NONE',  ( -21.61577042763667578, 39.11111834142336363, -146.9311419176080733 ) ) ;
#14940=EDGE_CURVE ( 'NONE', #13908, #12438, #6005, .T. ) ;
#14951=CARTESIAN_POINT ( 'NONE',  ( -27.20920484747068713, 39.08183102471901549, -146.8889507634862071 ) ) ;
#14953=CARTESIAN_POINT ( 'NONE',  ( -22.47466675763224231, 32.97119510217613936, -146.3662674461704967 ) ) ;
#14957=PRODUCT_CONTEXT ( 'NONE', #23319, 'mechanical' ) ;
#14960=CARTESIAN_POINT ( 'NONE',  ( -14.21887350769999969, 37.71951061619999734, -140.5431489169999963 ) ) ;
#14965=CARTESIAN_POINT ( 'NONE',  ( -7.774431620203307247, 38.87593842133829725, -139.9151280782420486 ) ) ;
#14966=ORIENTED_EDGE ( 'NONE', *, *, #5903, .F. ) ;
#14972=CARTESIAN_POINT ( 'NONE',  ( -11.97832217620000073, 39.59660284089999749, -147.8163995769999985 ) ) ;
#14978=CARTESIAN_POINT ( 'NONE',  ( -30.41918043656676574, 40.92081927820395038, -146.2642377558170494 ) ) ;
#14982=EDGE_LOOP ( 'NONE', ( #3005, #6591, #16961, #16213 ) ) ;
#14984=CARTESIAN_POINT ( 'NONE',  ( -20.83134323208084027, 41.14286042260535936, -141.6931026970137850 ) ) ;
#14986=CARTESIAN_POINT ( 'NONE',  ( -27.59585739157013151, 36.27528467301697646, -147.4543200874812214 ) ) ;
#14995=CARTESIAN_POINT ( 'NONE',  ( -20.61753010269739406, 36.92891383027767205, -140.0927360959155692 ) ) ;
#15001=CARTESIAN_POINT ( 'NONE',  ( -29.95441468910000182, 40.29796007080000209, -145.3430615500000158 ) ) ;
#15005=CARTESIAN_POINT ( 'NONE',  ( -22.52780672249999938, 37.05898997719999954, -140.0074087190000114 ) ) ;
#15010=CARTESIAN_POINT ( 'NONE',  ( -25.01023491195180881, 37.91851060511771720, -148.1495535101706480 ) ) ;
#15013=CARTESIAN_POINT ( 'NONE',  ( -16.54277457342332269, 34.95491693752516227, -141.0331736024299971 ) ) ;
#15018=CARTESIAN_POINT ( 'NONE',  ( -6.183234097834880316, 41.28010592191888151, -143.5033826244021782 ) ) ;
#15021=CARTESIAN_POINT ( 'NONE',  ( -23.19912457534285366, 34.77544957999561603, -141.0327754292524389 ) ) ;
#15025=ORIENTED_EDGE ( 'NONE', *, *, #19867, .T. ) ;
#15026=CARTESIAN_POINT ( 'NONE',  ( -12.58047663530000015, 34.35960099889999952, -147.8017659109999897 ) ) ;
#15034=CARTESIAN_POINT ( 'NONE',  ( -28.42317279839999955, 33.35748734759999934, -144.4144508710000139 ) ) ;
#15036=EDGE_CURVE ( 'NONE', #3155, #14150, #21524, .T. ) ;
#15040=CARTESIAN_POINT ( 'NONE',  ( -6.033650297970000409, 36.94170754819999303, -147.9652040070000112 ) ) ;
#15050=CARTESIAN_POINT ( 'NONE',  ( -21.19005019800000156, 41.30866696430000218, -143.6114845980000041 ) ) ;
#15063=CARTESIAN_POINT ( 'NONE',  ( -25.95437585267248082, 39.65968214943575987, -140.4458241776663954 ) ) ;
#15073=CARTESIAN_POINT ( 'NONE',  ( -27.77832206610000298, 37.03059619289999915, -147.6270870419999710 ) ) ;
#15074=CARTESIAN_POINT ( 'NONE',  ( -15.00140173379999986, 40.20535686069999315, -145.8913236320000237 ) ) ;
#15077=CARTESIAN_POINT ( 'NONE',  ( -7.010349701930000066, 37.05829245179999987, -148.1453878979999956 ) ) ;
#15078=CARTESIAN_POINT ( 'NONE',  ( -6.227860603739999945, 35.34754625490000279, -147.7419925389999946 ) ) ;
#15079=CARTESIAN_POINT ( 'NONE',  ( -8.514310886032820491, 36.94123471670531700, -140.1199228274701909 ) ) ;
#15083=CARTESIAN_POINT ( 'NONE',  ( -26.39607007120000048, 36.95534867429999792, -140.3840478969999879 ) ) ;
#15086=CARTESIAN_POINT ( 'NONE',  ( -10.86836323999999898, 38.91206754959999614, -139.9811931129999891 ) ) ;
#15087=CARTESIAN_POINT ( 'NONE',  ( -18.22769797923110957, 36.96487028399720742, -148.6596776398728821 ) ) ;
#15091=CARTESIAN_POINT ( 'NONE',  ( -7.324031428439999658, 35.31041870520000003, -140.2046280479999893 ) ) ;
#15095=CARTESIAN_POINT ( 'NONE',  ( -27.97684248819999908, 35.51254237909999745, -147.4365014880000047 ) ) ;
#15100=CARTESIAN_POINT ( 'NONE',  ( -21.42908239836678774, 38.93534789603918966, -148.4669439360840784 ) ) ;
#15126=EDGE_CURVE ( 'NONE', #7237, #2371, #6770, .T. ) ;
#15127=CARTESIAN_POINT ( 'NONE',  ( -24.22314457607379623, 36.96432676151304264, -148.6204621725955519 ) ) ;
#15130=CARTESIAN_POINT ( 'NONE',  ( -15.57039528535599970, 36.22627288623296238, -147.5570433397527665 ) ) ;
#15131=CARTESIAN_POINT ( 'NONE',  ( -16.48516879800526169, 34.41988679506793858, -147.5123417674411144 ) ) ;
#15136=CARTESIAN_POINT ( 'NONE',  ( -5.450498087531185476, 40.62522382734958626, -144.4475518853465701 ) ) ;
#15143=CARTESIAN_POINT ( 'NONE',  ( -22.21135766849999982, 35.30661492690000358, -147.9492090369999744 ) ) ;
#15146=CARTESIAN_POINT ( 'NONE',  ( -12.64961778247436897, 33.30795510890303746, -144.5205897159969481 ) ) ;
#15156=CARTESIAN_POINT ( 'NONE',  ( -28.06178240312047834, 37.06443177824845492, -147.7991814974922420 ) ) ;
#15161=CARTESIAN_POINT ( 'NONE',  ( -14.58163105951714655, 36.93319896292500459, -139.6872257169340514 ) ) ;
#15169=CARTESIAN_POINT ( 'NONE',  ( -30.02199999990000023, 40.03108891319999429, -145.8052959529999839 ) ) ;
#15171=CARTESIAN_POINT ( 'NONE',  ( -20.66421688137213053, 40.12815996892139481, -145.9609113517520029 ) ) ;
#15178=CARTESIAN_POINT ( 'NONE',  ( -25.55414838373298991, 33.45093896582719140, -143.7269752718342488 ) ) ;
#15188=CARTESIAN_POINT ( 'NONE',  ( -27.29941367908698524, 38.43084994578902069, -147.2672509616508307 ) ) ;
#15191=ORIENTED_EDGE ( 'NONE', *, *, #826, .T. ) ;
#15195=CARTESIAN_POINT ( 'NONE',  ( -27.90252014676526926, 38.00321959428593743, -148.5304241855687906 ) ) ;
#15202=CARTESIAN_POINT ( 'NONE',  ( -6.697072761360190363, 32.84210578784889378, -146.5313758896071477 ) ) ;
#15204=CARTESIAN_POINT ( 'NONE',  ( -8.585705256233374882, 39.77515751163792146, -140.1536556790775023 ) ) ;
#15214=CARTESIAN_POINT ( 'NONE',  ( -12.45288479873165954, 40.94156371644511694, -144.5313000001702619 ) ) ;
#15228=CARTESIAN_POINT ( 'NONE',  ( -20.32722469806098076, 41.69472958972785648, -143.6736157908201790 ) ) ;
#15229=VERTEX_POINT ( 'NONE', #11230 ) ;
#15230=CARTESIAN_POINT ( 'NONE',  ( -28.24106514979908056, 36.25312149646672566, -140.0297965533989384 ) ) ;
#15244=CARTESIAN_POINT ( 'NONE',  ( -30.02199999990000023, 40.03108891319999429, -145.8052959529999839 ) ) ;
#15252=CARTESIAN_POINT ( 'NONE',  ( -24.46575914854654243, 41.11257952955785555, -146.4371654771300086 ) ) ;
#15262=CARTESIAN_POINT ( 'NONE',  ( -9.697321561110106458, 33.26273935370599588, -144.1849952531234180 ) ) ;
#15266=( BOUNDED_CURVE ( )  B_SPLINE_CURVE ( 5, ( #6558, #13825, #8455, #10113, #21088, #13699 ),
 .UNSPECIFIED., .F., .F. ) 
 B_SPLINE_CURVE_WITH_KNOTS ( ( 6, 6 ),
 ( 1.570796326447242430, 3.141592653590000062 ),
 .UNSPECIFIED. ) 
 CURVE ( )  GEOMETRIC_REPRESENTATION_ITEM ( )  RATIONAL_B_SPLINE_CURVE ( ( 0.2500000000000000000, 0.2499999999557221131, 0.2999999999335831724, 0.3999999999114442484, 0.5999999999114442595, 1.000000000000000000 ) ) 
 REPRESENTATION_ITEM ( '' )  );
#15269=FACE_OUTER_BOUND ( 'NONE', #7561, .T. ) ;
#15275=CARTESIAN_POINT ( 'NONE',  ( -13.60030749279999895, 34.19157895370000233, -140.3499153360000093 ) ) ;
#15276=CARTESIAN_POINT ( 'NONE',  ( -16.35051094565787366, 37.08015310164943656, -139.9332297720364977 ) ) ;
#15280=CARTESIAN_POINT ( 'NONE',  ( -9.072898850179999641, 36.94639249900000522, -148.2684494029999769 ) ) ;
#15281=CARTESIAN_POINT ( 'NONE',  ( -7.828824709450000086, 39.51093879980000168, -140.6700787229999889 ) ) ;
#15284=( LENGTH_UNIT ( ) NAMED_UNIT ( * ) SI_UNIT ( .MILLI., .METRE. ) );
#15286=CARTESIAN_POINT ( 'NONE',  ( -14.47796399077968310, 35.98708302378778967, -139.7013159814367782 ) ) ;
#15295=CARTESIAN_POINT ( 'NONE',  ( -20.41826969035592754, 40.54732898170615840, -143.7678329423778223 ) ) ;
#15297=CARTESIAN_POINT ( 'NONE',  ( -18.28711887264178060, 38.42777126315955627, -147.2271535123214790 ) ) ;
#15301=CARTESIAN_POINT ( 'NONE',  ( -25.27079369000000142, 34.74837955689999802, -147.2605407199999945 ) ) ;
#15312=ORIENTED_EDGE ( 'NONE', *, *, #14006, .T. ) ;
#15321=CARTESIAN_POINT ( 'NONE',  ( -9.870393330222821504, 37.85345449821588204, -147.8311166188136099 ) ) ;
#15328=CARTESIAN_POINT ( 'NONE',  ( -18.18930989805799925, 36.96028804432503989, -147.6841622078449916 ) ) ;
#15339=CARTESIAN_POINT ( 'NONE',  ( -25.61321927598924475, 33.33310017243326229, -146.2757612383772710 ) ) ;
#15357=CARTESIAN_POINT ( 'NONE',  ( -30.68396739435298670, 40.64794745105150753, -146.0701989576813844 ) ) ;
#15368=CARTESIAN_POINT ( 'NONE',  ( -16.37184312240000139, 32.37338091950000063, -144.3414871020000021 ) ) ;
#15374=CARTESIAN_POINT ( 'NONE',  ( -10.75221293964388103, 33.20739279112564191, -143.4848104349948130 ) ) ;
#15379=CARTESIAN_POINT ( 'NONE',  ( -21.73453520643527881, 32.91403690840683538, -144.3663112597812130 ) ) ;
#15382=CARTESIAN_POINT ( 'NONE',  ( -22.73109880836567953, 38.77532135900968058, -140.2559096062584274 ) ) ;
#15386=CARTESIAN_POINT ( 'NONE',  ( -10.17933436543764003, 35.38122503070080427, -147.6311798951892058 ) ) ;
#15388=CARTESIAN_POINT ( 'NONE',  ( -7.888511564689155264, 38.45496397857106530, -140.8398455980544099 ) ) ;
#15394=CARTESIAN_POINT ( 'NONE',  ( -12.58047663530000015, 34.35960099889999952, -147.8017659109999897 ) ) ;
#15397=( BOUNDED_SURFACE ( )  B_SPLINE_SURFACE ( 5, 5, ( 
 ( #13036, #20306, #10279, #1146, #3042, #6594 ),
 ( #11821, #22909, #17189, #15649, #15521, #17550 ),
 ( #21007, #4698, #4345, #9914, #20889, #11579 ),
 ( #11939, #8376, #10030, #2917, #17306, #10149 ),
 ( #22552, #17422, #15404, #11698, #13857, #21125 ),
 ( #4578, #1268, #19330, #6243, #6357, #4816 ),
 ( #12059, #19095, #13492, #1020, #906, #8491 ),
 ( #18856, #19205, #15761, #23022, #6708, #13970 ),
 ( #2800, #2568, #9790, #17067, #18974, #788 ),
 ( #8014, #15297, #13613, #20766, #4459, #2687 ),
 ( #8247, #8132, #22783, #22662, #6483, #13742 ),
 ( #4936, #16117, #1372, #6830, #19922, #3621 ) ),
 .UNSPECIFIED., .F., .F., .F. ) 
 B_SPLINE_SURFACE_WITH_KNOTS ( ( 6, 3, 3, 6 ),
 ( 6, 6 ),
 ( 0.000000000000000000, 4.124045064660000648, 8.344666563069999654, 12.67057240369999960 ),
 ( 1.570796326600514936, 3.141592653590000062 ),
 .UNSPECIFIED. ) 
 GEOMETRIC_REPRESENTATION_ITEM ( )  RATIONAL_B_SPLINE_SURFACE ( (
 ( 0.2500000000000000000, 0.2499999999752375024, 0.2999999999628560343, 0.3999999999504744719, 0.5999999999504750381, 1.000000000000000000),
 ( 0.2500000000000000000, 0.2499999999752375024, 0.2999999999628560343, 0.3999999999504744719, 0.5999999999504750381, 1.000000000000000000),
 ( 0.2500000000000000000, 0.2499999999752375024, 0.2999999999628560343, 0.3999999999504744719, 0.5999999999504750381, 1.000000000000000000),
 ( 0.2500000000000000000, 0.2499999999752375024, 0.2999999999628560343, 0.3999999999504744719, 0.5999999999504750381, 1.000000000000000000),
 ( 0.2500000000000000000, 0.2499999999752375024, 0.2999999999628560343, 0.3999999999504744719, 0.5999999999504750381, 1.000000000000000000),
 ( 0.2500000000000000000, 0.2499999999752375024, 0.2999999999628560343, 0.3999999999504744719, 0.5999999999504750381, 1.000000000000000000),
 ( 0.2500000000000000000, 0.2499999999752375024, 0.2999999999628560343, 0.3999999999504744719, 0.5999999999504750381, 1.000000000000000000),
 ( 0.2500000000000000000, 0.2499999999752375024, 0.2999999999628560343, 0.3999999999504744719, 0.5999999999504750381, 1.000000000000000000),
 ( 0.2500000000000000000, 0.2499999999752375024, 0.2999999999628560343, 0.3999999999504744719, 0.5999999999504750381, 1.000000000000000000),
 ( 0.2500000000000000000, 0.2499999999752375024, 0.2999999999628560343, 0.3999999999504744719, 0.5999999999504750381, 1.000000000000000000),
 ( 0.2500000000000000000, 0.2499999999752375024, 0.2999999999628560343, 0.3999999999504744719, 0.5999999999504750381, 1.000000000000000000),
 ( 0.2500000000000000000, 0.2499999999752375024, 0.2999999999628560343, 0.3999999999504744719, 0.5999999999504750381, 1.000000000000000000) ) ) 
 REPRESENTATION_ITEM ( '' )  SURFACE ( )  );
#15400=CARTESIAN_POINT ( 'NONE',  ( -14.45813593939999997, 41.09907220950000095, -141.6721478100000127 ) ) ;
#15404=CARTESIAN_POINT ( 'NONE',  ( -18.01907198844549995, 40.17100866524817349, -142.0952484789442849 ) ) ;
#15407=CARTESIAN_POINT ( 'NONE',  ( -24.20244548955877661, 34.61374440578268974, -147.2354883249831516 ) ) ;
#15414=CARTESIAN_POINT ( 'NONE',  ( -26.82473810827688254, 37.81866192723410336, -148.2916060357279378 ) ) ;
#15426=CARTESIAN_POINT ( 'NONE',  ( -7.052957782236454420, 32.23883816114348377, -143.6422217563765287 ) ) ;
#15444=CARTESIAN_POINT ( 'NONE',  ( -14.90221424347422818, 38.57597971860518982, -140.2753094542739802 ) ) ;
#15446=CARTESIAN_POINT ( 'NONE',  ( -25.86608305657696860, 32.48195522393204016, -143.6651831558542369 ) ) ;
#15447=EDGE_CURVE ( 'NONE', #19550, #8868, #399, .T. ) ;
#15457=ORIENTED_EDGE ( 'NONE', *, *, #15126, .T. ) ;
#15478=CARTESIAN_POINT ( 'NONE',  ( -16.36784392973273938, 33.86562477380443426, -142.0582287347409931 ) ) ;
#15483=CARTESIAN_POINT ( 'NONE',  ( -7.529689113779999943, 37.05876528330000497, -139.9906690790000141 ) ) ;
#15485=CARTESIAN_POINT ( 'NONE',  ( -9.948438925625499252, 33.43836456409815838, -141.7026862686744835 ) ) ;
#15495=CARTESIAN_POINT ( 'NONE',  ( -23.40625992182578941, 38.40432287900232922, -140.8828493825280361 ) ) ;
#15503=CARTESIAN_POINT ( 'NONE',  ( -9.971101149527340723, 37.05360750091212196, -147.8421425029205807 ) ) ;
#15512=CARTESIAN_POINT ( 'NONE',  ( -7.015833805750000707, 33.30032478630000270, -141.9582197170000200 ) ) ;
#15513=CARTESIAN_POINT ( 'NONE',  ( -26.73151279740000064, 41.02465574069999121, -146.3859699699999908 ) ) ;
#15514=CARTESIAN_POINT ( 'NONE',  ( -21.70878449369999785, 39.52018264390000013, -147.4849246469999855 ) ) ;
#15517=CARTESIAN_POINT ( 'NONE',  ( -15.47708384459999920, 37.95279615419999431, -148.5507537150000132 ) ) ;
#15520=CARTESIAN_POINT ( 'NONE',  ( -20.84101097267440039, 38.55092845031688142, -147.7610021335696047 ) ) ;
#15521=CARTESIAN_POINT ( 'NONE',  ( -17.62617954421223132, 37.82805002212005974, -139.7243320108600813 ) ) ;
#15526=CARTESIAN_POINT ( 'NONE',  ( -24.00819484748617327, 36.12951795105237096, -147.8708185612008208 ) ) ;
#15543=CARTESIAN_POINT ( 'NONE',  ( -18.90246017563120162, 37.04541408822156967, -147.4848489021858313 ) ) ;
#15546=CARTESIAN_POINT ( 'NONE',  ( -7.296416894500538319, 32.72008036306245771, -141.6746418080609828 ) ) ;
#15548=CARTESIAN_POINT ( 'NONE',  ( -9.852708451402975243, 38.00872972452032883, -148.5766935762293031 ) ) ;
#15554=CARTESIAN_POINT ( 'NONE',  ( -14.11967125440000004, 36.98834135279999913, -140.5455248810000057 ) ) ;
#15568=FACE_OUTER_BOUND ( 'NONE', #12226, .T. ) ;
#15570=CARTESIAN_POINT ( 'NONE',  ( -26.01424353331992734, 34.14238437626309519, -140.2248994934187181 ) ) ;
#15584=CARTESIAN_POINT ( 'NONE',  ( -24.57863953949999924, 33.12365565980000071, -146.2648171790000049 ) ) ;
#15592=CARTESIAN_POINT ( 'NONE',  ( -21.63220705389140619, 37.01315499805642162, -148.7192284428339804 ) ) ;
#15594=CARTESIAN_POINT ( 'NONE',  ( -14.47497890702397605, 41.61557973986633385, -144.5624617423342784 ) ) ;
#15603=ORIENTED_EDGE ( 'NONE', *, *, #20145, .F. ) ;
#15622=CARTESIAN_POINT ( 'NONE',  ( -23.81889237380000068, 39.38287674749999923, -140.7489234159999967 ) ) ;
#15631=EDGE_CURVE ( 'NONE', #22408, #15229, #19084, .T. ) ;
#15635=CARTESIAN_POINT ( 'NONE',  ( -6.131111726649999483, 36.14321585209999910, -147.9535578170000178 ) ) ;
#15649=CARTESIAN_POINT ( 'NONE',  ( -17.78798770263510320, 37.73719101445376367, -140.0682257265029023 ) ) ;
#15654=CARTESIAN_POINT ( 'NONE',  ( -24.84704225925436916, 37.03879906168187830, -147.5513581853046219 ) ) ;
#15673=CARTESIAN_POINT ( 'NONE',  ( -18.46643761637815828, 34.84883242728916031, -147.1252693408089840 ) ) ;
#15677=CARTESIAN_POINT ( 'NONE',  ( -6.481896728065510871, 33.11542685677439124, -146.3378416582211230 ) ) ;
#15678=CARTESIAN_POINT ( 'NONE',  ( -10.14042191033886020, 37.07381867794361341, -148.2039739395295612 ) ) ;
#15689=ORIENTED_EDGE ( 'NONE', *, *, #9657, .T. ) ;
#15693=CARTESIAN_POINT ( 'NONE',  ( -14.83278250954328037, 40.60058613834879537, -144.4189779530036049 ) ) ;
#15694=CARTESIAN_POINT ( 'NONE',  ( -26.41286337068730461, 35.11800629833786047, -140.0118796628326834 ) ) ;
#15709=CARTESIAN_POINT ( 'NONE',  ( -15.27002291898349995, 38.46844526377720541, -147.3668459616200153 ) ) ;
#15719=CARTESIAN_POINT ( 'NONE',  ( -15.86130022171997389, 33.41189223525291396, -141.7054377170709927 ) ) ;
#15727=CARTESIAN_POINT ( 'NONE',  ( -10.56415788819999868, 36.18163687389999694, -139.7056672729999889 ) ) ;
#15732=CARTESIAN_POINT ( 'NONE',  ( -29.03767587600000155, 36.26045984259999955, -140.5446710220000170 ) ) ;
#15735=CARTESIAN_POINT ( 'NONE',  ( -23.90246201272782400, 40.41935502004460545, -144.4616775445051644 ) ) ;
#15750=CARTESIAN_POINT ( 'NONE',  ( -6.993473002926046789, 35.65312348993318636, -147.2648311488452748 ) ) ;
#15751=CARTESIAN_POINT ( 'NONE',  ( -26.16983372440000011, 40.98399646770000260, -141.7700373849999949 ) ) ;
#15753=CARTESIAN_POINT ( 'NONE',  ( -22.00705883600000234, 37.05789963359999462, -148.1619053240000028 ) ) ;
#15761=CARTESIAN_POINT ( 'NONE',  ( -18.43821035757416027, 40.21414801953198292, -145.7948256318368578 ) ) ;
#15764=CARTESIAN_POINT ( 'NONE',  ( -6.804059094464555812, 37.03366832433020761, -147.4295713063915230 ) ) ;
#15777=CARTESIAN_POINT ( 'NONE',  ( -28.52142019845012655, 37.05975231236342182, -139.6605181375830682 ) ) ;
#15780=CARTESIAN_POINT ( 'NONE',  ( -16.81794493339999619, 37.02435727940000731, -140.5111119820000170 ) ) ;
#15782=CARTESIAN_POINT ( 'NONE',  ( -11.68420994734520235, 39.25205177024059822, -141.0178453344531988 ) ) ;
#15805=CARTESIAN_POINT ( 'NONE',  ( -26.19803085470000070, 35.41001212129999942, -140.6029839040000127 ) ) ;
#15815=CARTESIAN_POINT ( 'NONE',  ( -24.90252082150000135, 32.60880315500000393, -143.5690609609999910 ) ) ;
#15820=CARTESIAN_POINT ( 'NONE',  ( -14.02405267930000043, 37.94700976039999318, -139.5674429869999926 ) ) ;
#15831=CARTESIAN_POINT ( 'NONE',  ( -16.26018138119240675, 34.43780680547004636, -140.2208411054963619 ) ) ;
#15839=CARTESIAN_POINT ( 'NONE',  ( -25.64408091310000160, 33.16124342930000068, -144.5387451670000019 ) ) ;
#15841=CARTESIAN_POINT ( 'NONE',  ( -28.90798551742755862, 37.01360947635620136, -139.5686590453623808 ) ) ;
#15845=CARTESIAN_POINT ( 'NONE',  ( -13.49610831274083189, 36.09202739918482195, -139.6200137135016064 ) ) ;
#15851=CARTESIAN_POINT ( 'NONE',  ( -10.28506259363968844, 34.15285781884922045, -147.7829287822364961 ) ) ;
#15855=CARTESIAN_POINT ( 'NONE',  ( -8.743032712512970761, 39.11948877732287144, -147.0257656743172845 ) ) ;
#15860=CARTESIAN_POINT ( 'NONE',  ( -7.249489785462221114, 33.98920719456333472, -145.9090368077603443 ) ) ;
#15861=CARTESIAN_POINT ( 'NONE',  ( -22.62924774399999706, 37.91877106609999970, -140.0196664479999811 ) ) ;
#15893=CARTESIAN_POINT ( 'NONE',  ( -8.810109936750000870, 39.32487244789999892, -140.7337397739999858 ) ) ;
#15896=CARTESIAN_POINT ( 'NONE',  ( -7.220568065030000149, 34.52259161599999970, -140.6708207100000152 ) ) ;
#15897=EDGE_CURVE ( 'NONE', #19149, #10191, #23047, .T. ) ;
#15914=CARTESIAN_POINT ( 'NONE',  ( -11.97832217620000073, 39.59660284089999749, -147.8163995769999985 ) ) ;
#15916=CARTESIAN_POINT ( 'NONE',  ( -15.66511667654221718, 38.49419402878272933, -147.3083789397792316 ) ) ;
#15942=CARTESIAN_POINT ( 'NONE',  ( -14.64556842670265802, 38.56874084764600497, -147.7756864782241166 ) ) ;
#15944=ORIENTED_EDGE ( 'NONE', *, *, #1474, .T. ) ;
#15950=CARTESIAN_POINT ( 'NONE',  ( -24.84704225926845922, 37.03879906168354097, -147.5513581853375058 ) ) ;
#15958=CARTESIAN_POINT ( 'NONE',  ( -6.705189174532299567, 39.56570632385503927, -147.4373625593833879 ) ) ;
#15976=CARTESIAN_POINT ( 'NONE',  ( -10.13678785082237077, 32.34748245543284639, -143.2747856603235732 ) ) ;
#15977=CARTESIAN_POINT ( 'NONE',  ( -17.91974642295373599, 36.92811127467410159, -148.3783205066400797 ) ) ;
#15985=CARTESIAN_POINT ( 'NONE',  ( -6.578755062799197084, 35.62001169219931995, -147.2160746728349920 ) ) ;
#15993=CARTESIAN_POINT ( 'NONE',  ( -17.01025018560000035, 38.48180121059999692, -140.7067500819999850 ) ) ;
#16010=CARTESIAN_POINT ( 'NONE',  ( -16.26554697147297190, 36.25315601839098889, -147.8310094943498711 ) ) ;
#16011=CARTESIAN_POINT ( 'NONE',  ( -28.14969746252968008, 32.41805236243940413, -143.4814202872574072 ) ) ;
#16020=CARTESIAN_POINT ( 'NONE',  ( -19.07874927058154668, 33.55317438757552395, -144.5781697712094171 ) ) ;
#16029=( BOUNDED_CURVE ( )  B_SPLINE_CURVE ( 5, ( #16410, #5348, #17840, #10792, #18075, #8777, #14513, #10679, #3798, #7125, #14387, #5103 ),
 .UNSPECIFIED., .F., .F. ) 
 B_SPLINE_CURVE_WITH_KNOTS ( ( 6, 3, 3, 6 ),
 ( 0.000000000000000000, 4.358589029760000066, 8.533830367689999363, 12.54112731390000057 ),
 .UNSPECIFIED. ) 
 CURVE ( )  GEOMETRIC_REPRESENTATION_ITEM ( )  RATIONAL_B_SPLINE_CURVE ( ( 0.2500000000000000000, 0.2500000000000000000, 0.2500000000000000000, 0.2500000000000000000, 0.2500000000000000000, 0.2500000000000000000, 0.2500000000000000000, 0.2500000000000000000, 0.2500000000000000000, 0.2500000000000000000, 0.2500000000000000000, 0.2500000000000000000 ) ) 
 REPRESENTATION_ITEM ( '' )  );
#16042=CARTESIAN_POINT ( 'NONE',  ( -16.16658683009993069, 37.07694188521394096, -148.2333767341113742 ) ) ;
#16048=CARTESIAN_POINT ( 'NONE',  ( -26.81163552868969191, 38.56513266870371837, -140.3212796651035319 ) ) ;
#16062=CARTESIAN_POINT ( 'NONE',  ( -13.50483231551108609, 37.84550326251047636, -140.3648548379449892 ) ) ;
#16078=CARTESIAN_POINT ( 'NONE',  ( -13.13790626639999992, 32.38985286280000508, -143.7114742199999853 ) ) ;
#16080=CARTESIAN_POINT ( 'NONE',  ( -5.268406987068996017, 41.62455876149470413, -143.5667302874617235 ) ) ;
#16083=ORIENTED_EDGE ( 'NONE', *, *, #14940, .T. ) ;
#16084=CARTESIAN_POINT ( 'NONE',  ( -26.39607007120000048, 36.95534867429999792, -140.3840478969999879 ) ) ;
#16092=CARTESIAN_POINT ( 'NONE',  ( -29.43227084506111879, 38.18732975763461468, -139.4730824933273539 ) ) ;
#16096=CARTESIAN_POINT ( 'NONE',  ( -10.88504013576124585, 37.01634837950538071, -139.4704149077313673 ) ) ;
#16099=CARTESIAN_POINT ( 'NONE',  ( -8.931798216462233597, 36.92954985151496317, -147.9669232058025159 ) ) ;
#16113=FACE_OUTER_BOUND ( 'NONE', #19111, .T. ) ;
#16115=ORIENTED_EDGE ( 'NONE', *, *, #1122, .F. ) ;
#16117=CARTESIAN_POINT ( 'NONE',  ( -18.48412402378637864, 36.99547888838029053, -147.4161207264589564 ) ) ;
#16122=CARTESIAN_POINT ( 'NONE',  ( -25.46206384013188284, 37.06683745572571098, -140.4480127386118511 ) ) ;
#16135=CARTESIAN_POINT ( 'NONE',  ( -12.66605126736717679, 36.07579439668360521, -148.6554523513628681 ) ) ;
#16141=CARTESIAN_POINT ( 'NONE',  ( -20.23971019809999916, 35.09018026569999904, -140.0771129649999978 ) ) ;
#16142=CARTESIAN_POINT ( 'NONE',  ( -11.42599417689999974, 41.52668172479999953, -143.7505393120000292 ) ) ;
#16162=CARTESIAN_POINT ( 'NONE',  ( -16.06600907547494828, 37.95602789737367289, -148.2176118107361162 ) ) ;
#16167=CARTESIAN_POINT ( 'NONE',  ( -26.68542098469999857, 39.18140699330000132, -140.9632721460000084 ) ) ;
#16171=( BOUNDED_CURVE ( )  B_SPLINE_CURVE ( 5, ( #21365, #3262, #15993, #21717, #23371, #16353, #23136, #56, #5406, #5156, #19807, #7306 ),
 .UNSPECIFIED., .F., .F. ) 
 B_SPLINE_CURVE_WITH_KNOTS ( ( 6, 3, 3, 6 ),
 ( 0.000000000000000000, 4.124045064660000648, 8.344666563069999654, 12.67057240369999782 ),
 .UNSPECIFIED. ) 
 CURVE ( )  GEOMETRIC_REPRESENTATION_ITEM ( )  RATIONAL_B_SPLINE_CURVE ( ( 0.2500000000000000000, 0.2500000000000000000, 0.2500000000000000000, 0.2500000000000000000, 0.2500000000000000000, 0.2500000000000000000, 0.2500000000000000000, 0.2500000000000000000, 0.2500000000000000000, 0.2500000000000000000, 0.2500000000000000000, 0.2500000000000000000 ) ) 
 REPRESENTATION_ITEM ( '' )  );
#16181=CARTESIAN_POINT ( 'NONE',  ( -16.65675009045287069, 37.97791044233296276, -139.5816482416001350 ) ) ;
#16183=VERTEX_POINT ( 'NONE', #14769 ) ;
#16196=CARTESIAN_POINT ( 'NONE',  ( -13.02237250279999969, 32.42872598539999274, -144.6889042450000034 ) ) ;
#16198=CARTESIAN_POINT ( 'NONE',  ( -4.875412749849999727, 39.32116320210000282, -140.9191069839999955 ) ) ;
#16203=ORIENTED_EDGE ( 'NONE', *, *, #7015, .F. ) ;
#16208=ORIENTED_EDGE ( 'NONE', *, *, #195, .F. ) ;
#16213=ORIENTED_EDGE ( 'NONE', *, *, #17582, .F. ) ;
#16215=CARTESIAN_POINT ( 'NONE',  ( -18.11332094088754729, 35.20436099510112626, -148.1391246873896534 ) ) ;
#16216=CARTESIAN_POINT ( 'NONE',  ( -8.245186567769970054, 40.93572612369973029, -144.5056815551646139 ) ) ;
#16221=ADVANCED_FACE ( 'NONE', ( #2059 ), #11912, .F. ) ;
#16250=ORIENTED_EDGE ( 'NONE', *, *, #15036, .T. ) ;
#16253=EDGE_LOOP ( 'NONE', ( #1668, #8678, #7432, #16394 ) ) ;
#16279=CARTESIAN_POINT ( 'NONE',  ( -21.05404274330185288, 36.02007484894763678, -148.3253262703269399 ) ) ;
#16280=CARTESIAN_POINT ( 'NONE',  ( -29.47785954729999958, 39.65718555499999809, -141.4786507110000287 ) ) ;
#16294=CARTESIAN_POINT ( 'NONE',  ( -14.11967125440000004, 36.98834135279999913, -140.5455248810000057 ) ) ;
#16295=CARTESIAN_POINT ( 'NONE',  ( -28.99249306591901032, 33.68760113747161000, -142.1526180105009871 ) ) ;
#16300=CARTESIAN_POINT ( 'NONE',  ( -17.42663577349999926, 38.80963643279999786, -139.8270276149999916 ) ) ;
#16314=CARTESIAN_POINT ( 'NONE',  ( -5.642215125958555788, 41.80899724057998412, -143.5028856654435003 ) ) ;
#16328=CARTESIAN_POINT ( 'NONE',  ( -30.45874311816843516, 41.26340968600602110, -144.2604718650849520 ) ) ;
#16330=CARTESIAN_POINT ( 'NONE',  ( -21.23917607309999767, 35.28761490579999816, -147.7082871199999943 ) ) ;
#16334=CARTESIAN_POINT ( 'NONE',  ( -19.28863050619207087, 36.17828169457454379, -139.9441849802047955 ) ) ;
#16340=ORIENTED_EDGE ( 'NONE', *, *, #8654, .T. ) ;
#16353=CARTESIAN_POINT ( 'NONE',  ( -17.44989882389999991, 40.67283837529999602, -143.6255418399999826 ) ) ;
#16378=CARTESIAN_POINT ( 'NONE',  ( -20.30489103444976351, 34.41680263911344895, -140.8326631860697091 ) ) ;
#16394=ORIENTED_EDGE ( 'NONE', *, *, #6416, .F. ) ;
#16395=CARTESIAN_POINT ( 'NONE',  ( -26.86882954950000268, 40.29793777999999804, -142.0811670120000088 ) ) ;
#16398=CARTESIAN_POINT ( 'NONE',  ( -15.86078924153199310, 37.04043998683727779, -147.5134597624270612 ) ) ;
#16410=CARTESIAN_POINT ( 'NONE',  ( -15.46613156839999981, 36.99333119719999985, -147.5584717940000132 ) ) ;
#16418=CARTESIAN_POINT ( 'NONE',  ( -17.06385656868887324, 41.33018260709537373, -143.5869266124798855 ) ) ;
#16428=EDGE_CURVE ( 'NONE', #11114, #4660, #19856, .T. ) ;
#16430=EDGE_LOOP ( 'NONE', ( #4009, #113, #2969, #5065 ) ) ;
#16435=CARTESIAN_POINT ( 'NONE',  ( -6.356911216211141635, 38.98543411609163911, -148.4775420273327597 ) ) ;
#16444=CARTESIAN_POINT ( 'NONE',  ( -23.48449349015690046, 36.94479390616788095, -140.4349842069357521 ) ) ;
#16445=CARTESIAN_POINT ( 'NONE',  ( -30.03413168677343492, 40.19007108948994045, -140.8797962025610104 ) ) ;
#16449=CARTESIAN_POINT ( 'NONE',  ( -19.28609856413475754, 34.66429844331295840, -140.9609051183012127 ) ) ;
#16453=CARTESIAN_POINT ( 'NONE',  ( -23.02245220108656909, 38.00600600913553961, -139.3782448799144618 ) ) ;
#16461=CARTESIAN_POINT ( 'NONE',  ( -6.807579269534479671, 38.78453684425459613, -147.8970667730299908 ) ) ;
#16472=CARTESIAN_POINT ( 'NONE',  ( -13.40552595227777211, 37.07358616897466419, -140.3498584192782062 ) ) ;
#16477=VERTEX_POINT ( 'NONE', #17257 ) ;
#16478=CARTESIAN_POINT ( 'NONE',  ( -16.63107678121195931, 35.60580843633908188, -140.6802342586736074 ) ) ;
#16479=CARTESIAN_POINT ( 'NONE',  ( -12.76385253868072134, 37.02886902027827887, -147.6186336933980101 ) ) ;
#16485=CARTESIAN_POINT ( 'NONE',  ( -19.79211671321127497, 32.85031535814157166, -144.7688754269952938 ) ) ;
#16499=CARTESIAN_POINT ( 'NONE',  ( -26.08236470951569785, 39.06228944650155199, -141.2475209953871342 ) ) ;
#16502=CARTESIAN_POINT ( 'NONE',  ( -22.42941481613483745, 36.22509709915611609, -139.9955747715279983 ) ) ;
#16507=( BOUNDED_SURFACE ( )  B_SPLINE_SURFACE ( 5, 5, ( 
 ( #4217, #15156, #5870, #2674, #22074, #22420 ),
 ( #9663, #6113, #20753, #11454, #4334, #14927 ),
 ( #17051, #9554, #4094, #11567, #13020, #18842 ),
 ( #6229, #14815, #18612, #13479, #539, #13129 ),
 ( #4446, #11682, #20401, #11328, #16829, #7771 ),
 ( #15034, #5988, #22298, #13244, #8464, #22992 ),
 ( #13942, #17396, #10470, #13833, #21096, #11791 ),
 ( #21214, #16295, #3013, #1114, #7249, #20856 ),
 ( #4904, #6679, #17516, #21334, #8570, #22752 ),
 ( #10251, #12153, #11914, #8686, #4553, #19424 ),
 ( #15732, #3129, #3236, #1237, #10360, #993 ),
 ( #23540, #17636, #1345, #4788, #19181, #15841 ) ),
 .UNSPECIFIED., .F., .F., .F. ) 
 B_SPLINE_SURFACE_WITH_KNOTS ( ( 6, 3, 3, 6 ),
 ( 6, 6 ),
 ( 0.000000000000000000, 4.564346237179999655, 9.066392868600001265, 13.51003987140000007 ),
 ( 0.000000000000000000, 1.570796326752264882 ),
 .UNSPECIFIED. ) 
 GEOMETRIC_REPRESENTATION_ITEM ( )  RATIONAL_B_SPLINE_SURFACE ( (
 ( 1.000000000000000000, 0.6000000000108819398, 0.4000000000108820397, 0.3000000000081615159, 0.2500000000054409810, 0.2500000000000000000),
 ( 1.000000000000000000, 0.6000000000108819398, 0.4000000000108820397, 0.3000000000081615159, 0.2500000000054409810, 0.2500000000000000000),
 ( 1.000000000000000000, 0.6000000000108819398, 0.4000000000108820397, 0.3000000000081615159, 0.2500000000054409810, 0.2500000000000000000),
 ( 1.000000000000000000, 0.6000000000108819398, 0.4000000000108820397, 0.3000000000081615159, 0.2500000000054409810, 0.2500000000000000000),
 ( 1.000000000000000000, 0.6000000000108819398, 0.4000000000108820397, 0.3000000000081615159, 0.2500000000054409810, 0.2500000000000000000),
 ( 1.000000000000000000, 0.6000000000108819398, 0.4000000000108820397, 0.3000000000081615159, 0.2500000000054409810, 0.2500000000000000000),
 ( 1.000000000000000000, 0.6000000000108819398, 0.4000000000108820397, 0.3000000000081615159, 0.2500000000054409810, 0.2500000000000000000),
 ( 1.000000000000000000, 0.6000000000108819398, 0.4000000000108820397, 0.3000000000081615159, 0.2500000000054409810, 0.2500000000000000000),
 ( 1.000000000000000000, 0.6000000000108819398, 0.4000000000108820397, 0.3000000000081615159, 0.2500000000054409810, 0.2500000000000000000),
 ( 1.000000000000000000, 0.6000000000108819398, 0.4000000000108820397, 0.3000000000081615159, 0.2500000000054409810, 0.2500000000000000000),
 ( 1.000000000000000000, 0.6000000000108819398, 0.4000000000108820397, 0.3000000000081615159, 0.2500000000054409810, 0.2500000000000000000),
 ( 1.000000000000000000, 0.6000000000108819398, 0.4000000000108820397, 0.3000000000081615159, 0.2500000000054409810, 0.2500000000000000000) ) ) 
 REPRESENTATION_ITEM ( '' )  SURFACE ( )  );
#16515=CARTESIAN_POINT ( 'NONE',  ( -10.59674732016127585, 36.36477667316268025, -140.6486635252139195 ) ) ;
#16523=ORIENTED_EDGE ( 'NONE', *, *, #9977, .F. ) ;
#16528=CARTESIAN_POINT ( 'NONE',  ( -18.09080689940000397, 41.54765954780000214, -144.4256796519999853 ) ) ;
#16529=CARTESIAN_POINT ( 'NONE',  ( -22.52056272209999932, 33.27763168300000274, -146.2006519230000094 ) ) ;
#16530=VERTEX_POINT ( 'NONE', #14519 ) ;
#16535=CARTESIAN_POINT ( 'NONE',  ( -17.22605506639999717, 36.97564272059999979, -139.5994799229999899 ) ) ;
#16536=CARTESIAN_POINT ( 'NONE',  ( -15.46613156839999981, 36.99333119719999985, -147.5584717940000132 ) ) ;
#16538=CARTESIAN_POINT ( 'NONE',  ( -27.55423410434942255, 32.98668071434571658, -144.3507793926698071 ) ) ;
#16545=CARTESIAN_POINT ( 'NONE',  ( -27.04496201379999931, 40.71797592360000095, -143.5957174049999878 ) ) ;
#16558=CARTESIAN_POINT ( 'NONE',  ( -18.42429559863251498, 33.08108273512412723, -146.4504986391189050 ) ) ;
#16561=CARTESIAN_POINT ( 'NONE',  ( -23.53713177915716059, 38.91803379064137403, -139.7038563397429698 ) ) ;
#16577=CARTESIAN_POINT ( 'NONE',  ( -13.27765529700754499, 34.26824771871878283, -140.3891660076678249 ) ) ;
#16588=CARTESIAN_POINT ( 'NONE',  ( -12.37691123100000112, 36.07411227369999551, -148.4862478850000116 ) ) ;
#16596=CARTESIAN_POINT ( 'NONE',  ( -20.49738647338961783, 39.04222973627229010, -141.2738626595669871 ) ) ;
#16599=FACE_OUTER_BOUND ( 'NONE', #20713, .T. ) ;
#16610=CARTESIAN_POINT ( 'NONE',  ( -25.88719801257649422, 40.74404324587289494, -141.9468274994828221 ) ) ;
#16618=ADVANCED_FACE ( 'NONE', ( #12472 ), #12683, .F. ) ;
#16623=CARTESIAN_POINT ( 'NONE',  ( -7.036544835898043360, 36.13414510776094346, -148.5487805666791132 ) ) ;
#16624=CARTESIAN_POINT ( 'NONE',  ( -8.238646733050000392, 41.24792906369999912, -143.6196368420000056 ) ) ;
#16634=CARTESIAN_POINT ( 'NONE',  ( -11.96343978471735880, 39.40444247627922181, -140.7635797601743093 ) ) ;
#16636=CARTESIAN_POINT ( 'NONE',  ( -17.31853222291778138, 41.66660742467398393, -143.5159414623645091 ) ) ;
#16646=CARTESIAN_POINT ( 'NONE',  ( -19.79317654011716243, 38.64314174742496277, -140.5356700202810032 ) ) ;
#16666=CARTESIAN_POINT ( 'NONE',  ( -29.86462848807619963, 41.46897301219815546, -145.0541174283790156 ) ) ;
#16668=CARTESIAN_POINT ( 'NONE',  ( -22.52780672249999938, 37.05898997719999954, -140.0074087190000114 ) ) ;
#16672=CARTESIAN_POINT ( 'NONE',  ( -20.28536656038061636, 36.96856293253166115, -139.5160734783576970 ) ) ;
#16677=CARTESIAN_POINT ( 'NONE',  ( -23.91265852341890508, 39.71016181377052590, -147.9043966267969665 ) ) ;
#16686=CARTESIAN_POINT ( 'NONE',  ( -6.133959734627684846, 40.45360061668009877, -141.9452128759455434 ) ) ;
#16691=CARTESIAN_POINT ( 'NONE',  ( -22.52374396461171102, 33.50559259353841668, -144.4021133944701774 ) ) ;
#16694=CARTESIAN_POINT ( 'NONE',  ( -12.53599637006591827, 32.89425847576748652, -144.5669343789962511 ) ) ;
#16709=CARTESIAN_POINT ( 'NONE',  ( -13.09712973210239895, 32.88797929499759931, -146.6032212821853022 ) ) ;
#16717=CARTESIAN_POINT ( 'NONE',  ( -20.74418227170635731, 39.28578094490452344, -147.3492911869098236 ) ) ;
#16730=CARTESIAN_POINT ( 'NONE',  ( -26.57320955767643511, 39.25615809526139799, -147.2502486967401580 ) ) ;
#16733=CARTESIAN_POINT ( 'NONE',  ( -22.23138069772303638, 34.62558912635464026, -140.6296127985235955 ) ) ;
#16735=CARTESIAN_POINT ( 'NONE',  ( -30.02199999990000023, 40.03108891319999429, -145.8052959529999839 ) ) ;
#16741=CARTESIAN_POINT ( 'NONE',  ( -27.22834295012582828, 41.68433299786980939, -144.4761705782878209 ) ) ;
#16745=CARTESIAN_POINT ( 'NONE',  ( -6.071644824238406457, 36.06915794949389920, -148.2800132152668766 ) ) ;
#16746=CARTESIAN_POINT ( 'NONE',  ( -8.712023184163379952, 38.57885015659952188, -140.3122811010784119 ) ) ;
#16756=CARTESIAN_POINT ( 'NONE',  ( -12.35807366786784911, 40.97448640521876229, -143.6870081750666657 ) ) ;
#16761=CARTESIAN_POINT ( 'NONE',  ( -30.02199999990000023, 40.03108891319999429, -145.8052959529999839 ) ) ;
#16764=CARTESIAN_POINT ( 'NONE',  ( -29.13601448249999848, 36.98639052360000079, -140.5419328609999923 ) ) ;
#16765=ORIENTED_EDGE ( 'NONE', *, *, #17841, .F. ) ;
#16767=CARTESIAN_POINT ( 'NONE',  ( -21.70878449369999785, 39.52018264390000013, -147.4849246469999855 ) ) ;
#16807=CARTESIAN_POINT ( 'NONE',  ( -6.909346445838660422, 37.92300339050624558, -148.1333867873858026 ) ) ;
#16813=CARTESIAN_POINT ( 'NONE',  ( -21.76391789540379662, 33.32496974993136973, -144.3326792069850626 ) ) ;
#16816=CARTESIAN_POINT ( 'NONE',  ( -12.37691123100000112, 36.07411227369999551, -148.4862478850000116 ) ) ;
#16829=CARTESIAN_POINT ( 'NONE',  ( -28.15861914003539468, 32.75082038491409975, -146.4619352604428286 ) ) ;
#16846=CARTESIAN_POINT ( 'NONE',  ( -27.60583033836061517, 37.01000650955438687, -148.6900182103051691 ) ) ;
#16852=CARTESIAN_POINT ( 'NONE',  ( -26.39607007120000048, 36.95534867429999792, -140.3840478969999879 ) ) ;
#16854=CARTESIAN_POINT ( 'NONE',  ( -22.92066848189358552, 37.01209555897772674, -139.3757315019954319 ) ) ;
#16859=CARTESIAN_POINT ( 'NONE',  ( -27.26567793353847691, 36.96940380708128515, -148.4835048635911789 ) ) ;
#16863=CARTESIAN_POINT ( 'NONE',  ( -6.263809632758733592, 36.02430696941269872, -148.6165307568110734 ) ) ;
#16865=ORIENTED_EDGE ( 'NONE', *, *, #5021, .T. ) ;
#16873=CARTESIAN_POINT ( 'NONE',  ( -12.48399912348327945, 39.13586957966980151, -147.0556079066718098 ) ) ;
#16875=CARTESIAN_POINT ( 'NONE',  ( -17.60582215389345251, 39.60819216315037750, -147.6714151693956580 ) ) ;
#16878=CARTESIAN_POINT ( 'NONE',  ( -8.271665395472865612, 36.97019838864552810, -139.4157638768302832 ) ) ;
#16881=CARTESIAN_POINT ( 'NONE',  ( -22.00705883600000234, 37.05789963359999462, -148.1619053240000028 ) ) ;
#16885=CARTESIAN_POINT ( 'NONE',  ( -20.02720694385126876, 38.00365282337508432, -139.3916297347710156 ) ) ;
#16887=CARTESIAN_POINT ( 'NONE',  ( -28.11832915603455874, 33.48892755769719543, -144.3678690803285463 ) ) ;
#16900=CARTESIAN_POINT ( 'NONE',  ( -23.29130810115783845, 35.45552060375986514, -140.6454276014299012 ) ) ;
#16901=CARTESIAN_POINT ( 'NONE',  ( -30.50301086745307444, 40.75553727831436390, -144.8176898276264239 ) ) ;
#16906=CARTESIAN_POINT ( 'NONE',  ( -8.343166633029998280, 41.26425690090000131, -144.5268661329999986 ) ) ;
#16908=CARTESIAN_POINT ( 'NONE',  ( -9.971101149720000834, 37.05360750090000721, -147.8421425029999909 ) ) ;
#16909=CARTESIAN_POINT ( 'NONE',  ( -23.87836733110767540, 41.18897180524523804, -141.6563648539963367 ) ) ;
#16912=CARTESIAN_POINT ( 'NONE',  ( -14.93328160137761351, 36.92972691758927084, -148.3740393307602119 ) ) ;
#16913=CARTESIAN_POINT ( 'NONE',  ( -16.11775386674015564, 33.36946837792675780, -144.2542744048583927 ) ) ;
#16914=CARTESIAN_POINT ( 'NONE',  ( -20.34672008420000111, 36.01786665889999739, -139.8153362750000213 ) ) ;
#16919=CARTESIAN_POINT ( 'NONE',  ( -6.103115051414089720, 40.52053609467341744, -143.6011192969590127 ) ) ;
#16922=( BOUNDED_SURFACE ( )  B_SPLINE_SURFACE ( 5, 5, ( 
 ( #21324, #10461, #17738, #8675, #22627, #13571 ),
 ( #20843, #4538, #19057, #9993, #20973, #2878 ),
 ( #19889, #1696, #14410, #1580, #3465, #3822 ),
 ( #1934, #2049, #10703, #14644, #21440, #16198 ),
 ( #24, #7383, #9153, #5595, #14537, #21684 ),
 ( #8803, #17985, #16314, #16080, #18098, #5368 ),
 ( #12617, #3586, #5123, #21914, #17864, #6912 ),
 ( #7268, #1809, #10815, #9028, #8915, #21800 ),
 ( #15958, #5485, #7145, #23335, #12731, #18218 ),
 ( #19645, #12845, #16435, #20003, #14176, #20123 ),
 ( #3698, #21557, #7027, #10936, #11057, #18338 ),
 ( #141, #23219, #12369, #3342, #10578, #14289 ) ),
 .UNSPECIFIED., .F., .F., .F. ) 
 B_SPLINE_SURFACE_WITH_KNOTS ( ( 6, 3, 3, 6 ),
 ( 6, 6 ),
 ( 0.000000000000000000, 4.445608688430000122, 8.917804078430000558, 13.41780914199999941 ),
 ( 1.570796326447220004, 3.141592653590000062 ),
 .UNSPECIFIED. ) 
 GEOMETRIC_REPRESENTATION_ITEM ( )  RATIONAL_B_SPLINE_SURFACE ( (
 ( 0.2500000000000000000, 0.2499999999557195041, 0.2999999999335790091, 0.3999999999114384752, 0.5999999999114390414, 1.000000000000000000),
 ( 0.2500000000000000000, 0.2499999999557195041, 0.2999999999335790091, 0.3999999999114384752, 0.5999999999114390414, 1.000000000000000000),
 ( 0.2500000000000000000, 0.2499999999557195041, 0.2999999999335790091, 0.3999999999114384752, 0.5999999999114390414, 1.000000000000000000),
 ( 0.2500000000000000000, 0.2499999999557195041, 0.2999999999335790091, 0.3999999999114384752, 0.5999999999114390414, 1.000000000000000000),
 ( 0.2500000000000000000, 0.2499999999557195041, 0.2999999999335790091, 0.3999999999114384752, 0.5999999999114390414, 1.000000000000000000),
 ( 0.2500000000000000000, 0.2499999999557195041, 0.2999999999335790091, 0.3999999999114384752, 0.5999999999114390414, 1.000000000000000000),
 ( 0.2500000000000000000, 0.2499999999557195041, 0.2999999999335790091, 0.3999999999114384752, 0.5999999999114390414, 1.000000000000000000),
 ( 0.2500000000000000000, 0.2499999999557195041, 0.2999999999335790091, 0.3999999999114384752, 0.5999999999114390414, 1.000000000000000000),
 ( 0.2500000000000000000, 0.2499999999557195041, 0.2999999999335790091, 0.3999999999114384752, 0.5999999999114390414, 1.000000000000000000),
 ( 0.2500000000000000000, 0.2499999999557195041, 0.2999999999335790091, 0.3999999999114384752, 0.5999999999114390414, 1.000000000000000000),
 ( 0.2500000000000000000, 0.2499999999557195041, 0.2999999999335790091, 0.3999999999114384752, 0.5999999999114390414, 1.000000000000000000),
 ( 0.2500000000000000000, 0.2499999999557195041, 0.2999999999335790091, 0.3999999999114384752, 0.5999999999114390414, 1.000000000000000000) ) ) 
 REPRESENTATION_ITEM ( '' )  SURFACE ( )  );
#16923=CARTESIAN_POINT ( 'NONE',  ( -21.53618355982399635, 33.35162261389687188, -146.0341402270590265 ) ) ;
#16929=CARTESIAN_POINT ( 'NONE',  ( -12.30251875917725179, 34.86346480590818686, -147.0212501965618230 ) ) ;
#16935=EDGE_CURVE ( 'NONE', #6123, #7827, #9198, .T. ) ;
#16941=CARTESIAN_POINT ( 'NONE',  ( -13.92295968795637506, 34.11491018883658199, -140.3106646644930890 ) ) ;
#16951=CARTESIAN_POINT ( 'NONE',  ( -21.29590688489999906, 41.28591597809999314, -144.5271551099999954 ) ) ;
#16961=ORIENTED_EDGE ( 'NONE', *, *, #4435, .T. ) ;
#16964=CARTESIAN_POINT ( 'NONE',  ( -27.58120011020000106, 38.53525547130000461, -147.4183263870000076 ) ) ;
#16966=CARTESIAN_POINT ( 'NONE',  ( -22.79119882237723616, 32.80244356386412363, -141.5899087428671521 ) ) ;
#16978=CARTESIAN_POINT ( 'NONE',  ( -8.371159465364423014, 37.93364697496366489, -139.4097093116685073 ) ) ;
#16982=CARTESIAN_POINT ( 'NONE',  ( -26.61369313923911761, 36.92937183404333723, -140.1328975134356369 ) ) ;
#16985=CARTESIAN_POINT ( 'NONE',  ( -12.18289575740000075, 37.87223172089999679, -148.4976681630000144 ) ) ;
#16990=CARTESIAN_POINT ( 'NONE',  ( -7.015833805750000707, 33.30032478630000270, -141.9582197170000200 ) ) ;
#16993=CARTESIAN_POINT ( 'NONE',  ( -21.03694116389999635, 36.94210036639999828, -147.9486865819999935 ) ) ;
#16997=CARTESIAN_POINT ( 'NONE',  ( -20.60427366044887521, 39.77066172006404798, -140.2727996545226858 ) ) ;
#16999=CARTESIAN_POINT ( 'NONE',  ( -27.66848331343965128, 32.56468501992201681, -144.4027908766657902 ) ) ;
#17002=ORIENTED_EDGE ( 'NONE', *, *, #21985, .T. ) ;
#17008=CARTESIAN_POINT ( 'NONE',  ( -20.54812748657685972, 36.93719815735425271, -140.4704715740689949 ) ) ;
#17023=CARTESIAN_POINT ( 'NONE',  ( -24.68730002459999895, 39.33688142210000649, -147.2285014869999884 ) ) ;
#17025=CARTESIAN_POINT ( 'NONE',  ( -14.95010530348893951, 36.06328527009492291, -147.9474140018595563 ) ) ;
#17027=CARTESIAN_POINT ( 'NONE',  ( -16.46027398316528334, 32.88080821139473642, -146.2791150315001403 ) ) ;
#17033=CARTESIAN_POINT ( 'NONE',  ( -9.036966863464655830, 36.06754287650300483, -147.9517351211478342 ) ) ;
#17035=ORIENTED_EDGE ( 'NONE', *, *, #14940, .F. ) ;
#17039=CARTESIAN_POINT ( 'NONE',  ( -21.84945680779619437, 33.33324089315806305, -143.5473053630374523 ) ) ;
#17042=CARTESIAN_POINT ( 'NONE',  ( -12.86016529631691974, 36.30837334280015227, -147.6243440206422122 ) ) ;
#17049=CARTESIAN_POINT ( 'NONE',  ( -8.199334625101119656, 37.67958715123329938, -140.7360079146043290 ) ) ;
#17051=CARTESIAN_POINT ( 'NONE',  ( -27.97684248819999908, 35.51254237909999745, -147.4365014880000047 ) ) ;
#17055=CARTESIAN_POINT ( 'NONE',  ( -13.33045527085381998, 32.30799570172891322, -144.7412170606758650 ) ) ;
#17065=CARTESIAN_POINT ( 'NONE',  ( -20.97542662470000252, 40.85881720449999932, -141.8340754020000247 ) ) ;
#17067=CARTESIAN_POINT ( 'NONE',  ( -18.85038775884696705, 39.40085191981486901, -147.1529297763815691 ) ) ;
#17072=CARTESIAN_POINT ( 'NONE',  ( -24.73433384546525104, 33.38239242349900593, -144.4107376024117002 ) ) ;
#17080=ORIENTED_EDGE ( 'NONE', *, *, #387, .F. ) ;
#17083=ORIENTED_EDGE ( 'NONE', *, *, #22749, .F. ) ;
#17084=DIRECTION ( 'NONE',  ( 0.000000000000000000, 0.000000000000000000, 1.000000000000000000 ) ) ;
#17094=CARTESIAN_POINT ( 'NONE',  ( -11.19806794730000021, 41.07225940149999843, -141.8826665010000170 ) ) ;
#17099=CARTESIAN_POINT ( 'NONE',  ( -8.897765304693569632, 39.73354477844125654, -147.8293186649044912 ) ) ;
#17119=CARTESIAN_POINT ( 'NONE',  ( -14.12781175210000129, 38.88127384660000274, -139.8125553750000165 ) ) ;
#17120=CARTESIAN_POINT ( 'NONE',  ( -20.65692115970000131, 38.75897267589999728, -140.0270467099999792 ) ) ;
#17122=CARTESIAN_POINT ( 'NONE',  ( -28.70612892858435927, 35.15950212974924227, -139.8035036602273919 ) ) ;
#17132=ORIENTED_EDGE ( 'NONE', *, *, #374, .F. ) ;
#17146=CARTESIAN_POINT ( 'NONE',  ( -24.39610112286784371, 41.30434740782117586, -144.5132185276669929 ) ) ;
#17149=CARTESIAN_POINT ( 'NONE',  ( -15.99498317667975122, 33.76443601943795869, -141.9451672683316872 ) ) ;
#17150=CARTESIAN_POINT ( 'NONE',  ( -16.46770182039374220, 34.68366497520294445, -147.1680949295432583 ) ) ;
#17155=CARTESIAN_POINT ( 'NONE',  ( -9.784659724394936475, 33.29695882288061171, -143.3891222208823422 ) ) ;
#17160=CARTESIAN_POINT ( 'NONE',  ( -21.32007872946885030, 35.46309690574533846, -147.3430777018452602 ) ) ;
#17166=CARTESIAN_POINT ( 'NONE',  ( -23.51619327739999932, 36.94101002280000046, -140.1031831869999849 ) ) ;
#17179=CARTESIAN_POINT ( 'NONE',  ( -13.84608127647538289, 33.21776854254977707, -143.8496330080570829 ) ) ;
#17184=ORIENTED_EDGE ( 'NONE', *, *, #23226, .T. ) ;
#17189=CARTESIAN_POINT ( 'NONE',  ( -17.65545014875934626, 37.67134846496733758, -140.4683765912815545 ) ) ;
#17192=CARTESIAN_POINT ( 'NONE',  ( -25.26464694443967929, 35.54252112450230783, -140.6256209330285287 ) ) ;
#17202=ADVANCED_FACE ( 'NONE', ( #5139 ), #4632, .F. ) ;
#17209=CARTESIAN_POINT ( 'NONE',  ( -10.95384970519167034, 40.87632101822132569, -142.0199864900084208 ) ) ;
#17214=CARTESIAN_POINT ( 'NONE',  ( -8.441146697811769073, 41.59278767816196876, -144.5480507108394477 ) ) ;
#17232=CARTESIAN_POINT ( 'NONE',  ( -15.02010258789212926, 41.63949583921710484, -143.5015232158323499 ) ) ;
#17235=CARTESIAN_POINT ( 'NONE',  ( -26.29566636579999894, 36.18167175180000328, -140.3932108110000172 ) ) ;
#17257=CARTESIAN_POINT ( 'NONE',  ( -4.584402860569999127, 37.05223431090000474, -140.2914745300000163 ) ) ;
#17270=CARTESIAN_POINT ( 'NONE',  ( -17.20894333738748117, 33.38229181965237302, -141.8650879853053368 ) ) ;
#17289=CARTESIAN_POINT ( 'NONE',  ( -9.285539185979999388, 35.09287230280000358, -147.9937876190000168 ) ) ;
#17294=ORIENTED_EDGE ( 'NONE', *, *, #19864, .T. ) ;
#17295=CARTESIAN_POINT ( 'NONE',  ( -7.010349701908019426, 37.05829245174740549, -148.1453878984958124 ) ) ;
#17301=CARTESIAN_POINT ( 'NONE',  ( -15.37212823710000009, 38.89807584180000077, -148.3010324070000081 ) ) ;
#17306=CARTESIAN_POINT ( 'NONE',  ( -17.83048858051152408, 39.52908467829296768, -140.3990652861876072 ) ) ;
#17310=CARTESIAN_POINT ( 'NONE',  ( -24.97797643630000053, 37.05442817780000553, -147.8575004449999994 ) ) ;
#17326=CARTESIAN_POINT ( 'NONE',  ( -15.27002291899999875, 38.46844526379999962, -147.3668459620000135 ) ) ;
#17329=CARTESIAN_POINT ( 'NONE',  ( -8.008464111580879674, 33.29536412579140148, -142.0809313905602096 ) ) ;
#17330=CARTESIAN_POINT ( 'NONE',  ( -9.937276790871505838, 38.82225217169769849, -147.9475752953410392 ) ) ;
#17349=CARTESIAN_POINT ( 'NONE',  ( -15.19793912339760134, 40.53066279750093770, -141.9083977990133860 ) ) ;
#17351=CARTESIAN_POINT ( 'NONE',  ( -25.40969612650229337, 34.57839653382308853, -147.5232836264007119 ) ) ;
#17358=EDGE_CURVE ( 'NONE', #3155, #7827, #10853, .T. ) ;
#17391=CARTESIAN_POINT ( 'NONE',  ( -10.67777851957104396, 33.99926051417099160, -142.1577009039073971 ) ) ;
#17396=CARTESIAN_POINT ( 'NONE',  ( -28.81652202475261859, 33.24392987422240253, -143.6567944639990628 ) ) ;
#17399=CARTESIAN_POINT ( 'NONE',  ( -13.26119488862553553, 36.18558975636723574, -139.9165878528899327 ) ) ;
#17404=CARTESIAN_POINT ( 'NONE',  ( -10.86833117931673875, 32.45440757875775262, -143.3755448009918894 ) ) ;
#17407=CARTESIAN_POINT ( 'NONE',  ( -8.514310886093261033, 36.94123471669811209, -140.1199228270031938 ) ) ;
#17410=CARTESIAN_POINT ( 'NONE',  ( -20.95225485091065565, 36.93199168240897734, -148.3394883768439456 ) ) ;
#17413=CARTESIAN_POINT ( 'NONE',  ( -6.323999170589999608, 34.61896835509999448, -147.3311432729999808 ) ) ;
#17415=CARTESIAN_POINT ( 'NONE',  ( -21.50444101780000139, 40.78041997809999941, -146.2395182369999986 ) ) ;
#17422=CARTESIAN_POINT ( 'NONE',  ( -17.62837147338279209, 40.04293477547881963, -142.2225117880255141 ) ) ;
#17426=CARTESIAN_POINT ( 'NONE',  ( -25.18528168905853803, 35.37446932239454611, -140.2257898707420054 ) ) ;
#17428=CARTESIAN_POINT ( 'NONE',  ( -11.44228618995933111, 41.26819778530094140, -141.7453465123093679 ) ) ;
#17450=ORIENTED_EDGE ( 'NONE', *, *, #6762, .T. ) ;
#17467=CARTESIAN_POINT ( 'NONE',  ( -19.59255166829999695, 37.05126161860000167, -140.3061871179999969 ) ) ;
#17470=CARTESIAN_POINT ( 'NONE',  ( -14.68945449529999969, 41.62249060810000145, -143.5408288559999903 ) ) ;
#17471=CARTESIAN_POINT ( 'NONE',  ( -25.35967232409695526, 32.77444722697165957, -141.6253268585252556 ) ) ;
#17491=CARTESIAN_POINT ( 'NONE',  ( -14.80611810279999929, 41.62812440830000327, -144.5263372940000011 ) ) ;
#17502=CARTESIAN_POINT ( 'NONE',  ( -16.45586251411692658, 37.06757768449097057, -140.3467090680682929 ) ) ;
#17510=CARTESIAN_POINT ( 'NONE',  ( -10.17933436568690020, 35.38122503049920198, -147.6311798956890016 ) ) ;
#17516=CARTESIAN_POINT ( 'NONE',  ( -29.38973091914479951, 34.58161923556721007, -140.8094832672705365 ) ) ;
#17519=CARTESIAN_POINT ( 'NONE',  ( -23.24588518186543951, 41.24341285037552041, -143.7187626422040125 ) ) ;
#17534=SURFACE_STYLE_FILL_AREA ( #1133 ) ;
#17537=CARTESIAN_POINT ( 'NONE',  ( -7.806459626917139794, 32.86659014882347662, -143.7778124396145927 ) ) ;
#17538=CARTESIAN_POINT ( 'NONE',  ( -30.02199999990000023, 40.89711431700000333, -146.3052959529999839 ) ) ;
#17550=CARTESIAN_POINT ( 'NONE',  ( -17.32451618079999633, 37.89224186959999940, -139.5945780149999962 ) ) ;
#17555=CARTESIAN_POINT ( 'NONE',  ( -6.033650297970000409, 36.94170754819999303, -147.9652040070000112 ) ) ;
#17556=CARTESIAN_POINT ( 'NONE',  ( -24.81824330196665329, 33.37107051305610383, -143.6358663909026916 ) ) ;
#17575=CARTESIAN_POINT ( 'NONE',  ( -9.197324267939999132, 40.96642299180000180, -143.5436038170000188 ) ) ;
#17576=CARTESIAN_POINT ( 'NONE',  ( -10.98325336546828623, 39.16634992210826738, -141.2646178871198117 ) ) ;
#17577=CARTESIAN_POINT ( 'NONE',  ( -8.357298602909251528, 35.07902350790208601, -139.9951508849170239 ) ) ;
#17579=CARTESIAN_POINT ( 'NONE',  ( -9.637198844916387230, 39.82560803348724221, -147.8101000518229853 ) ) ;
#17582=EDGE_CURVE ( 'NONE', #18180, #22397, #1943, .T. ) ;
#17596=CARTESIAN_POINT ( 'NONE',  ( -14.70358821724112630, 36.91864139954906676, -140.0875527721922822 ) ) ;
#17609=CARTESIAN_POINT ( 'NONE',  ( -24.16551117139999860, 36.07182940189999698, -148.2420083170000282 ) ) ;
#17614=CARTESIAN_POINT ( 'NONE',  ( -13.92389048506121441, 38.46313951856771496, -140.8221090936200426 ) ) ;
#17627=FACE_OUTER_BOUND ( 'NONE', #18070, .T. ) ;
#17636=CARTESIAN_POINT ( 'NONE',  ( -29.45815224830205992, 36.94793816026839295, -140.4653836173367836 ) ) ;
#17639=CARTESIAN_POINT ( 'NONE',  ( -13.73025257492641060, 37.03482478361183183, -140.6242165752723565 ) ) ;
#17647=CARTESIAN_POINT ( 'NONE',  ( -8.835671558513036317, 38.44113563076084006, -147.4188414315597129 ) ) ;
#17654=CARTESIAN_POINT ( 'NONE',  ( -7.324031428439999658, 35.31041870520000003, -140.2046280479999893 ) ) ;
#17656=CARTESIAN_POINT ( 'NONE',  ( -20.65692115970000131, 38.75897267589999728, -140.0270467099999792 ) ) ;
#17662=CARTESIAN_POINT ( 'NONE',  ( -21.50145757607925390, 36.99754792876771603, -147.3684231709947312 ) ) ;
#17672=CARTESIAN_POINT ( 'NONE',  ( -23.51619327739999932, 36.94101002280000046, -140.1031831869999849 ) ) ;
#17685=CARTESIAN_POINT ( 'NONE',  ( -18.37691940389999701, 35.51168060189999665, -147.4900940509999998 ) ) ;
#17688=CARTESIAN_POINT ( 'NONE',  ( -7.466450641298933100, 32.18700325849513888, -143.6846124506146509 ) ) ;
#17692=( BOUNDED_CURVE ( )  B_SPLINE_CURVE ( 5, ( #2678, #4807, #19087, #11931, #15751, #20997, #13850, #15513, #19449, #23013, #9905, #22772 ),
 .UNSPECIFIED., .F., .F. ) 
 B_SPLINE_CURVE_WITH_KNOTS ( ( 6, 3, 3, 6 ),
 ( 0.000000000000000000, 4.469553974960000176, 8.969854531369998440, 13.50363095830000049 ),
 .UNSPECIFIED. ) 
 CURVE ( )  GEOMETRIC_REPRESENTATION_ITEM ( )  RATIONAL_B_SPLINE_CURVE ( ( 0.2500000000000000000, 0.2500000000000000000, 0.2500000000000000000, 0.2500000000000000000, 0.2500000000000000000, 0.2500000000000000000, 0.2500000000000000000, 0.2500000000000000000, 0.2500000000000000000, 0.2500000000000000000, 0.2500000000000000000, 0.2500000000000000000 ) ) 
 REPRESENTATION_ITEM ( '' )  );
#17706=CARTESIAN_POINT ( 'NONE',  ( -21.13851658211848061, 36.11334442976911419, -147.9366295165976055 ) ) ;
#17720=CARTESIAN_POINT ( 'NONE',  ( -24.06602356359999817, 36.94557182220000158, -148.2530914610000252 ) ) ;
#17724=CARTESIAN_POINT ( 'NONE',  ( -13.80268676182414112, 38.89075166758362201, -139.8876559908354693 ) ) ;
#17738=CARTESIAN_POINT ( 'NONE',  ( -4.855180678435647046, 37.01991258974685906, -139.3889649350431910 ) ) ;
#17740=PLANE ( 'NONE',  #8896 ) ;
#17745=CARTESIAN_POINT ( 'NONE',  ( -25.07725372939999886, 36.26300138690000097, -147.8685835880000070 ) ) ;
#17766=CARTESIAN_POINT ( 'NONE',  ( -7.220568065030000149, 34.52259161599999970, -140.6708207100000152 ) ) ;
#17770=CARTESIAN_POINT ( 'NONE',  ( -4.740745377981987474, 37.03357229753903113, -140.5852769424096493 ) ) ;
#17786=CARTESIAN_POINT ( 'NONE',  ( -23.64946213540040887, 37.84712475405090260, -139.7583381698287042 ) ) ;
#17793=CARTESIAN_POINT ( 'NONE',  ( -15.46613156818549939, 36.99333119717887541, -147.5584717933951708 ) ) ;
#17794=CARTESIAN_POINT ( 'NONE',  ( -28.33971964074914851, 37.08144121879573163, -140.0461821376498506 ) ) ;
#17799=CARTESIAN_POINT ( 'NONE',  ( -15.36599175859999988, 37.73046438850000328, -147.5598381920000008 ) ) ;
#17825=CARTESIAN_POINT ( 'NONE',  ( -22.21135766849999982, 35.30661492690000358, -147.9492090369999744 ) ) ;
#17830=CARTESIAN_POINT ( 'NONE',  ( -26.49522641139999735, 37.71913029610000478, -140.3749603070000092 ) ) ;
#17835=( BOUNDED_SURFACE ( )  B_SPLINE_SURFACE ( 5, 5, ( 
 ( #13443, #4404, #11645, #18922, #2634, #858 ),
 ( #15820, #19274, #12473, #16062, #14038, #13811 ),
 ( #21075, #17724, #21193, #22971, #17614, #10687 ),
 ( #23204, #23086, #12124, #1567, #1325, #5000 ),
 ( #12243, #19757, #23320, #8784, #21308, #10562 ),
 ( #3453, #6893, #17968, #2983, #1680, #6543 ),
 ( #17491, #15594, #3215, #10446, #22856, #7011 ),
 ( #1440, #4761, #12009, #19403, #12354, #14274 ),
 ( #14161, #8659, #3103, #21542, #10220, #1215 ),
 ( #8441, #5224, #21425, #15942, #3326, #15709 ),
 ( #17848, #6656, #13919, #4877, #19630, #10339 ),
 ( #8546, #5110, #6773, #19521, #1916, #10797 ) ),
 .UNSPECIFIED., .F., .F., .F. ) 
 B_SPLINE_SURFACE_WITH_KNOTS ( ( 6, 3, 3, 6 ),
 ( 6, 6 ),
 ( 0.000000000000000000, 4.151671928079999851, 8.316542232069998875, 12.50501063799999990 ),
 ( 0.000000000000000000, 1.570796326821630062 ),
 .UNSPECIFIED. ) 
 GEOMETRIC_REPRESENTATION_ITEM ( )  RATIONAL_B_SPLINE_SURFACE ( (
 ( 1.000000000000000000, 0.5999999999932189576, 0.3999999999932190020, 0.2999999999949140017, 0.2499999999966094899, 0.2500000000000000000),
 ( 1.000000000000000000, 0.5999999999932189576, 0.3999999999932190020, 0.2999999999949140017, 0.2499999999966094899, 0.2500000000000000000),
 ( 1.000000000000000000, 0.5999999999932189576, 0.3999999999932190020, 0.2999999999949140017, 0.2499999999966094899, 0.2500000000000000000),
 ( 1.000000000000000000, 0.5999999999932189576, 0.3999999999932190020, 0.2999999999949140017, 0.2499999999966094899, 0.2500000000000000000),
 ( 1.000000000000000000, 0.5999999999932189576, 0.3999999999932190020, 0.2999999999949140017, 0.2499999999966094899, 0.2500000000000000000),
 ( 1.000000000000000000, 0.5999999999932189576, 0.3999999999932190020, 0.2999999999949140017, 0.2499999999966094899, 0.2500000000000000000),
 ( 1.000000000000000000, 0.5999999999932189576, 0.3999999999932190020, 0.2999999999949140017, 0.2499999999966094899, 0.2500000000000000000),
 ( 1.000000000000000000, 0.5999999999932189576, 0.3999999999932190020, 0.2999999999949140017, 0.2499999999966094899, 0.2500000000000000000),
 ( 1.000000000000000000, 0.5999999999932189576, 0.3999999999932190020, 0.2999999999949140017, 0.2499999999966094899, 0.2500000000000000000),
 ( 1.000000000000000000, 0.5999999999932189576, 0.3999999999932190020, 0.2999999999949140017, 0.2499999999966094899, 0.2500000000000000000),
 ( 1.000000000000000000, 0.5999999999932189576, 0.3999999999932190020, 0.2999999999949140017, 0.2499999999966094899, 0.2500000000000000000),
 ( 1.000000000000000000, 0.5999999999932189576, 0.3999999999932190020, 0.2999999999949140017, 0.2499999999966094899, 0.2500000000000000000) ) ) 
 REPRESENTATION_ITEM ( '' )  SURFACE ( )  );
#17840=CARTESIAN_POINT ( 'NONE',  ( -15.67014142459999881, 35.45905754580000036, -147.3461856840000053 ) ) ;
#17841=EDGE_CURVE ( 'NONE', #1248, #14370, #21671, .T. ) ;
#17848=CARTESIAN_POINT ( 'NONE',  ( -15.47708384459999920, 37.95279615419999431, -148.5507537150000132 ) ) ;
#17864=CARTESIAN_POINT ( 'NONE',  ( -5.241146848258035007, 41.27390541520301781, -144.5340427261826051 ) ) ;
#17865=CARTESIAN_POINT ( 'NONE',  ( -8.514310886080000529, 36.94123471670000214, -140.1199228270000106 ) ) ;
#17868=CARTESIAN_POINT ( 'NONE',  ( -26.49522641139999735, 37.71913029610000478, -140.3749603070000092 ) ) ;
#17869=CARTESIAN_POINT ( 'NONE',  ( -15.57786843150000067, 37.00666880280000726, -148.5521201120000114 ) ) ;
#17878=CARTESIAN_POINT ( 'NONE',  ( -24.10813950015861451, 36.95059904175489862, -147.5089432697649556 ) ) ;
#17885=CARTESIAN_POINT ( 'NONE',  ( -8.869124888310000898, 38.72872035620000020, -148.0517159070000162 ) ) ;
#17895=CARTESIAN_POINT ( 'NONE',  ( -5.647208160094595364, 36.92537127315257806, -140.1716802708971557 ) ) ;
#17918=CARTESIAN_POINT ( 'NONE',  ( -28.59946202397140169, 34.31616424879415916, -140.2812573677312002 ) ) ;
#17923=ORIENTED_EDGE ( 'NONE', *, *, #1084, .F. ) ;
#17925=CARTESIAN_POINT ( 'NONE',  ( -19.79184979336553241, 37.02747215728108188, -140.6521846888477114 ) ) ;
#17926=CARTESIAN_POINT ( 'NONE',  ( -11.66591920674827065, 38.51472844954471242, -147.7933753654626798 ) ) ;
#17953=CARTESIAN_POINT ( 'NONE',  ( -26.39256767694444150, 41.50003988677031685, -143.5805134116744171 ) ) ;
#17959=CARTESIAN_POINT ( 'NONE',  ( -11.11377970773875923, 36.98904460433606545, -140.6889018750556772 ) ) ;
#17966=CARTESIAN_POINT ( 'NONE',  ( -11.59475511489694988, 36.93163239416678323, -139.6817994052732388 ) ) ;
#17968=CARTESIAN_POINT ( 'NONE',  ( -14.08453874197354416, 41.33416090294871026, -143.6415802795030743 ) ) ;
#17969=CARTESIAN_POINT ( 'NONE',  ( -28.47499893025420548, 37.06529344306947138, -140.4421442387196350 ) ) ;
#17985=CARTESIAN_POINT ( 'NONE',  ( -6.044964120310517330, 41.66664426582369174, -143.4739125349191795 ) ) ;
#17995=VERTEX_POINT ( 'NONE', #3777 ) ;
#17996=CARTESIAN_POINT ( 'NONE',  ( -24.74875653007431708, 37.76084906505778349, -147.5435553219018061 ) ) ;
#18001=FILL_AREA_STYLE ('',( #20144 ) ) ;
#18002=CARTESIAN_POINT ( 'NONE',  ( -19.95597284623131173, 34.08874935939712714, -140.3436463108538703 ) ) ;
#18003=CARTESIAN_POINT ( 'NONE',  ( -8.554523812450000264, 40.80811760249999764, -146.2789059460000090 ) ) ;
#18008=APPLICATION_CONTEXT ( 'automotive_design' ) ;
#18012=CARTESIAN_POINT ( 'NONE',  ( -22.73109880829999696, 38.77532135890000120, -140.2559096070000066 ) ) ;
#18036=CARTESIAN_POINT ( 'NONE',  ( -12.95309207247981753, 35.58606224187055744, -147.4460499723959970 ) ) ;
#18042=CARTESIAN_POINT ( 'NONE',  ( -20.61753010269738340, 36.92891383027765784, -140.0927360959155976 ) ) ;
#18043=CARTESIAN_POINT ( 'NONE',  ( -11.81646477902665637, 40.44164707346661913, -144.5342250517892353 ) ) ;
#18050=CARTESIAN_POINT ( 'NONE',  ( -18.60901166351237279, 37.01038625230346923, -148.6497975989736346 ) ) ;
#18056=CARTESIAN_POINT ( 'NONE',  ( -19.89002371299999794, 39.36161564540000057, -140.9617346340000381 ) ) ;
#18062=CARTESIAN_POINT ( 'NONE',  ( -15.70137303715876875, 38.91953314721723700, -148.2523098871654383 ) ) ;
#18070=EDGE_LOOP ( 'NONE', ( #17080, #11767, #10124, #20298 ) ) ;
#18075=CARTESIAN_POINT ( 'NONE',  ( -15.94523344369999940, 33.71216531379999282, -145.7766456660000074 ) ) ;
#18078=ORIENTED_EDGE ( 'NONE', *, *, #8046, .T. ) ;
#18082=CARTESIAN_POINT ( 'NONE',  ( -16.55827375307784877, 37.05535324330323732, -139.5705083843519390 ) ) ;
#18098=CARTESIAN_POINT ( 'NONE',  ( -5.136302089049142872, 41.25620344490214819, -143.6246837869908575 ) ) ;
#18110=CARTESIAN_POINT ( 'NONE',  ( -29.82391180389999619, 40.55477172079999804, -144.2881336360000262 ) ) ;
#18116=CARTESIAN_POINT ( 'NONE',  ( -20.34672008420000111, 36.01786665889999739, -139.8153362750000213 ) ) ;
#18118=CARTESIAN_POINT ( 'NONE',  ( -9.197324267974639866, 40.96642299190880010, -143.5436038169824258 ) ) ;
#18141=STYLED_ITEM ( 'NONE', ( #1711 ), #19431 ) ;
#18151=CARTESIAN_POINT ( 'NONE',  ( -13.11071995283477953, 37.07027326795081734, -147.8134892432882452 ) ) ;
#18157=CARTESIAN_POINT ( 'NONE',  ( -19.59117934188227395, 33.37909977088141744, -146.4170658873010495 ) ) ;
#18159=CARTESIAN_POINT ( 'NONE',  ( -11.16766646727579015, 41.31356556668690416, -143.7956700918360298 ) ) ;
#18176=CARTESIAN_POINT ( 'NONE',  ( -25.74743564712004229, 37.94517732367248186, -139.7356315992777809 ) ) ;
#18180=VERTEX_POINT ( 'NONE', #13972 ) ;
#18185=ORIENTED_EDGE ( 'NONE', *, *, #8654, .F. ) ;
#18187=CARTESIAN_POINT ( 'NONE',  ( -10.92854443057495928, 33.70908472042151516, -142.0058283512219930 ) ) ;
#18202=CARTESIAN_POINT ( 'NONE',  ( -29.64895016830000429, 40.48034887659999725, -142.7934167989999992 ) ) ;
#18218=CARTESIAN_POINT ( 'NONE',  ( -5.733381482170000432, 39.34803470290000149, -147.3316303149999840 ) ) ;
#18231=CARTESIAN_POINT ( 'NONE',  ( -24.68730002459999895, 39.33688142210000649, -147.2285014869999884 ) ) ;
#18232=CARTESIAN_POINT ( 'NONE',  ( -29.36832786400000117, 38.86294434210000048, -140.8528603229999874 ) ) ;
#18238=( LENGTH_UNIT ( ) NAMED_UNIT ( * ) SI_UNIT ( .MILLI., .METRE. ) );
#18239=CARTESIAN_POINT ( 'NONE',  ( -19.04867772230000256, 35.29145880730000329, -148.2212826610000036 ) ) ;
#18243=CARTESIAN_POINT ( 'NONE',  ( -23.61758233950000019, 37.78045452579999619, -140.0909254550000185 ) ) ;
#18253=CARTESIAN_POINT ( 'NONE',  ( -5.762834417994439740, 39.50865942498580097, -140.4825946862647754 ) ) ;
#18255=EDGE_LOOP ( 'NONE', ( #1910, #16340, #15689, #17035 ) ) ;
#18268=CARTESIAN_POINT ( 'NONE',  ( -13.36469768600054486, 37.07845968427643157, -139.9331372610153608 ) ) ;
#18270=ORIENTED_EDGE ( 'NONE', *, *, #15631, .T. ) ;
#18275=CARTESIAN_POINT ( 'NONE',  ( -16.23340181981567198, 34.21381099665894965, -147.7313700749976988 ) ) ;
#18282=CARTESIAN_POINT ( 'NONE',  ( -19.38998902330187590, 34.64861313674464327, -147.6078979941154898 ) ) ;
#18292=CARTESIAN_POINT ( 'NONE',  ( -27.26567793380000282, 36.96940380710000085, -148.4835048639999968 ) ) ;
#18299=CARTESIAN_POINT ( 'NONE',  ( -26.17844700321043661, 36.98132551455271511, -140.6351982806931176 ) ) ;
#18301=CARTESIAN_POINT ( 'NONE',  ( -21.77251801933481445, 32.71408580851625203, -146.4208751718306303 ) ) ;
#18305=ORIENTED_EDGE ( 'NONE', *, *, #19412, .F. ) ;
#18306=CARTESIAN_POINT ( 'NONE',  ( -26.61369313923914603, 36.92937183404335855, -140.1328975134355517 ) ) ;
#18310=CARTESIAN_POINT ( 'NONE',  ( -6.166004029541132248, 36.95750611116266526, -148.6250205690584778 ) ) ;
#18311=CARTESIAN_POINT ( 'NONE',  ( -11.10890527118989901, 34.84141842858843319, -140.9538660573311972 ) ) ;
#18322=CARTESIAN_POINT ( 'NONE',  ( -17.44989882376803791, 40.67283837537863889, -143.6255418396287666 ) ) ;
#18323=CARTESIAN_POINT ( 'NONE',  ( -29.21069264103822150, 41.10559376373601737, -145.0521024197723818 ) ) ;
#18338=CARTESIAN_POINT ( 'NONE',  ( -5.932764524189999555, 37.76833845600000217, -147.9772051180000005 ) ) ;
#18346=STYLED_ITEM ( 'NONE', ( #23362 ), #19731 ) ;
#18355=CARTESIAN_POINT ( 'NONE',  ( -17.98984244384617526, 36.14647386681518526, -147.9375626265034498 ) ) ;
#18359=CARTESIAN_POINT ( 'NONE',  ( -15.17576278497271502, 36.16931166175189105, -147.5919646919771822 ) ) ;
#18366=CARTESIAN_POINT ( 'NONE',  ( -6.804059094464567359, 37.03366832433017208, -147.4295713063914377 ) ) ;
#18371=CARTESIAN_POINT ( 'NONE',  ( -24.97797643630000053, 37.05442817780000553, -147.8575004449999994 ) ) ;
#18372=CARTESIAN_POINT ( 'NONE',  ( -13.38748872365634135, 33.38537881988771971, -144.5933708985054125 ) ) ;
#18389=CARTESIAN_POINT ( 'NONE',  ( -20.51299658253075009, 36.06115981397903170, -140.1078951487501456 ) ) ;
#18392=CARTESIAN_POINT ( 'NONE',  ( -19.89304997513555051, 37.75112169002715490, -140.6578993746063020 ) ) ;
#18396=CARTESIAN_POINT ( 'NONE',  ( -17.91974642297901354, 36.92811127467708587, -148.3783205066631297 ) ) ;
#18404=ADVANCED_FACE ( 'NONE', ( #15269 ), #10862, .F. ) ;
#18406=CARTESIAN_POINT ( 'NONE',  ( -26.39256767726975994, 41.50003988705911695, -143.5805134116048123 ) ) ;
#18414=( BOUNDED_CURVE ( )  B_SPLINE_CURVE ( 5, ( #10630, #535, #18268, #16472, #7767, #10987 ),
 .UNSPECIFIED., .F., .F. ) 
 B_SPLINE_CURVE_WITH_KNOTS ( ( 6, 6 ),
 ( 0.000000000000000000, 1.570796326821625399 ),
 .UNSPECIFIED. ) 
 CURVE ( )  GEOMETRIC_REPRESENTATION_ITEM ( )  RATIONAL_B_SPLINE_CURVE ( ( 1.000000000000000000, 0.5999999999932199568, 0.3999999999932200012, 0.2999999999949150009, 0.2499999999966100173, 0.2500000000000000000 ) ) 
 REPRESENTATION_ITEM ( '' )  );
#18417=CARTESIAN_POINT ( 'NONE',  ( -7.305231917150000420, 34.61982510829999882, -147.5275646999999992 ) ) ;
#18420=CARTESIAN_POINT ( 'NONE',  ( -11.38486064716495960, 36.95668670071903961, -140.3965526140712257 ) ) ;
#18421=CARTESIAN_POINT ( 'NONE',  ( -8.814413626191640816, 41.18437930593979956, -141.5628561694050234 ) ) ;
#18428=CARTESIAN_POINT ( 'NONE',  ( -11.68420994714742100, 39.25205177013263125, -141.0178453346331935 ) ) ;
#18431=CARTESIAN_POINT ( 'NONE',  ( -29.94412816112640030, 41.23953273985599566, -145.7122098474877987 ) ) ;
#18433=CARTESIAN_POINT ( 'NONE',  ( -7.427142538590000065, 36.18616221519999954, -139.9783837409999876 ) ) ;
#18437=CARTESIAN_POINT ( 'NONE',  ( -17.42663577349999926, 38.80963643279999786, -139.8270276149999916 ) ) ;
#18439=CARTESIAN_POINT ( 'NONE',  ( -19.86433599696554353, 39.82348905163189556, -140.3451089131285698 ) ) ;
#18441=CARTESIAN_POINT ( 'NONE',  ( -27.95514704228551750, 33.86422026307950262, -145.8098529824889340 ) ) ;
#18446=CARTESIAN_POINT ( 'NONE',  ( -11.19828263940000035, 35.50589712219999683, -140.5907466439999780 ) ) ;
#18452=( BOUNDED_CURVE ( )  B_SPLINE_CURVE ( 5, ( #20864, #13717, #2545, #13591, #11921, #7994 ),
 .UNSPECIFIED., .F., .F. ) 
 B_SPLINE_CURVE_WITH_KNOTS ( ( 6, 6 ),
 ( 0.000000000000000000, 1.570796326769926088 ),
 .UNSPECIFIED. ) 
 CURVE ( )  GEOMETRIC_REPRESENTATION_ITEM ( )  RATIONAL_B_SPLINE_CURVE ( ( 1.000000000000000000, 0.6000000000063849814, 0.4000000000063849703, 0.3000000000047887139, 0.2500000000031924463, 0.2499999999999999445 ) ) 
 REPRESENTATION_ITEM ( '' )  );
#18456=CARTESIAN_POINT ( 'NONE',  ( -21.53618355989999955, 33.35162261420000362, -146.0341402270000231 ) ) ;
#18459=EDGE_LOOP ( 'NONE', ( #540, #6374 ) ) ;
#18462=CARTESIAN_POINT ( 'NONE',  ( -19.48816230402476180, 36.23023348068691973, -140.2952556285365802 ) ) ;
#18465=CARTESIAN_POINT ( 'NONE',  ( -23.24304760862829156, 39.89470199026986563, -140.1709173790817999 ) ) ;
#18466=CARTESIAN_POINT ( 'NONE',  ( -15.57786843150000067, 37.00666880280000726, -148.5521201120000114 ) ) ;
#18471=CARTESIAN_POINT ( 'NONE',  ( -5.764515702665429231, 39.05871236480190589, -141.1073062976952599 ) ) ;
#18476=CARTESIAN_POINT ( 'NONE',  ( -22.82643395159999855, 32.86988923359999859, -143.6006525860000238 ) ) ;
#18479=CARTESIAN_POINT ( 'NONE',  ( -13.52923207339164335, 35.54581745406167670, -140.8134052129221061 ) ) ;
#18493=CARTESIAN_POINT ( 'NONE',  ( -9.834719431799998191, 32.58365614919999587, -144.2353630830000100 ) ) ;
#18500=CARTESIAN_POINT ( 'NONE',  ( -21.44245888780737630, 40.16992768860739460, -145.8848771850359469 ) ) ;
#18506=ORIENTED_EDGE ( 'NONE', *, *, #9657, .F. ) ;
#18511=CARTESIAN_POINT ( 'NONE',  ( -26.61767157499349423, 39.52029466085011222, -147.6008517105564408 ) ) ;
#18513=CARTESIAN_POINT ( 'NONE',  ( -22.03156944974935882, 33.39557638551315932, -141.8445571067651940 ) ) ;
#18516=ORIENTED_EDGE ( 'NONE', *, *, #6416, .T. ) ;
#18521=CARTESIAN_POINT ( 'NONE',  ( -28.00347998519043458, 37.05747243973696925, -148.5422211677327766 ) ) ;
#18525=CARTESIAN_POINT ( 'NONE',  ( -6.166004029541136688, 36.95750611116264395, -148.6250205690584210 ) ) ;
#18538=CARTESIAN_POINT ( 'NONE',  ( -12.84574840978007693, 37.96884797463420114, -148.5681481162234263 ) ) ;
#18540=CARTESIAN_POINT ( 'NONE',  ( -29.55850978561355902, 41.47329217818079883, -142.4456950392344083 ) ) ;
#18550=CARTESIAN_POINT ( 'NONE',  ( -20.68104909725491680, 41.14100626298056085, -146.5604280120006990 ) ) ;
#18568=ORIENTED_EDGE ( 'NONE', *, *, #6601, .F. ) ;
#18569=CARTESIAN_POINT ( 'NONE',  ( -23.31991597950000283, 35.31558869410000057, -140.3324749399999973 ) ) ;
#18571=CARTESIAN_POINT ( 'NONE',  ( -30.41918043656675508, 40.92081927820395748, -146.2642377558170494 ) ) ;
#18581=CARTESIAN_POINT ( 'NONE',  ( -23.86695900996863884, 38.68196870774303164, -148.0474502902359859 ) ) ;
#18582=CARTESIAN_POINT ( 'NONE',  ( -15.57778390732538298, 34.09428877113495560, -147.7625705869996580 ) ) ;
#18584=CARTESIAN_POINT ( 'NONE',  ( -19.36113520410000177, 33.15198947340000046, -146.5298456060000092 ) ) ;
#18590=CARTESIAN_POINT ( 'NONE',  ( -5.972224716156503632, 40.79464204724823873, -141.7656025440403766 ) ) ;
#18599=CARTESIAN_POINT ( 'NONE',  ( -22.23138069775068004, 34.62558912611336126, -140.6296127981910047 ) ) ;
#18601=ORIENTED_EDGE ( 'NONE', *, *, #3436, .F. ) ;
#18602=CARTESIAN_POINT ( 'NONE',  ( -12.47706116150000000, 35.17890886639999337, -148.2557368829999973 ) ) ;
#18612=CARTESIAN_POINT ( 'NONE',  ( -28.48845118146442346, 34.53992523626719446, -147.5004638035997573 ) ) ;
#18618=CARTESIAN_POINT ( 'NONE',  ( -14.30645844936410427, 35.39002938633848316, -140.6974358100255529 ) ) ;
#18639=CARTESIAN_POINT ( 'NONE',  ( -27.06022691664431790, 38.83733237976459662, -148.2479545113073982 ) ) ;
#18641=CARTESIAN_POINT ( 'NONE',  ( -22.82187525211859125, 36.04812013258515435, -139.3733050199115837 ) ) ;
#18655=CARTESIAN_POINT ( 'NONE',  ( -8.170418261672836024, 39.82841872393940008, -140.1620592250056347 ) ) ;
#18666=CARTESIAN_POINT ( 'NONE',  ( -12.03885416238175132, 41.13341945414818213, -146.5840868153462964 ) ) ;
#18667=CARTESIAN_POINT ( 'NONE',  ( -17.90603444523116039, 39.81532604249508722, -147.8912533906195961 ) ) ;
#18668=CARTESIAN_POINT ( 'NONE',  ( -28.82642799346931284, 39.82454263016848017, -141.4161836699787784 ) ) ;
#18678=CARTESIAN_POINT ( 'NONE',  ( -20.64937491868320407, 39.51007782554450642, -147.6820107799256050 ) ) ;
#18681=CARTESIAN_POINT ( 'NONE',  ( -27.49486172903679204, 36.99676060752978657, -147.4549925864818931 ) ) ;
#18682=CARTESIAN_POINT ( 'NONE',  ( -11.38486064709999823, 36.95668670079999885, -140.3965526140000009 ) ) ;
#18688=CARTESIAN_POINT ( 'NONE',  ( -10.47418533549999964, 33.50012463689999720, -145.9259304109999960 ) ) ;
#18706=CARTESIAN_POINT ( 'NONE',  ( -8.031950161270000166, 40.75709267670000457, -141.9144354160000034 ) ) ;
#18710=CARTESIAN_POINT ( 'NONE',  ( -24.28961182125106077, 41.32638505982121302, -143.5933768036660751 ) ) ;
#18714=CARTESIAN_POINT ( 'NONE',  ( -17.43215188622844636, 36.07634741369874831, -139.7482345171883082 ) ) ;
#18716=CARTESIAN_POINT ( 'NONE',  ( -18.95027878879999861, 36.16636532760000478, -148.4341920939999966 ) ) ;
#18720=CARTESIAN_POINT ( 'NONE',  ( -5.537589236589999686, 40.52957482200000072, -146.1175057039999956 ) ) ;
#18725=CARTESIAN_POINT ( 'NONE',  ( -21.60271751204859214, 36.29226947926043323, -147.3679125513968131 ) ) ;
#18728=CARTESIAN_POINT ( 'NONE',  ( -12.76385253889189997, 37.02886902030352445, -147.6186336935166139 ) ) ;
#18736=FACE_OUTER_BOUND ( 'NONE', #22614, .T. ) ;
#18738=CARTESIAN_POINT ( 'NONE',  ( -13.82058007329999860, 36.03909227049999942, -139.5626078809999910 ) ) ;
#18739=CARTESIAN_POINT ( 'NONE',  ( -9.178237216079999428, 36.01795878010000251, -148.2568923610000127 ) ) ;
#18757=CARTESIAN_POINT ( 'NONE',  ( -27.77832206610000298, 37.03059619289999915, -147.6270870419999710 ) ) ;
#18758=ORIENTED_EDGE ( 'NONE', *, *, #22749, .T. ) ;
#18759=CARTESIAN_POINT ( 'NONE',  ( -21.73453520646456028, 32.91403690881655564, -144.3663112597476186 ) ) ;
#18764=CARTESIAN_POINT ( 'NONE',  ( -27.66970514971757922, 40.84802520247237823, -146.1653953613356975 ) ) ;
#18768=CARTESIAN_POINT ( 'NONE',  ( -6.323999170589999608, 34.61896835509999448, -147.3311432729999808 ) ) ;
#18773=CARTESIAN_POINT ( 'NONE',  ( -26.61707828802657261, 36.92896776167481221, -139.7487649555727671 ) ) ;
#18775=CARTESIAN_POINT ( 'NONE',  ( -11.42599417689999974, 41.52668172479999953, -143.7505393120000292 ) ) ;
#18789=CARTESIAN_POINT ( 'NONE',  ( -21.18194668304453288, 41.60546844456856519, -144.5792247508281605 ) ) ;
#18791=CARTESIAN_POINT ( 'NONE',  ( -27.02696672876702522, 36.03294499660979966, -148.2622105679788547 ) ) ;
#18805=CARTESIAN_POINT ( 'NONE',  ( -30.53444983796061152, 41.17095381152200417, -144.9066004078397896 ) ) ;
#18817=CARTESIAN_POINT ( 'NONE',  ( -17.68978131335611081, 36.92028947728231714, -140.0842674915936072 ) ) ;
#18823=CARTESIAN_POINT ( 'NONE',  ( -9.611837139799998653, 32.98927337829999829, -146.0840312179999785 ) ) ;
#18828=CARTESIAN_POINT ( 'NONE',  ( -21.78746107307105362, 34.94849561060180321, -146.8035918688234176 ) ) ;
#18833=CARTESIAN_POINT ( 'NONE',  ( -12.14655699389284038, 34.61986692078499317, -147.3395159944840032 ) ) ;
#18840=CARTESIAN_POINT ( 'NONE',  ( -8.462973826026347623, 36.94736262684725858, -140.5165674475847766 ) ) ;
#18842=CARTESIAN_POINT ( 'NONE',  ( -27.47244207672152072, 35.09215423528084443, -148.2237751110284023 ) ) ;
#18856=CARTESIAN_POINT ( 'NONE',  ( -17.71126569018024099, 40.30718541996639459, -145.9389846959718113 ) ) ;
#18861=CARTESIAN_POINT ( 'NONE',  ( -25.70078729276114515, 36.31727625687209837, -140.6851652563827031 ) ) ;
#18874=CARTESIAN_POINT ( 'NONE',  ( -27.57732796661917973, 40.50144436171580509, -145.9796795535191336 ) ) ;
#18877=CARTESIAN_POINT ( 'NONE',  ( -10.76224745929999926, 37.97907322949999553, -139.7231730900000173 ) ) ;
#18881=CARTESIAN_POINT ( 'NONE',  ( -7.728596210859999260, 38.74386132360000090, -140.2295773360000055 ) ) ;
#18889=CARTESIAN_POINT ( 'NONE',  ( -18.60901166351236924, 37.01038625230344792, -148.6497975989735494 ) ) ;
#18898=CARTESIAN_POINT ( 'NONE',  ( -14.34860313725863712, 37.92192996123270632, -139.4939723716648530 ) ) ;
#18900=CARTESIAN_POINT ( 'NONE',  ( -19.92532084488878752, 37.01154022405491872, -139.3892291660223748 ) ) ;
#18903=CARTESIAN_POINT ( 'NONE',  ( -28.90798551749711720, 37.01360947634791643, -139.5686590453459814 ) ) ;
#18922=CARTESIAN_POINT ( 'NONE',  ( -13.40552595227776855, 37.07358616897465708, -140.3498584192782062 ) ) ;
#18929=CARTESIAN_POINT ( 'NONE',  ( -11.38486064709999823, 36.95668670079999885, -140.3965526140000009 ) ) ;
#18930=CARTESIAN_POINT ( 'NONE',  ( -23.10566298545525754, 41.14502951780827544, -141.7794040582555510 ) ) ;
#18948=CARTESIAN_POINT ( 'NONE',  ( -23.03778781520344054, 40.78628791112352303, -141.9896475654208245 ) ) ;
#18956=CARTESIAN_POINT ( 'NONE',  ( -8.925445592990907784, 40.16747143530070474, -142.1449410552589825 ) ) ;
#18963=CARTESIAN_POINT ( 'NONE',  ( -13.82353779650958003, 34.78290842727324161, -141.1681162278995885 ) ) ;
#18965=DIRECTION ( 'NONE',  ( -0.1185248058649825964, -0.4964755458219273776, -0.8599208700778737668 ) ) ;
#18968=ORIENTED_EDGE ( 'NONE', *, *, #15897, .F. ) ;
#18974=CARTESIAN_POINT ( 'NONE',  ( -18.79127896110195906, 39.63013235846046456, -147.4718746916258851 ) ) ;
#18980=CARTESIAN_POINT ( 'NONE',  ( -25.07725372939999886, 36.26300138690000097, -147.8685835880000070 ) ) ;
#19013=CARTESIAN_POINT ( 'NONE',  ( -23.31991597950000283, 35.31558869410000057, -140.3324749399999973 ) ) ;
#19022=CARTESIAN_POINT ( 'NONE',  ( -14.31404048463135936, 38.45176613018843881, -140.7319883511322018 ) ) ;
#19024=CARTESIAN_POINT ( 'NONE',  ( -25.44349950013895878, 35.21826511855759634, -139.9516901550857995 ) ) ;
#19056=CARTESIAN_POINT ( 'NONE',  ( -16.65899329396956219, 33.56230705803076830, -145.9446936787583411 ) ) ;
#19057=CARTESIAN_POINT ( 'NONE',  ( -4.954580150880754097, 37.98786518323144179, -139.3930060029525748 ) ) ;
#19061=CARTESIAN_POINT ( 'NONE',  ( -9.137845891433649115, 36.16121174422281825, -147.5839243320841945 ) ) ;
#19073=CARTESIAN_POINT ( 'NONE',  ( -13.40552595227776855, 37.07358616897465708, -140.3498584192782062 ) ) ;
#19077=CARTESIAN_POINT ( 'NONE',  ( -5.537589236589999686, 40.52957482200000072, -146.1175057039999956 ) ) ;
#19084=( BOUNDED_CURVE ( )  B_SPLINE_CURVE ( 5, ( #17555, #1271, #8494, #15764, #6712, #4939 ),
 .UNSPECIFIED., .F., .F. ) 
 B_SPLINE_CURVE_WITH_KNOTS ( ( 6, 6 ),
 ( 0.000000000000000000, 1.570796326505558671 ),
 .UNSPECIFIED. ) 
 CURVE ( )  GEOMETRIC_REPRESENTATION_ITEM ( )  RATIONAL_B_SPLINE_CURVE ( ( 1.000000000000000000, 0.6000000000737055750, 0.4000000000737055639, 0.3000000000552791590, 0.2500000000368527431, 0.2500000000000000000 ) ) 
 REPRESENTATION_ITEM ( '' )  );
#19086=CARTESIAN_POINT ( 'NONE',  ( -6.713398844220000328, 32.91877557720000169, -144.5413327229999823 ) ) ;
#19087=CARTESIAN_POINT ( 'NONE',  ( -25.84964047060000070, 38.84307078620000198, -139.9757795270000145 ) ) ;
#19088=PLANE ( 'NONE',  #13844 ) ;
#19092=CARTESIAN_POINT ( 'NONE',  ( -14.80611810279999929, 41.62812440830000327, -144.5263372940000011 ) ) ;
#19095=CARTESIAN_POINT ( 'NONE',  ( -17.86540859994439145, 40.46207760455489222, -144.3551126902200110 ) ) ;
#19099=CARTESIAN_POINT ( 'NONE',  ( -25.38678224704462494, 37.07582353397745578, -140.0279244688365168 ) ) ;
#19106=CARTESIAN_POINT ( 'NONE',  ( -26.86963863710373701, 36.92213009831746007, -147.8538433455846359 ) ) ;
#19111=EDGE_LOOP ( 'NONE', ( #18305, #8886, #12759, #13784 ) ) ;
#19115=FACE_OUTER_BOUND ( 'NONE', #21593, .T. ) ;
#19121=CARTESIAN_POINT ( 'NONE',  ( -27.36723106709999698, 36.02973761859999513, -148.4771530680000353 ) ) ;
#19141=CARTESIAN_POINT ( 'NONE',  ( -24.99941573887451796, 32.27097850041364069, -144.5668997986605007 ) ) ;
#19149=VERTEX_POINT ( 'NONE', #1976 ) ;
#19168=CARTESIAN_POINT ( 'NONE',  ( -17.13033207850000039, 36.08498863180000171, -139.6042211940000186 ) ) ;
#19175=CARTESIAN_POINT ( 'NONE',  ( -9.447016884546547644, 33.25211036581616497, -145.9271147563237321 ) ) ;
#19178=ORIENTED_EDGE ( 'NONE', *, *, #1122, .T. ) ;
#19181=CARTESIAN_POINT ( 'NONE',  ( -29.29455083639855673, 36.96746664034980512, -139.4767999530844520 ) ) ;
#19184=CARTESIAN_POINT ( 'NONE',  ( -23.77821355560346817, 39.18276288788521811, -141.0264728964231153 ) ) ;
#19189=CARTESIAN_POINT ( 'NONE',  ( -10.75221293931074129, 33.20739279160920177, -143.4848104350353992 ) ) ;
#19191=CARTESIAN_POINT ( 'NONE',  ( -8.748495699880534104, 39.09191467989751345, -141.0690580214405259 ) ) ;
#19194=ORIENTED_EDGE ( 'NONE', *, *, #307, .F. ) ;
#19195=CARTESIAN_POINT ( 'NONE',  ( -7.187032243693241895, 34.73215247832149544, -140.9426763503612676 ) ) ;
#19197=CARTESIAN_POINT ( 'NONE',  ( -20.76253627919999900, 39.57534689110000414, -140.5049880910000013 ) ) ;
#19200=CARTESIAN_POINT ( 'NONE',  ( -14.23530246729999860, 39.72954597060000026, -140.2988105550000171 ) ) ;
#19205=CARTESIAN_POINT ( 'NONE',  ( -18.02589426845994680, 40.09893371072652002, -145.7828789349928229 ) ) ;
#19211=CARTESIAN_POINT ( 'NONE',  ( -25.17085604102206275, 34.85061541308337496, -141.0238190163674687 ) ) ;
#19214=CARTESIAN_POINT ( 'NONE',  ( -11.36739930689422451, 37.96852355311366978, -139.4217770014837754 ) ) ;
#19227=CARTESIAN_POINT ( 'NONE',  ( -19.04867772230000256, 35.29145880730000329, -148.2212826610000036 ) ) ;
#19228=CARTESIAN_POINT ( 'NONE',  ( -10.89103387395912215, 38.50335587980050889, -140.8674315661253331 ) ) ;
#19230=CARTESIAN_POINT ( 'NONE',  ( -6.808372428180324398, 32.54462665076120231, -143.6393730288246218 ) ) ;
#19231=CARTESIAN_POINT ( 'NONE',  ( -9.353760014424715052, 38.97728680361760922, -148.4651161360701508 ) ) ;
#19251=CARTESIAN_POINT ( 'NONE',  ( -26.11589873370086323, 33.33025833338455612, -142.0389129396357362 ) ) ;
#19257=CARTESIAN_POINT ( 'NONE',  ( -11.68420994730000118, 39.25205177019999780, -141.0178453350000041 ) ) ;
#19269=COLOUR_RGB ( '', 0.09019608, 0.27058824, 0.51372549) ;
#19274=CARTESIAN_POINT ( 'NONE',  ( -13.69950222120749928, 37.97208955950073772, -139.6409136025020246 ) ) ;
#19279=EDGE_CURVE ( 'NONE', #4474, #9000, #5248, .T. ) ;
#19285=CARTESIAN_POINT ( 'NONE',  ( -16.72821278489138663, 35.17558473326719337, -139.6880632856704381 ) ) ;
#19296=FACE_OUTER_BOUND ( 'NONE', #8942, .T. ) ;
#19304=CARTESIAN_POINT ( 'NONE',  ( -23.25111789197735845, 40.11822973618910027, -142.3379301973523923 ) ) ;
#19310=CARTESIAN_POINT ( 'NONE',  ( -9.394775000179999225, 34.25903911019999981, -147.4808749560000081 ) ) ;
#19319=CARTESIAN_POINT ( 'NONE',  ( -6.817148331763788427, 33.23134552036847111, -143.6958372513363145 ) ) ;
#19328=CARTESIAN_POINT ( 'NONE',  ( -21.12162747662785733, 36.95220905036273962, -147.5578847871555581 ) ) ;
#19330=CARTESIAN_POINT ( 'NONE',  ( -18.18725233745032455, 40.59074569709380853, -143.5523115782840193 ) ) ;
#19333=CARTESIAN_POINT ( 'NONE',  ( -13.11071995283477420, 37.07027326795080313, -147.8134892432881884 ) ) ;
#19335=CARTESIAN_POINT ( 'NONE',  ( -24.20723148424393756, 36.23170097884169394, -147.4988838138595213 ) ) ;
#19350=CARTESIAN_POINT ( 'NONE',  ( -28.94327676059999988, 35.53474617860000251, -140.7339624629999832 ) ) ;
#19355=CARTESIAN_POINT ( 'NONE',  ( -19.19584323397005221, 36.24030718097106529, -148.2165564152711568 ) ) ;
#19360=CARTESIAN_POINT ( 'NONE',  ( -8.343166633029998280, 41.26425690090000131, -144.5268661329999986 ) ) ;
#19365=( BOUNDED_CURVE ( )  B_SPLINE_CURVE ( 5, ( #7242, #19969, #21650, #9126, #14149, #5212 ),
 .UNSPECIFIED., .F., .F. ) 
 B_SPLINE_CURVE_WITH_KNOTS ( ( 6, 6 ),
 ( 0.000000000000000000, 1.570796326852883729 ),
 .UNSPECIFIED. ) 
 CURVE ( )  GEOMETRIC_REPRESENTATION_ITEM ( )  RATIONAL_B_SPLINE_CURVE ( ( 1.000000000000000000, 0.5999999999852601018, 0.3999999999852600907, 0.2999999999889450542, 0.2499999999926300620, 0.2500000000000000000 ) ) 
 REPRESENTATION_ITEM ( '' )  );
#19377=CARTESIAN_POINT ( 'NONE',  ( -23.54789306460687826, 36.93722613941783806, -139.7713821671024448 ) ) ;
#19381=CARTESIAN_POINT ( 'NONE',  ( -14.80611810279999929, 41.62812440830000327, -144.5263372940000011 ) ) ;
#19382=CARTESIAN_POINT ( 'NONE',  ( -25.91744746520000220, 33.58572460659999592, -142.1592104600000255 ) ) ;
#19403=CARTESIAN_POINT ( 'NONE',  ( -14.35172583810447478, 40.49725901027402841, -146.1414193758190549 ) ) ;
#19412=EDGE_CURVE ( 'NONE', #16477, #22408, #21332, .T. ) ;
#19417=CARTESIAN_POINT ( 'NONE',  ( -8.008464111600000379, 33.29536412539999901, -142.0809313899999893 ) ) ;
#19421=ADVANCED_FACE ( 'NONE', ( #12277 ), #9326, .F. ) ;
#19424=CARTESIAN_POINT ( 'NONE',  ( -28.70612892851496056, 35.15950212976387235, -139.8035036602401817 ) ) ;
#19427=CARTESIAN_POINT ( 'NONE',  ( -23.71856152630000025, 38.62313066519999438, -140.3058339320000130 ) ) ;
#19431=MANIFOLD_SOLID_BREP ( 'lock_assembly.1\\Product1.1\\spring.1\\PartBody', #61 ) ;
#19435=CARTESIAN_POINT ( 'NONE',  ( -9.611837139799998653, 32.98927337829999829, -146.0840312179999785 ) ) ;
#19448=CARTESIAN_POINT ( 'NONE',  ( -7.406300769258751693, 33.57817176939022374, -144.5322665435940053 ) ) ;
#19449=CARTESIAN_POINT ( 'NONE',  ( -26.95224972460000146, 39.68365438100000375, -147.7577323689999957 ) ) ;
#19458=CARTESIAN_POINT ( 'NONE',  ( -21.40343141177097053, 37.68083471479108226, -147.3689155900011372 ) ) ;
#19464=CARTESIAN_POINT ( 'NONE',  ( -17.55745234320252024, 36.93608508457233341, -140.4812394865590761 ) ) ;
#19485=CARTESIAN_POINT ( 'NONE',  ( -6.713398844220000328, 32.91877557720000169, -144.5413327229999823 ) ) ;
#19496=CARTESIAN_POINT ( 'NONE',  ( -20.93854596069999729, 37.74500530009999721, -147.9603137869999898 ) ) ;
#19499=CARTESIAN_POINT ( 'NONE',  ( -23.32853373983441969, 36.96341023004794835, -139.4571126577996836 ) ) ;
#19502=CARTESIAN_POINT ( 'NONE',  ( -15.46613156833100078, 36.99333119719623397, -147.5584717933785726 ) ) ;
#19503=CARTESIAN_POINT ( 'NONE',  ( -25.46021907539999773, 33.59345108530000346, -146.1038275270000213 ) ) ;
#19512=( BOUNDED_CURVE ( )  B_SPLINE_CURVE ( 5, ( #329, #20326, #4019, #11247, #2240, #9461 ),
 .UNSPECIFIED., .F., .F. ) 
 B_SPLINE_CURVE_WITH_KNOTS ( ( 6, 6 ),
 ( 0.000000000000000000, 1.570796326712887714 ),
 .UNSPECIFIED. ) 
 CURVE ( )  GEOMETRIC_REPRESENTATION_ITEM ( )  RATIONAL_B_SPLINE_CURVE ( ( 1.000000000000000000, 0.6000000000209096962, 0.4000000000209096296, 0.3000000000156822222, 0.2500000000104548037, 0.2499999999999999445 ) ) 
 REPRESENTATION_ITEM ( '' )  );
#19514=CARTESIAN_POINT ( 'NONE',  ( -24.26662447749999885, 35.20109951629999756, -148.0073960930000112 ) ) ;
#19521=CARTESIAN_POINT ( 'NONE',  ( -14.84561440075239780, 36.91926241633263572, -147.9647079511389620 ) ) ;
#19522=CARTESIAN_POINT ( 'NONE',  ( -28.59509960825648278, 39.22088873720170454, -140.4143345430010470 ) ) ;
#19528=CARTESIAN_POINT ( 'NONE',  ( -24.10813950047970522, 36.95059904179322530, -147.5089432696624954 ) ) ;
#19550=VERTEX_POINT ( 'NONE', #15005 ) ;
#19551=CARTESIAN_POINT ( 'NONE',  ( -9.319507568709141765, 35.96837468366262414, -148.5620496009611884 ) ) ;
#19553=CARTESIAN_POINT ( 'NONE',  ( -8.314736843700092805, 40.56062062648400257, -143.6903644850042099 ) ) ;
#19558=CARTESIAN_POINT ( 'NONE',  ( -21.12031522135587380, 37.91567797510568028, -148.6783548734256328 ) ) ;
#19560=CARTESIAN_POINT ( 'NONE',  ( -7.811725169189109863, 33.27862147039694207, -143.8116909731542705 ) ) ;
#19561=CARTESIAN_POINT ( 'NONE',  ( -5.762834417829999722, 39.50865942520000118, -140.4825946859999988 ) ) ;
#19574=CARTESIAN_POINT ( 'NONE',  ( -12.76385253890000016, 37.02886902030000016, -147.6186336929999925 ) ) ;
#19581=CARTESIAN_POINT ( 'NONE',  ( -22.56584646716593667, 37.05444931714164625, -139.6092474954592433 ) ) ;
#19588=CARTESIAN_POINT ( 'NONE',  ( -28.28132655699793929, 35.56853653578105678, -140.6131719533408102 ) ) ;
#19593=CARTESIAN_POINT ( 'NONE',  ( -9.674592407259998694, 39.37273218290000187, -147.1879168910000146 ) ) ;
#19595=CARTESIAN_POINT ( 'NONE',  ( -11.32406291796261399, 40.56182626977977179, -143.8345514045001892 ) ) ;
#19610=CARTESIAN_POINT ( 'NONE',  ( -19.92532084500992440, 37.01154022404042365, -139.3892291660651779 ) ) ;
#19613=CARTESIAN_POINT ( 'NONE',  ( -15.90674982584208941, 37.04592612750104053, -148.5146100863323966 ) ) ;
#19626=CARTESIAN_POINT ( 'NONE',  ( -13.47165290130000059, 33.35876621949999787, -143.8174469059999865 ) ) ;
#19630=CARTESIAN_POINT ( 'NONE',  ( -14.97130487713839919, 37.69282299035099015, -147.6145025267201447 ) ) ;
#19633=ORIENTED_EDGE ( 'NONE', *, *, #2702, .F. ) ;
#19645=CARTESIAN_POINT ( 'NONE',  ( -6.807579269548480028, 38.78453684422532177, -147.8970667729606134 ) ) ;
#19646=CARTESIAN_POINT ( 'NONE',  ( -24.68730002459999895, 39.33688142210000649, -147.2285014869999884 ) ) ;
#19663=CARTESIAN_POINT ( 'NONE',  ( -18.18930989808823995, 36.96028804432864234, -147.6841622078175931 ) ) ;
#19672=CARTESIAN_POINT ( 'NONE',  ( -5.972224716009999490, 40.79464204750000533, -141.7656025439999894 ) ) ;
#19692=ORIENTED_EDGE ( 'NONE', *, *, #6481, .T. ) ;
#19701=CARTESIAN_POINT ( 'NONE',  ( -27.83857872746931506, 33.37060406817593616, -143.5613806138642872 ) ) ;
#19707=CARTESIAN_POINT ( 'NONE',  ( -19.58896675450998615, 35.53469097119599240, -140.8466141450865621 ) ) ;
#19708=CARTESIAN_POINT ( 'NONE',  ( -11.19078917913330962, 40.90943599255746932, -144.6700718817450593 ) ) ;
#19726=CARTESIAN_POINT ( 'NONE',  ( -19.59255166829999695, 37.05126161860000167, -140.3061871179999969 ) ) ;
#19731=ADVANCED_BREP_SHAPE_REPRESENTATION ( '', ( #19431, #5025 ), #3911 ) ;
#19733=CARTESIAN_POINT ( 'NONE',  ( -15.17828643423089829, 39.13746915041124197, -146.9793796816295810 ) ) ;
#19740=FACE_OUTER_BOUND ( 'NONE', #16253, .T. ) ;
#19746=CARTESIAN_POINT ( 'NONE',  ( -10.84486070616090991, 35.03979930411003352, -141.1912331422082900 ) ) ;
#19757=CARTESIAN_POINT ( 'NONE',  ( -14.12939694657403678, 41.07986042234944080, -141.7257002008347229 ) ) ;
#19758=CARTESIAN_POINT ( 'NONE',  ( -28.79441775903490353, 39.40253724237003041, -140.0594529943023758 ) ) ;
#19765=CARTESIAN_POINT ( 'NONE',  ( -24.06602356359999817, 36.94557182220000158, -148.2530914610000252 ) ) ;
#19786=CARTESIAN_POINT ( 'NONE',  ( -30.05504742970118670, 39.87093548741106019, -141.1846073849872312 ) ) ;
#19790=CARTESIAN_POINT ( 'NONE',  ( -10.56415788819999868, 36.18163687389999694, -139.7056672729999889 ) ) ;
#19792=CARTESIAN_POINT ( 'NONE',  ( -18.56307309666442862, 32.92303375952681677, -144.6176528170184099 ) ) ;
#19793=CARTESIAN_POINT ( 'NONE',  ( -8.831009117212259341, 37.75574244304178961, -147.9814132533029465 ) ) ;
#19801=CARTESIAN_POINT ( 'NONE',  ( -23.76507348470000025, 39.47303768190000284, -147.6024660349999920 ) ) ;
#19807=CARTESIAN_POINT ( 'NONE',  ( -18.08788331839999941, 37.73304001160000354, -147.6923967950000076 ) ) ;
#19832=CARTESIAN_POINT ( 'NONE',  ( -11.85909339607291457, 36.92087135288571886, -147.9691652862101421 ) ) ;
#19852=CARTESIAN_POINT ( 'NONE',  ( -16.06083392305800928, 37.86731064063600627, -147.7990361411401068 ) ) ;
#19856=( BOUNDED_CURVE ( )  B_SPLINE_CURVE ( 5, ( #14160, #12123, #15592, #11763, #2754, #23202 ),
 .UNSPECIFIED., .F., .F. ) 
 B_SPLINE_CURVE_WITH_KNOTS ( ( 6, 6 ),
 ( 0.000000000000000000, 1.570796326702242673 ),
 .UNSPECIFIED. ) 
 CURVE ( )  GEOMETRIC_REPRESENTATION_ITEM ( )  RATIONAL_B_SPLINE_CURVE ( ( 1.000000000000000000, 0.6000000000236205278, 0.4000000000236205167, 0.3000000000177153736, 0.2500000000118102750, 0.2500000000000000000 ) ) 
 REPRESENTATION_ITEM ( '' )  );
#19858=CARTESIAN_POINT ( 'NONE',  ( -25.84964047037207990, 38.84307078610155628, -139.9757795274772150 ) ) ;
#19864=EDGE_CURVE ( 'NONE', #14150, #3155, #13303, .T. ) ;
#19867=EDGE_CURVE ( 'NONE', #22408, #3155, #8190, .T. ) ;
#19873=CARTESIAN_POINT ( 'NONE',  ( -10.88504013570612905, 37.01634837951200296, -139.4704149077907402 ) ) ;
#19889=CARTESIAN_POINT ( 'NONE',  ( -5.659867863851591352, 38.70771930245251724, -140.0293976192359935 ) ) ;
#19900=CARTESIAN_POINT ( 'NONE',  ( -30.24848017571688175, 41.17617824351370359, -142.4709749654889208 ) ) ;
#19906=CARTESIAN_POINT ( 'NONE',  ( -19.07674765109432613, 34.46746647540513209, -140.6674949932227889 ) ) ;
#19907=CARTESIAN_POINT ( 'NONE',  ( -9.194386776583943544, 38.39074869067930251, -147.2010703919465300 ) ) ;
#19914=CARTESIAN_POINT ( 'NONE',  ( -6.498948513140000216, 40.81543345029999870, -146.1568765789999986 ) ) ;
#19918=CARTESIAN_POINT ( 'NONE',  ( -5.558768696205168780, 37.82651365787447872, -139.8085169319456043 ) ) ;
#19920=EDGE_LOOP ( 'NONE', ( #21277, #1480, #13389, #1673 ) ) ;
#19922=CARTESIAN_POINT ( 'NONE',  ( -19.10036853998401085, 37.06903765908931803, -148.2030617969537616 ) ) ;
#19924=CARTESIAN_POINT ( 'NONE',  ( -25.10891061336687358, 37.07005729393736004, -148.1636427047451718 ) ) ;
#19935=ORIENTED_EDGE ( 'NONE', *, *, #7566, .T. ) ;
#19936=CARTESIAN_POINT ( 'NONE',  ( -16.12052341118245380, 35.09110744045798924, -148.2635301759968343 ) ) ;
#19943=CARTESIAN_POINT ( 'NONE',  ( -20.45144833149999997, 36.94873838139999833, -139.8044047869999815 ) ) ;
#19944=CARTESIAN_POINT ( 'NONE',  ( -11.97832217620000073, 39.59660284089999749, -147.8163995769999985 ) ) ;
#19960=CARTESIAN_POINT ( 'NONE',  ( -27.04496201379999931, 40.71797592360000095, -143.5957174049999878 ) ) ;
#19962=CARTESIAN_POINT ( 'NONE',  ( -20.95225485081686045, 36.93199168239783603, -148.3394883767275019 ) ) ;
#19968=CARTESIAN_POINT ( 'NONE',  ( -26.45246943592391631, 41.22394968972064788, -141.5932472704602958 ) ) ;
#19969=CARTESIAN_POINT ( 'NONE',  ( -10.43323856990612342, 37.07027821888498664, -139.9576636760149597 ) ) ;
#19984=CARTESIAN_POINT ( 'NONE',  ( -16.85333322537449519, 40.81111939231837482, -141.8642558381071694 ) ) ;
#19985=CARTESIAN_POINT ( 'NONE',  ( -28.92883298428190031, 41.10844391202770254, -142.6522296194680166 ) ) ;
#19989=( BOUNDED_CURVE ( )  B_SPLINE_CURVE ( 5, ( #18929, #8325, #22864, #6432, #1331, #4533 ),
 .UNSPECIFIED., .F., .F. ) 
 B_SPLINE_CURVE_WITH_KNOTS ( ( 6, 6 ),
 ( 1.570796326852883729, 3.141592653590000062 ),
 .UNSPECIFIED. ) 
 CURVE ( )  GEOMETRIC_REPRESENTATION_ITEM ( )  RATIONAL_B_SPLINE_CURVE ( ( 0.2500000000000000000, 0.2500000000073699935, 0.3000000000110549792, 0.4000000000147399537, 0.6000000000147399648, 1.000000000000000000 ) ) 
 REPRESENTATION_ITEM ( '' )  );
#20002=B_SPLINE_CURVE_WITH_KNOTS ( 'NONE', 5,
 ( #9315, #18739, #423, #779, #5764, #18493, #14931, #22302, #14820, #5877, #651, #9667 ),
 .UNSPECIFIED., .F., .F.,
 ( 6, 3, 3, 6 ),
 ( 0.000000000000000000, 4.570086947620000117, 8.869210483019999813, 12.91901055009999943 ),
 .UNSPECIFIED. ) ;
#20003=CARTESIAN_POINT ( 'NONE',  ( -5.958543189560369768, 38.89133234075744383, -148.3841615053280805 ) ) ;
#20006=CARTESIAN_POINT ( 'NONE',  ( -27.30725598840000146, 40.30964169850000189, -145.9048855949999961 ) ) ;
#20013=CARTESIAN_POINT ( 'NONE',  ( -24.78261485200000180, 38.62237172060000034, -147.6366313890000015 ) ) ;
#20020=SURFACE_SIDE_STYLE ('',( #8932 ) ) ;
#20021=CARTESIAN_POINT ( 'NONE',  ( -19.36113520410000177, 33.15198947340000046, -146.5298456060000092 ) ) ;
#20023=CARTESIAN_POINT ( 'NONE',  ( -9.072898850179999641, 36.94639249900000522, -148.2684494029999769 ) ) ;
#20029=EDGE_CURVE ( 'NONE', #2371, #7237, #11760, .T. ) ;
#20032=CARTESIAN_POINT ( 'NONE',  ( -5.558768696030000456, 37.82651365799999610, -139.8085169320000034 ) ) ;
#20035=CARTESIAN_POINT ( 'NONE',  ( -6.346791270776173555, 40.13779649986400955, -145.7921771525873567 ) ) ;
#20041=CARTESIAN_POINT ( 'NONE',  ( -24.06602356352919969, 36.94557182214808222, -148.2530914607175703 ) ) ;
#20054=CARTESIAN_POINT ( 'NONE',  ( -16.69741762601382717, 33.17454851232909618, -146.1538744914665244 ) ) ;
#20061=CARTESIAN_POINT ( 'NONE',  ( -19.36113520410000177, 33.15198947340000046, -146.5298456060000092 ) ) ;
#20080=CARTESIAN_POINT ( 'NONE',  ( -25.89998524117842393, 37.72641173383139801, -140.6959480270122640 ) ) ;
#20082=CARTESIAN_POINT ( 'NONE',  ( -23.22224815339999893, 34.57381638260000045, -140.7548632179999970 ) ) ;
#20088=CARTESIAN_POINT ( 'NONE',  ( -24.97797643630000053, 37.05442817780000553, -147.8575004449999994 ) ) ;
#20113=CARTESIAN_POINT ( 'NONE',  ( -17.97686571119999854, 41.53571570570000659, -143.4577736070000071 ) ) ;
#20119=PRODUCT_DEFINITION ( 'UNKNOWN', '', #8864, #8732 ) ;
#20123=CARTESIAN_POINT ( 'NONE',  ( -5.832642628619999492, 38.59814668869999821, -147.7665506369999662 ) ) ;
#20135=( BOUNDED_CURVE ( )  B_SPLINE_CURVE ( 5, ( #12261, #21325, #14057, #18417, #12936, #12143, #23336, #19417, #7460, #12492, #8676, #17865 ),
 .UNSPECIFIED., .F., .F. ) 
 B_SPLINE_CURVE_WITH_KNOTS ( ( 6, 3, 3, 6 ),
 ( 0.000000000000000000, 4.346865784160000246, 8.778337911509998648, 13.29702284770000098 ),
 .UNSPECIFIED. ) 
 CURVE ( )  GEOMETRIC_REPRESENTATION_ITEM ( )  RATIONAL_B_SPLINE_CURVE ( ( 0.2500000000000000000, 0.2500000000000000000, 0.2500000000000000000, 0.2500000000000000000, 0.2500000000000000000, 0.2500000000000000000, 0.2500000000000000000, 0.2500000000000000000, 0.2500000000000000000, 0.2500000000000000000, 0.2500000000000000000, 0.2500000000000000000 ) ) 
 REPRESENTATION_ITEM ( '' )  );
#20144=FILL_AREA_STYLE_COLOUR ( '', #19269 ) ;
#20145=EDGE_CURVE ( 'NONE', #10397, #4660, #4480, .T. ) ;
#20146=CARTESIAN_POINT ( 'NONE',  ( -18.75678166064549757, 32.44474377655248531, -143.7296912422551429 ) ) ;
#20159=CARTESIAN_POINT ( 'NONE',  ( -6.033650297970000409, 36.94170754819999303, -147.9652040070000112 ) ) ;
#20167=CARTESIAN_POINT ( 'NONE',  ( -13.04270098972981984, 34.92521805811855984, -147.0831430691404194 ) ) ;
#20183=CARTESIAN_POINT ( 'NONE',  ( -12.94305406498005162, 37.05025962682652363, -148.5780888799759794 ) ) ;
#20188=CARTESIAN_POINT ( 'NONE',  ( -19.89396978539216576, 32.81765722514309402, -143.8793666190109661 ) ) ;
#20193=CARTESIAN_POINT ( 'NONE',  ( -20.82021697191324705, 38.61793539557643129, -140.2922895080757257 ) ) ;
#20207=CARTESIAN_POINT ( 'NONE',  ( -23.41786221899999987, 36.12684018730000446, -140.1150171360000058 ) ) ;
#20209=CARTESIAN_POINT ( 'NONE',  ( -29.64895016830000429, 40.48034887659999725, -142.7934167989999992 ) ) ;
#20214=CARTESIAN_POINT ( 'NONE',  ( -23.61758233950000019, 37.78045452579999619, -140.0909254550000185 ) ) ;
#20217=CARTESIAN_POINT ( 'NONE',  ( -11.19828263951698055, 35.50589712222299710, -140.5907466442008058 ) ) ;
#20228=CARTESIAN_POINT ( 'NONE',  ( -12.88538148427827679, 39.54446768249285071, -147.5580768661236277 ) ) ;
#20229=CARTESIAN_POINT ( 'NONE',  ( -17.17121306734199493, 41.35383210599469095, -144.5122939762497936 ) ) ;
#20230=CARTESIAN_POINT ( 'NONE',  ( -30.02200000005139913, 40.89711431701928035, -146.3052959529881889 ) ) ;
#20233=CARTESIAN_POINT ( 'NONE',  ( -25.46206384041683535, 37.06683745569177546, -140.4480127388158905 ) ) ;
#20238=CARTESIAN_POINT ( 'NONE',  ( -19.64847913693946069, 38.01206741062298988, -139.5740658646235488 ) ) ;
#20242=CARTESIAN_POINT ( 'NONE',  ( -27.16804840547268540, 34.58594410721605783, -147.1822449632341829 ) ) ;
#20244=CARTESIAN_POINT ( 'NONE',  ( -12.47706116150000000, 35.17890886639999337, -148.2557368829999973 ) ) ;
#20256=CARTESIAN_POINT ( 'NONE',  ( -22.69591931514189298, 36.33656945782036729, -140.6974727659104758 ) ) ;
#20257=CARTESIAN_POINT ( 'NONE',  ( -29.68301555213733423, 36.92109708053600770, -140.1550845752329053 ) ) ;
#20262=CARTESIAN_POINT ( 'NONE',  ( -18.91006587267516181, 33.19603641716903297, -143.7906546518633775 ) ) ;
#20265=CARTESIAN_POINT ( 'NONE',  ( -23.47736846006178979, 41.31403509295417820, -141.6371185060827429 ) ) ;
#20272=CARTESIAN_POINT ( 'NONE',  ( -5.621737161624158041, 40.23839945177277855, -145.9417178035539848 ) ) ;
#20277=CARTESIAN_POINT ( 'NONE',  ( -24.73161923030975373, 36.03940581491394823, -148.7361830015362045 ) ) ;
#20279=CARTESIAN_POINT ( 'NONE',  ( -13.02237250279999969, 32.42872598539999274, -144.6889042450000034 ) ) ;
#20298=ORIENTED_EDGE ( 'NONE', *, *, #3948, .F. ) ;
#20304=CARTESIAN_POINT ( 'NONE',  ( -20.90175983535185011, 40.40386100034367445, -144.4637348342631356 ) ) ;
#20306=CARTESIAN_POINT ( 'NONE',  ( -17.18002735250068369, 36.98113687426175034, -140.6755148967653497 ) ) ;
#20314=CARTESIAN_POINT ( 'NONE',  ( -27.30725598840000146, 40.30964169850000189, -145.9048855949999961 ) ) ;
#20318=CARTESIAN_POINT ( 'NONE',  ( -21.70515251718890326, 32.50310406744011971, -144.3999433124957363 ) ) ;
#20326=CARTESIAN_POINT ( 'NONE',  ( -29.45815224828859868, 36.94793816027001299, -140.4653836173399952 ) ) ;
#20327=CARTESIAN_POINT ( 'NONE',  ( -14.74965217829999986, 40.59671102100000439, -143.6490422509999973 ) ) ;
#20331=CARTESIAN_POINT ( 'NONE',  ( -7.572469997257414320, 37.05365869149854774, -139.6601318950708048 ) ) ;
#20338=CARTESIAN_POINT ( 'NONE',  ( -12.36981052416691362, 38.87293897908389084, -148.4153451430249504 ) ) ;
#20340=CARTESIAN_POINT ( 'NONE',  ( -29.54694772409695247, 41.21849320775534409, -145.7548069272761211 ) ) ;
#20345=CARTESIAN_POINT ( 'NONE',  ( -28.42317279839999955, 33.35748734759999934, -144.4144508710000139 ) ) ;
#20349=CARTESIAN_POINT ( 'NONE',  ( -21.08990197296929026, 41.23523075628224888, -146.5634232099747578 ) ) ;
#20363=CARTESIAN_POINT ( 'NONE',  ( -22.79386933271686999, 37.02723109250344891, -140.7029355817511771 ) ) ;
#20375=CARTESIAN_POINT ( 'NONE',  ( -24.30767937719999949, 40.97374044589999897, -144.4830919949999952 ) ) ;
#20377=CARTESIAN_POINT ( 'NONE',  ( -15.24898703719208548, 36.96741147810104167, -148.5896301378323585 ) ) ;
#20378=CARTESIAN_POINT ( 'NONE',  ( -18.85469010170000459, 37.03971195569999963, -148.4264296979999926 ) ) ;
#20382=CARTESIAN_POINT ( 'NONE',  ( -6.498948513235520252, 40.81543345002808110, -146.1568765785555968 ) ) ;
#20388=CARTESIAN_POINT ( 'NONE',  ( -23.01751655211429437, 33.66177664240989742, -142.1309265747219115 ) ) ;
#20391=CARTESIAN_POINT ( 'NONE',  ( -12.63629858846534404, 32.85239007250503107, -143.6876766073750957 ) ) ;
#20401=CARTESIAN_POINT ( 'NONE',  ( -28.69387994521298069, 33.30271062198844589, -146.2196849097338429 ) ) ;
#20404=FACE_OUTER_BOUND ( 'NONE', #7243, .T. ) ;
#20412=CARTESIAN_POINT ( 'NONE',  ( -20.76253627919999900, 39.57534689110000414, -140.5049880910000013 ) ) ;
#20424=CARTESIAN_POINT ( 'NONE',  ( -26.72208319964573775, 38.71204575040589901, -148.0666639806206035 ) ) ;
#20426=CARTESIAN_POINT ( 'NONE',  ( -23.54789306461742626, 36.93722613941654487, -139.7713821669921117 ) ) ;
#20433=CARTESIAN_POINT ( 'NONE',  ( -27.05559917085387056, 41.25481893626260899, -146.4757227208741597 ) ) ;
#20438=CARTESIAN_POINT ( 'NONE',  ( -5.974012367538351853, 36.93458879463114641, -148.2930816546007122 ) ) ;
#20441=FACE_OUTER_BOUND ( 'NONE', #8267, .T. ) ;
#20451=CARTESIAN_POINT ( 'NONE',  ( -12.16288092095636308, 40.58801103627050821, -142.0245251747066391 ) ) ;
#20453=CARTESIAN_POINT ( 'NONE',  ( -17.91974642297896381, 36.92811127467702903, -148.3783205066630444 ) ) ;
#20456=CARTESIAN_POINT ( 'NONE',  ( -6.131111726649999483, 36.14321585209999910, -147.9535578170000178 ) ) ;
#20463=CARTESIAN_POINT ( 'NONE',  ( -20.26899604979344005, 40.93030953051304266, -143.7497896408696363 ) ) ;
#20464=VERTEX_POINT ( 'NONE', #6842 ) ;
#20465=CARTESIAN_POINT ( 'NONE',  ( -26.97085048307042854, 36.11604132840786718, -147.8376774906664366 ) ) ;
#20474=CARTESIAN_POINT ( 'NONE',  ( -20.45144833149999997, 36.94873838139999833, -139.8044047869999815 ) ) ;
#20487=CARTESIAN_POINT ( 'NONE',  ( -7.628878236750000319, 37.90286001179999431, -140.0026079769999683 ) ) ;
#20492=CARTESIAN_POINT ( 'NONE',  ( -23.64871425658228432, 39.79993930545538916, -140.2199279868687256 ) ) ;
#20493=CARTESIAN_POINT ( 'NONE',  ( -15.07147389515268721, 36.94622240755791864, -147.6034838243276113 ) ) ;
#20494=CARTESIAN_POINT ( 'NONE',  ( -16.13502618060000060, 32.80445174449999968, -146.2787800969999807 ) ) ;
#20500=CARTESIAN_POINT ( 'NONE',  ( -5.844227446867898301, 38.54059235905305059, -140.3554711806842477 ) ) ;
#20508=CARTESIAN_POINT ( 'NONE',  ( -22.56645868524751464, 33.58406826459463446, -146.0350363999489502 ) ) ;
#20510=VERTEX_POINT ( 'NONE', #23268 ) ;
#20511=CARTESIAN_POINT ( 'NONE',  ( -12.21344923919432546, 35.51569570616177174, -147.3850191185591143 ) ) ;
#20512=CARTESIAN_POINT ( 'NONE',  ( -16.45586251407963729, 37.06757768449541146, -140.3467090679219780 ) ) ;
#20524=CARTESIAN_POINT ( 'NONE',  ( -12.87353035906786047, 34.29620811505558464, -147.9524828210263934 ) ) ;
#20531=CARTESIAN_POINT ( 'NONE',  ( -20.61753010269738340, 36.92891383027765784, -140.0927360959155976 ) ) ;
#20532=ADVANCED_FACE ( 'NONE', ( #14105 ), #22279, .F. ) ;
#20557=CARTESIAN_POINT ( 'NONE',  ( -6.663373516737825852, 36.04829920608432303, -148.7421194615091906 ) ) ;
#20558=CARTESIAN_POINT ( 'NONE',  ( -8.098664391214354552, 41.05008105453497080, -141.7339891042810223 ) ) ;
#20567=CARTESIAN_POINT ( 'NONE',  ( -12.18519546026979050, 41.69055574765604177, -144.6655014886106017 ) ) ;
#20570=CARTESIAN_POINT ( 'NONE',  ( -23.22224815339999893, 34.57381638260000045, -140.7548632179999970 ) ) ;
#20572=CARTESIAN_POINT ( 'NONE',  ( -7.529689113779999943, 37.05876528330000497, -139.9906690790000141 ) ) ;
#20579=CARTESIAN_POINT ( 'NONE',  ( -19.49482955066354606, 37.94579615576876108, -139.9758014792360541 ) ) ;
#20599=CARTESIAN_POINT ( 'NONE',  ( -23.11170852288484667, 36.28661503646119257, -140.7058601757693737 ) ) ;
#20603=ORIENTED_EDGE ( 'NONE', *, *, #13727, .T. ) ;
#20613=CARTESIAN_POINT ( 'NONE',  ( -23.72311861867038729, 41.82577330078812849, -143.6112047735845181 ) ) ;
#20614=CARTESIAN_POINT ( 'NONE',  ( -15.15646599586469634, 34.44462052388409745, -147.2304959536884894 ) ) ;
#20616=CARTESIAN_POINT ( 'NONE',  ( -17.49915212496940953, 35.33646836210735387, -140.3085081534657093 ) ) ;
#20618=CARTESIAN_POINT ( 'NONE',  ( -19.14968637899999848, 34.49201595030000078, -147.7870032629999741 ) ) ;
#20627=CARTESIAN_POINT ( 'NONE',  ( -22.11386115772126004, 33.57646858666087297, -144.3495254905444085 ) ) ;
#20630=CARTESIAN_POINT ( 'NONE',  ( -12.91608596194663861, 33.62894392469238625, -142.1625766469311429 ) ) ;
#20636=CARTESIAN_POINT ( 'NONE',  ( -7.695630400395947923, 37.03895750127035313, -140.6427397355593030 ) ) ;
#20643=CARTESIAN_POINT ( 'NONE',  ( -14.70358821728447474, 36.91864139954388691, -140.0875527723345897 ) ) ;
#20653=CARTESIAN_POINT ( 'NONE',  ( -23.48449349015688270, 36.94479390616783832, -140.4349842069358090 ) ) ;
#20654=CARTESIAN_POINT ( 'NONE',  ( -25.46021907539999773, 33.59345108530000346, -146.1038275270000213 ) ) ;
#20669=CARTESIAN_POINT ( 'NONE',  ( -27.68847005644245129, 39.80069049611315535, -147.7731842270326581 ) ) ;
#20681=CARTESIAN_POINT ( 'NONE',  ( -18.31895680040000229, 41.06933176500000116, -146.2870363079999834 ) ) ;
#20691=CARTESIAN_POINT ( 'NONE',  ( -21.53332179724142748, 37.97490292932302935, -148.7165867017075982 ) ) ;
#20695=CARTESIAN_POINT ( 'NONE',  ( -28.62185635698285324, 35.60280024164048029, -140.7936020328396296 ) ) ;
#20701=CARTESIAN_POINT ( 'NONE',  ( -11.29029698189999920, 36.23043332049999776, -140.4049246349999862 ) ) ;
#20713=EDGE_LOOP ( 'NONE', ( #2187, #19692, #17184, #12425 ) ) ;
#20719=CARTESIAN_POINT ( 'NONE',  ( -24.02064066296885514, 38.85110534163130325, -148.3889946021463970 ) ) ;
#20728=CARTESIAN_POINT ( 'NONE',  ( -10.07619956199374123, 36.21908991350156271, -147.8536995445676041 ) ) ;
#20740=CARTESIAN_POINT ( 'NONE',  ( -22.62924774403715844, 37.91877106620272286, -140.0196664478621926 ) ) ;
#20749=CARTESIAN_POINT ( 'NONE',  ( -8.031950161270000166, 40.75709267670000457, -141.9144354160000034 ) ) ;
#20752=( BOUNDED_SURFACE ( )  B_SPLINE_SURFACE ( 5, 5, ( 
 ( #6507, #6264, #8272, #11844, #10300, #22810 ),
 ( #18877, #21150, #13514, #2590, #20788, #21031 ),
 ( #13771, #4720, #11963, #19228, #10175, #4478 ),
 ( #22937, #2712, #9816, #17576, #1290, #15782 ),
 ( #17094, #17209, #812, #11721, #8151, #13992 ),
 ( #16142, #18159, #5184, #19595, #9094, #5431 ),
 ( #10760, #1520, #19708, #23515, #18043, #1394 ),
 ( #7212, #3530, #23283, #3288, #23396, #4961 ),
 ( #19944, #10412, #1871, #21265, #21389, #8620 ),
 ( #10643, #23045, #17926, #8863, #6973, #5075 ),
 ( #14121, #12434, #21743, #7092, #14351, #14474 ),
 ( #21623, #1754, #19832, #12676, #5305, #10879 ) ),
 .UNSPECIFIED., .F., .F., .F. ) 
 B_SPLINE_SURFACE_WITH_KNOTS ( ( 6, 3, 3, 6 ),
 ( 6, 6 ),
 ( 0.000000000000000000, 4.398006073320000375, 8.633600727160001043, 12.71824907600000110 ),
 ( 0.000000000000000000, 1.570796326852889946 ),
 .UNSPECIFIED. ) 
 GEOMETRIC_REPRESENTATION_ITEM ( )  RATIONAL_B_SPLINE_SURFACE ( (
 ( 1.000000000000000000, 0.5999999999852579924, 0.3999999999852579813, 0.2999999999889434998, 0.2499999999926290073, 0.2500000000000000000),
 ( 1.000000000000000000, 0.5999999999852579924, 0.3999999999852579813, 0.2999999999889434998, 0.2499999999926290073, 0.2500000000000000000),
 ( 1.000000000000000000, 0.5999999999852579924, 0.3999999999852579813, 0.2999999999889434998, 0.2499999999926290073, 0.2500000000000000000),
 ( 1.000000000000000000, 0.5999999999852579924, 0.3999999999852579813, 0.2999999999889434998, 0.2499999999926290073, 0.2500000000000000000),
 ( 1.000000000000000000, 0.5999999999852579924, 0.3999999999852579813, 0.2999999999889434998, 0.2499999999926290073, 0.2500000000000000000),
 ( 1.000000000000000000, 0.5999999999852579924, 0.3999999999852579813, 0.2999999999889434998, 0.2499999999926290073, 0.2500000000000000000),
 ( 1.000000000000000000, 0.5999999999852579924, 0.3999999999852579813, 0.2999999999889434998, 0.2499999999926290073, 0.2500000000000000000),
 ( 1.000000000000000000, 0.5999999999852579924, 0.3999999999852579813, 0.2999999999889434998, 0.2499999999926290073, 0.2500000000000000000),
 ( 1.000000000000000000, 0.5999999999852579924, 0.3999999999852579813, 0.2999999999889434998, 0.2499999999926290073, 0.2500000000000000000),
 ( 1.000000000000000000, 0.5999999999852579924, 0.3999999999852579813, 0.2999999999889434998, 0.2499999999926290073, 0.2500000000000000000),
 ( 1.000000000000000000, 0.5999999999852579924, 0.3999999999852579813, 0.2999999999889434998, 0.2499999999926290073, 0.2500000000000000000),
 ( 1.000000000000000000, 0.5999999999852579924, 0.3999999999852579813, 0.2999999999889434998, 0.2499999999926290073, 0.2500000000000000000) ) ) 
 REPRESENTATION_ITEM ( '' )  SURFACE ( )  );
#20753=CARTESIAN_POINT ( 'NONE',  ( -28.28302905045270421, 36.20688177001763819, -148.1802150528449999 ) ) ;
#20765=CARTESIAN_POINT ( 'NONE',  ( -21.90852802850000103, 37.90475843469999973, -148.1502781210000137 ) ) ;
#20766=CARTESIAN_POINT ( 'NONE',  ( -18.94796313193197079, 38.67526590167940981, -147.5829755502408318 ) ) ;
#20770=CARTESIAN_POINT ( 'NONE',  ( -25.47266295436726580, 33.45219305391066200, -144.4863246959951084 ) ) ;
#20788=CARTESIAN_POINT ( 'NONE',  ( -11.21635108262976388, 37.71473148017482657, -140.6865916277538133 ) ) ;
#20790=CARTESIAN_POINT ( 'NONE',  ( -6.565507373411109349, 37.00519331013509827, -148.7410818962521830 ) ) ;
#20791=CARTESIAN_POINT ( 'NONE',  ( -9.460728761480464044, 37.99149710710148042, -148.7262519339525966 ) ) ;
#20806=EDGE_LOOP ( 'NONE', ( #18601, #4858, #12717, #14368 ) ) ;
#20810=CARTESIAN_POINT ( 'NONE',  ( -14.78687493254208363, 41.11828399665055400, -141.6185954194986039 ) ) ;
#20811=CARTESIAN_POINT ( 'NONE',  ( -25.33725402850548036, 34.39035690846336024, -140.4300890444341974 ) ) ;
#20834=CARTESIAN_POINT ( 'NONE',  ( -7.828824709450000086, 39.51093879980000168, -140.6700787229999889 ) ) ;
#20841=CARTESIAN_POINT ( 'NONE',  ( -16.36060017231690011, 36.32623467514464721, -140.3335547247180841 ) ) ;
#20842=CARTESIAN_POINT ( 'NONE',  ( -16.15870017774198431, 34.84090251771772273, -146.9067376896876453 ) ) ;
#20843=CARTESIAN_POINT ( 'NONE',  ( -5.558768696239984486, 37.82651365785675779, -139.8085169320104058 ) ) ;
#20848=( BOUNDED_CURVE ( )  B_SPLINE_CURVE ( 5, ( #16993, #2606, #4276, #6396, #13657, #16881 ),
 .UNSPECIFIED., .F., .F. ) 
 B_SPLINE_CURVE_WITH_KNOTS ( ( 6, 6 ),
 ( 1.570796326702242673, 3.141592653590000062 ),
 .UNSPECIFIED. ) 
 CURVE ( )  GEOMETRIC_REPRESENTATION_ITEM ( )  RATIONAL_B_SPLINE_CURVE ( ( 0.2500000000000000000, 0.2499999999881897805, 0.2999999999822846597, 0.3999999999763795278, 0.5999999999763795389, 1.000000000000000000 ) ) 
 REPRESENTATION_ITEM ( '' )  );
#20849=CARTESIAN_POINT ( 'NONE',  ( -9.072898850179999641, 36.94639249900000522, -148.2684494029999769 ) ) ;
#20856=CARTESIAN_POINT ( 'NONE',  ( -28.37825339583908146, 32.94869610820727246, -141.6352474658712026 ) ) ;
#20859=EDGE_LOOP ( 'NONE', ( #3701, #12611, #10430, #14966 ) ) ;
#20861=CARTESIAN_POINT ( 'NONE',  ( -23.24386692375823316, 40.83902259678306024, -144.5872313496660695 ) ) ;
#20864=CARTESIAN_POINT ( 'NONE',  ( -15.57786843150000067, 37.00666880280000726, -148.5521201120000114 ) ) ;
#20868=CARTESIAN_POINT ( 'NONE',  ( -8.561883997267385027, 37.68227764167581029, -140.5058735119322648 ) ) ;
#20875=CARTESIAN_POINT ( 'NONE',  ( -14.60018857135958292, 36.05920633199687586, -140.1047136458358864 ) ) ;
#20889=CARTESIAN_POINT ( 'NONE',  ( -17.72712734282866265, 38.71922357431461847, -139.9447469178576000 ) ) ;
#20895=CARTESIAN_POINT ( 'NONE',  ( -25.08423778095658463, 34.60282621925794189, -140.6697649010042426 ) ) ;
#20898=( BOUNDED_CURVE ( )  B_SPLINE_CURVE ( 5, ( #22039, #5498, #16330, #7504, #18456, #3712, #5838, #14655, #10827, #2060, #13094, #16668 ),
 .UNSPECIFIED., .F., .F. ) 
 B_SPLINE_CURVE_WITH_KNOTS ( ( 6, 3, 3, 6 ),
 ( 0.000000000000000000, 4.463483057499999518, 8.880954762089999122, 13.25426345570000031 ),
 .UNSPECIFIED. ) 
 CURVE ( )  GEOMETRIC_REPRESENTATION_ITEM ( )  RATIONAL_B_SPLINE_CURVE ( ( 0.2500000000000000000, 0.2500000000000000000, 0.2500000000000000000, 0.2500000000000000000, 0.2500000000000000000, 0.2500000000000000000, 0.2500000000000000000, 0.2500000000000000000, 0.2500000000000000000, 0.2500000000000000000, 0.2500000000000000000, 0.2500000000000000000 ) ) 
 REPRESENTATION_ITEM ( '' )  );
#20912=CARTESIAN_POINT ( 'NONE',  ( -9.971101149720000834, 37.05360750090000721, -147.8421425029999909 ) ) ;
#20918=CARTESIAN_POINT ( 'NONE',  ( -7.712174556309761009, 32.67941313690337068, -141.7048212837721621 ) ) ;
#20921=VERTEX_POINT ( 'NONE', #16536 ) ;
#20936=CARTESIAN_POINT ( 'NONE',  ( -14.45293675682532886, 38.87179601339980906, -139.7374547563314593 ) ) ;
#20937=CARTESIAN_POINT ( 'NONE',  ( -26.10314130450000292, 34.70878586860000325, -141.0128996759999893 ) ) ;
#20973=CARTESIAN_POINT ( 'NONE',  ( -4.527137292580695416, 37.91261575257937722, -140.0120598367263085 ) ) ;
#20978=CARTESIAN_POINT ( 'NONE',  ( -9.238580206868249434, 35.38369298950671293, -147.3609278768369677 ) ) ;
#20985=VERTEX_POINT ( 'NONE', #5706 ) ;
#20987=CARTESIAN_POINT ( 'NONE',  ( -22.79386933270184556, 37.02723109250518263, -140.7029355817512339 ) ) ;
#20991=CARTESIAN_POINT ( 'NONE',  ( -10.38572958583939254, 32.19234684762017196, -144.3174661366601299 ) ) ;
#20996=CARTESIAN_POINT ( 'NONE',  ( -7.081915218507915277, 37.06683495603981271, -147.7519347215450409 ) ) ;
#20997=CARTESIAN_POINT ( 'NONE',  ( -26.39256767719999885, 41.50003988699999979, -143.5805134120000162 ) ) ;
#21005=CARTESIAN_POINT ( 'NONE',  ( -21.31094475132173471, 38.36490538190786737, -147.1930922076768411 ) ) ;
#21007=CARTESIAN_POINT ( 'NONE',  ( -17.01025018536428135, 38.48180121065468029, -140.7067500820375869 ) ) ;
#21011=CARTESIAN_POINT ( 'NONE',  ( -24.69700618074178777, 35.61223127418029577, -147.2014722472205506 ) ) ;
#21013=CARTESIAN_POINT ( 'NONE',  ( -12.35737375542222161, 41.41429090104503530, -143.6540282846627576 ) ) ;
#21017=EDGE_LOOP ( 'NONE', ( #6631, #16250, #19178, #17083 ) ) ;
#21030=CARTESIAN_POINT ( 'NONE',  ( -19.33778615812330415, 35.56580707893081694, -147.6585156976900919 ) ) ;
#21031=CARTESIAN_POINT ( 'NONE',  ( -11.48759298139373897, 37.74537190003064069, -140.3874188149447946 ) ) ;
#21033=CARTESIAN_POINT ( 'NONE',  ( -7.254103886545301805, 34.31303075260233726, -140.3989650697497495 ) ) ;
#21038=( BOUNDED_SURFACE ( )  B_SPLINE_SURFACE ( 5, 5, ( 
 ( #4160, #5820, #18900, #2610, #22017, #9841 ),
 ( #11510, #360, #16885, #20238, #20579, #9721 ),
 ( #17120, #7484, #13077, #14748, #11167, #16646 ),
 ( #13424, #16997, #7718, #18439, #4386, #7946 ),
 ( #482, #14984, #5707, #12961, #594, #3931 ),
 ( #4043, #2154, #9373, #15228, #7601, #20463 ),
 ( #22480, #18789, #14875, #22133, #6173, #2500 ),
 ( #11277, #7829, #20349, #18550, #2270, #9495 ),
 ( #16767, #22244, #5937, #13190, #18678, #11397 ),
 ( #2390, #9611, #15100, #22360, #6059, #13311 ),
 ( #4280, #711, #20691, #19558, #13957, #2903 ),
 ( #22897, #10017, #14084, #12047, #17410, #6582 ) ),
 .UNSPECIFIED., .F., .F., .F. ) 
 B_SPLINE_SURFACE_WITH_KNOTS ( ( 6, 3, 3, 6 ),
 ( 6, 6 ),
 ( 0.000000000000000000, 4.390059406679999832, 8.746277600790000051, 13.07048654049999925 ),
 ( 0.000000000000000000, 1.570796326702240009 ),
 .UNSPECIFIED. ) 
 GEOMETRIC_REPRESENTATION_ITEM ( )  RATIONAL_B_SPLINE_SURFACE ( (
 ( 1.000000000000000000, 0.6000000000236209718, 0.4000000000236205167, 0.3000000000177154846, 0.2500000000118104970, 0.2500000000000000000),
 ( 1.000000000000000000, 0.6000000000236209718, 0.4000000000236205167, 0.3000000000177154846, 0.2500000000118104970, 0.2500000000000000000),
 ( 1.000000000000000000, 0.6000000000236209718, 0.4000000000236205167, 0.3000000000177154846, 0.2500000000118104970, 0.2500000000000000000),
 ( 1.000000000000000000, 0.6000000000236209718, 0.4000000000236205167, 0.3000000000177154846, 0.2500000000118104970, 0.2500000000000000000),
 ( 1.000000000000000000, 0.6000000000236209718, 0.4000000000236205167, 0.3000000000177154846, 0.2500000000118104970, 0.2500000000000000000),
 ( 1.000000000000000000, 0.6000000000236209718, 0.4000000000236205167, 0.3000000000177154846, 0.2500000000118104970, 0.2500000000000000000),
 ( 1.000000000000000000, 0.6000000000236209718, 0.4000000000236205167, 0.3000000000177154846, 0.2500000000118104970, 0.2500000000000000000),
 ( 1.000000000000000000, 0.6000000000236209718, 0.4000000000236205167, 0.3000000000177154846, 0.2500000000118104970, 0.2500000000000000000),
 ( 1.000000000000000000, 0.6000000000236209718, 0.4000000000236205167, 0.3000000000177154846, 0.2500000000118104970, 0.2500000000000000000),
 ( 1.000000000000000000, 0.6000000000236209718, 0.4000000000236205167, 0.3000000000177154846, 0.2500000000118104970, 0.2500000000000000000),
 ( 1.000000000000000000, 0.6000000000236209718, 0.4000000000236205167, 0.3000000000177154846, 0.2500000000118104970, 0.2500000000000000000),
 ( 1.000000000000000000, 0.6000000000236209718, 0.4000000000236205167, 0.3000000000177154846, 0.2500000000118104970, 0.2500000000000000000) ) ) 
 REPRESENTATION_ITEM ( '' )  SURFACE ( )  );
#21039=CARTESIAN_POINT ( 'NONE',  ( -14.58163105939557624, 36.93319896293952098, -139.6872257168654414 ) ) ;
#21052=CARTESIAN_POINT ( 'NONE',  ( -18.75277607359999976, 37.97046254950000588, -148.4181951110000171 ) ) ;
#21054=CARTESIAN_POINT ( 'NONE',  ( -14.23530246729999860, 39.72954597060000026, -140.2988105550000171 ) ) ;
#21055=CARTESIAN_POINT ( 'NONE',  ( -25.17490547269999723, 35.46855981759999565, -147.6699473629999773 ) ) ;
#21072=ADVANCED_FACE ( 'NONE', ( #15568 ), #1174, .F. ) ;
#21075=CARTESIAN_POINT ( 'NONE',  ( -14.12781175210000129, 38.88127384660000274, -139.8125553750000165 ) ) ;
#21088=CARTESIAN_POINT ( 'NONE',  ( -4.428060343052311332, 37.07089632425688563, -139.9976721173915735 ) ) ;
#21091=CARTESIAN_POINT ( 'NONE',  ( -9.389499115867565138, 36.98418387198957902, -147.3811924090515788 ) ) ;
#21096=CARTESIAN_POINT ( 'NONE',  ( -28.52054873391283962, 32.26575815815821358, -143.5049952843087908 ) ) ;
#21100=CARTESIAN_POINT ( 'NONE',  ( -23.61758233950000019, 37.78045452579999619, -140.0909254550000185 ) ) ;
#21101=ADVANCED_FACE ( 'NONE', ( #14607 ), #2967, .F. ) ;
#21114=CARTESIAN_POINT ( 'NONE',  ( -8.309953467263280658, 35.25464643872108184, -140.3668538350108008 ) ) ;
#21125=CARTESIAN_POINT ( 'NONE',  ( -17.75130813170000366, 41.00325609940000504, -141.6328284839999867 ) ) ;
#21129=CARTESIAN_POINT ( 'NONE',  ( -25.54709891127356158, 36.13246793439832061, -139.7173810941668251 ) ) ;
#21135=CARTESIAN_POINT ( 'NONE',  ( -23.13005137196992678, 38.99857027944433696, -139.6437547635814553 ) ) ;
#21150=CARTESIAN_POINT ( 'NONE',  ( -10.53621254372777472, 37.95353954631509907, -139.9724837675152571 ) ) ;
#21152=CARTESIAN_POINT ( 'NONE',  ( -8.271665395881317551, 36.97019838859678487, -139.4157638768425613 ) ) ;
#21171=CARTESIAN_POINT ( 'NONE',  ( -14.88943025167819201, 39.58359338906777936, -140.3712910920068566 ) ) ;
#21174=CARTESIAN_POINT ( 'NONE',  ( -25.80805072497740227, 36.03780844042944409, -139.4223974946287967 ) ) ;
#21178=CARTESIAN_POINT ( 'NONE',  ( -11.38486064709999823, 36.95668670079999885, -140.3965526140000009 ) ) ;
#21193=CARTESIAN_POINT ( 'NONE',  ( -13.56475956976288444, 38.79166783126999007, -140.1832272770149643 ) ) ;
#21214=CARTESIAN_POINT ( 'NONE',  ( -28.67645553090000021, 33.79622934780000065, -142.1760638819999940 ) ) ;
#21217=CARTESIAN_POINT ( 'NONE',  ( -23.42774316933405387, 40.39856899166812099, -146.1482362793011021 ) ) ;
#21223=CARTESIAN_POINT ( 'NONE',  ( -10.51637644729841092, 32.80416691061421375, -146.2924636027869383 ) ) ;
#21225=CARTESIAN_POINT ( 'NONE',  ( -8.436279545364561372, 40.51610847932013826, -146.1280570644845511 ) ) ;
#21230=CARTESIAN_POINT ( 'NONE',  ( -7.231565869921675827, 33.87808888013704944, -142.3031534620325260 ) ) ;
#21231=CARTESIAN_POINT ( 'NONE',  ( -29.78377644599999741, 41.56884167520000517, -144.3599435680000056 ) ) ;
#21232=CARTESIAN_POINT ( 'NONE',  ( -21.80913741070000000, 38.74859698539999897, -147.9243209519999880 ) ) ;
#21247=CARTESIAN_POINT ( 'NONE',  ( -15.57786843150000067, 37.00666880280000726, -148.5521201120000114 ) ) ;
#21259=CARTESIAN_POINT ( 'NONE',  ( -28.36041799518341833, 33.90485755864479955, -142.1995097533358319 ) ) ;
#21264=CARTESIAN_POINT ( 'NONE',  ( -19.10036854000342998, 37.06903765909164861, -148.2030617969362538 ) ) ;
#21265=CARTESIAN_POINT ( 'NONE',  ( -11.74549879742581204, 39.03442698418600543, -147.0603333942009101 ) ) ;
#21268=CARTESIAN_POINT ( 'NONE',  ( -7.530507654992796951, 34.12260748990723869, -140.1991143277646188 ) ) ;
#21277=ORIENTED_EDGE ( 'NONE', *, *, #4435, .F. ) ;
#21284=CARTESIAN_POINT ( 'NONE',  ( -19.39325354309108818, 37.07505107991995175, -139.9601895475230151 ) ) ;
#21288=CARTESIAN_POINT ( 'NONE',  ( -24.36912841275935904, 34.40976477778183806, -147.5507798122575878 ) ) ;
#21294=CARTESIAN_POINT ( 'NONE',  ( -12.57385931489999997, 38.47543513199999410, -147.4253642439999794 ) ) ;
#21308=CARTESIAN_POINT ( 'NONE',  ( -14.18713694461474439, 40.16576858557153429, -142.2514428343604038 ) ) ;
#21309=CARTESIAN_POINT ( 'NONE',  ( -28.90798551748587641, 37.01360947634927356, -139.5686590453487952 ) ) ;
#21316=CARTESIAN_POINT ( 'NONE',  ( -23.90890255121786367, 36.92681688281093955, -147.8857207493851433 ) ) ;
#21318=ADVANCED_FACE ( 'NONE', ( #2320 ), #1312, .F. ) ;
#21320=CARTESIAN_POINT ( 'NONE',  ( -16.92431971699136994, 37.01165972488241351, -139.4624774945036449 ) ) ;
#21323=ADVANCED_FACE ( 'NONE', ( #2780 ), #7808, .F. ) ;
#21324=CARTESIAN_POINT ( 'NONE',  ( -5.459597139497688545, 36.94776568913771797, -139.8191173758904142 ) ) ;
#21325=CARTESIAN_POINT ( 'NONE',  ( -7.107905118369999720, 36.22301459080000541, -148.1570340890000068 ) ) ;
#21330=CARTESIAN_POINT ( 'NONE',  ( -25.27079369000000142, 34.74837955689999802, -147.2605407199999945 ) ) ;
#21331=ORIENTED_EDGE ( 'NONE', *, *, #15036, .F. ) ;
#21332=B_SPLINE_CURVE_WITH_KNOTS ( 'NONE', 5,
 ( #3245, #6809, #1249, #3023, #13840, #1354, #4915, #19077, #22645, #8579, #23001, #12040 ),
 .UNSPECIFIED., .F., .F.,
 ( 6, 3, 3, 6 ),
 ( 0.000000000000000000, 4.445608688430000122, 8.917804078430000558, 13.41780914199999941 ),
 .UNSPECIFIED. ) ;
#21334=CARTESIAN_POINT ( 'NONE',  ( -29.32420091883213331, 34.33926911055133502, -140.4578922366215465 ) ) ;
#21338=CARTESIAN_POINT ( 'NONE',  ( -23.71327735677587611, 38.51283207398868313, -147.7059059786899979 ) ) ;
#21343=CARTESIAN_POINT ( 'NONE',  ( -10.35239533838411852, 35.24123622976342318, -147.9781929050253382 ) ) ;
#21355=CARTESIAN_POINT ( 'NONE',  ( -7.549714246211497226, 33.73496036356508654, -146.1021208403070091 ) ) ;
#21356=CARTESIAN_POINT ( 'NONE',  ( -6.183234097709999766, 41.28010592229999531, -143.5033826240000110 ) ) ;
#21365=CARTESIAN_POINT ( 'NONE',  ( -16.81794493339999619, 37.02435727940000731, -140.5111119820000170 ) ) ;
#21388=CARTESIAN_POINT ( 'NONE',  ( -19.38605492679999998, 35.40602226210000225, -140.5130341980000139 ) ) ;
#21389=CARTESIAN_POINT ( 'NONE',  ( -12.14203431770015484, 38.98285737023589093, -146.9062848651227853 ) ) ;
#21391=CARTESIAN_POINT ( 'NONE',  ( -8.168738184452987383, 35.97421812808207164, -139.4219941368502305 ) ) ;
#21408=CARTESIAN_POINT ( 'NONE',  ( -15.86641283045871020, 39.36988465981706753, -147.1618092805611013 ) ) ;
#21425=CARTESIAN_POINT ( 'NONE',  ( -14.72926790370904904, 38.75043575020603726, -148.1588405132401647 ) ) ;
#21426=CARTESIAN_POINT ( 'NONE',  ( -28.93621398888856433, 40.40455385674768252, -140.8397343873709531 ) ) ;
#21440=CARTESIAN_POINT ( 'NONE',  ( -4.726668495498447697, 39.51488736142145797, -140.6795032275781807 ) ) ;
#21451=CARTESIAN_POINT ( 'NONE',  ( -24.00988078544188653, 37.66389269266682049, -147.5188782761057382 ) ) ;
#21459=CARTESIAN_POINT ( 'NONE',  ( -9.289091550977641276, 37.68670816229094811, -147.3844454406949467 ) ) ;
#21466=CARTESIAN_POINT ( 'NONE',  ( -7.506111428101620575, 33.37436714625175682, -146.3147224704404152 ) ) ;
#21501=CARTESIAN_POINT ( 'NONE',  ( -20.34672008420000111, 36.01786665889999739, -139.8153362750000213 ) ) ;
#21519=CARTESIAN_POINT ( 'NONE',  ( -10.97748938910000049, 39.75689975739999937, -140.4868351200000234 ) ) ;
#21521=CARTESIAN_POINT ( 'NONE',  ( -21.21916986615164902, 36.96385231546391736, -148.6710958206639646 ) ) ;
#21524=( BOUNDED_CURVE ( )  B_SPLINE_CURVE ( 5, ( #10307, #22944, #8519, #23290, #3296, #5081 ),
 .UNSPECIFIED., .F., .F. ) 
 B_SPLINE_CURVE_WITH_KNOTS ( ( 6, 6 ),
 ( 0.000000000000000000, 1.570796326891506167 ),
 .UNSPECIFIED. ) 
 CURVE ( )  GEOMETRIC_REPRESENTATION_ITEM ( )  RATIONAL_B_SPLINE_CURVE ( ( 1.000000000000000000, 0.5999999999754248581, 0.3999999999754249025, 0.2999999999815686769, 0.2499999999877124679, 0.2500000000000000000 ) ) 
 REPRESENTATION_ITEM ( '' )  );
#21526=CARTESIAN_POINT ( 'NONE',  ( -27.13569889285190229, 40.84437936193481988, -141.7271500514046920 ) ) ;
#21542=CARTESIAN_POINT ( 'NONE',  ( -14.54684675599480137, 39.31632282492414276, -147.3469236774771502 ) ) ;
#21557=CARTESIAN_POINT ( 'NONE',  ( -6.837524392801337392, 37.99761324335693757, -148.5285986741252771 ) ) ;
#21558=CARTESIAN_POINT ( 'NONE',  ( -24.01715389780000010, 40.57582142210000598, -141.9832779239999923 ) ) ;
#21568=PRODUCT ( 'Latch Return Spring', 'Latch Return Spring', '', ( #14957 ) ) ;
#21571=CARTESIAN_POINT ( 'NONE',  ( -24.38851193153152508, 40.21356925245557790, -145.9141185447818998 ) ) ;
#21572=CARTESIAN_POINT ( 'NONE',  ( -29.89717128122237000, 39.22683608722478965, -140.1129597738056418 ) ) ;
#21576=CARTESIAN_POINT ( 'NONE',  ( -10.69040905424370003, 35.19607541363222225, -139.6909101219067963 ) ) ;
#21579=CARTESIAN_POINT ( 'NONE',  ( -8.631906738831403914, 39.33441879577958389, -147.3392595813083119 ) ) ;
#21586=CARTESIAN_POINT ( 'NONE',  ( -8.514310886093261033, 36.94123471669811209, -140.1199228270031938 ) ) ;
#21593=EDGE_LOOP ( 'NONE', ( #1299, #3559, #14567, #3055 ) ) ;
#21623=CARTESIAN_POINT ( 'NONE',  ( -12.28014746100000032, 36.97113097969999984, -148.4919582129999753 ) ) ;
#21650=CARTESIAN_POINT ( 'NONE',  ( -10.41700570847820195, 37.07221587398770879, -140.3414633426674243 ) ) ;
#21666=CARTESIAN_POINT ( 'NONE',  ( -28.33971964075230332, 37.08144121879533373, -140.0461821376590308 ) ) ;
#21671=( BOUNDED_CURVE ( )  B_SPLINE_CURVE ( 5, ( #16761, #11735, #476, #7712, #14978, #22701 ),
 .UNSPECIFIED., .F., .F. ) 
 B_SPLINE_CURVE_WITH_KNOTS ( ( 6, 6 ),
 ( 0.000000000000000000, 1.570796326823717504 ),
 .UNSPECIFIED. ) 
 CURVE ( )  GEOMETRIC_REPRESENTATION_ITEM ( )  RATIONAL_B_SPLINE_CURVE ( ( 1.000000000000000000, 0.5999999999926871608, 0.3999999999926872052, 0.2999999999945154316, 0.2499999999963436192, 0.2500000000000000000 ) ) 
 REPRESENTATION_ITEM ( '' )  );
#21684=CARTESIAN_POINT ( 'NONE',  ( -5.064279449469999861, 40.47653686799999662, -142.0698957560000224 ) ) ;
#21695=CARTESIAN_POINT ( 'NONE',  ( -29.80856694857513034, 37.96151168870303394, -140.1460686462327203 ) ) ;
#21699=CARTESIAN_POINT ( 'NONE',  ( -10.65913935279999869, 37.04331329920000115, -139.7140392919999954 ) ) ;
#21700=CARTESIAN_POINT ( 'NONE',  ( -18.37691940378883970, 35.51168060186468267, -147.4900940510613907 ) ) ;
#21702=CARTESIAN_POINT ( 'NONE',  ( -9.072898850179999641, 36.94639249900000522, -148.2684494029999769 ) ) ;
#21711=CARTESIAN_POINT ( 'NONE',  ( -23.34997301940000014, 41.23575095009999814, -144.6233831890000090 ) ) ;
#21717=CARTESIAN_POINT ( 'NONE',  ( -17.10091063390000343, 39.14571640540000175, -141.0837638240000160 ) ) ;
#21735=CARTESIAN_POINT ( 'NONE',  ( -13.04270098951570134, 34.92521805816488012, -147.0831430690302000 ) ) ;
#21743=CARTESIAN_POINT ( 'NONE',  ( -11.76216916721041805, 37.71582637476514321, -147.9848159988354723 ) ) ;
#21764=CARTESIAN_POINT ( 'NONE',  ( -15.67604317050167140, 40.52459757754237302, -145.9876088847360052 ) ) ;
#21769=CARTESIAN_POINT ( 'NONE',  ( -26.53689163751006674, 38.88307050151443889, -139.6803910534961517 ) ) ;
#21787=CARTESIAN_POINT ( 'NONE',  ( -17.10091063381063847, 39.14571640549888087, -141.0837638240818137 ) ) ;
#21788=CARTESIAN_POINT ( 'NONE',  ( -22.10875017890000294, 36.18377167419999552, -148.1739623899999856 ) ) ;
#21800=CARTESIAN_POINT ( 'NONE',  ( -5.537589236589999686, 40.52957482200000072, -146.1175057039999956 ) ) ;
#21811=( BOUNDED_SURFACE ( )  B_SPLINE_SURFACE ( 5, 5, ( 
 ( #8115, #8475, #20636, #11565, #18840, #17407 ),
 ( #2788, #4683, #8233, #17049, #20868, #2548 ),
 ( #22536, #767, #15388, #8000, #6227, #10014 ),
 ( #15281, #22765, #6463, #11925, #19191, #13476 ),
 ( #20749, #4443, #11679, #891, #18956, #9896 ),
 ( #22647, #10480, #19553, #8936, #23003, #18118 ),
 ( #9045, #16216, #14307, #8822, #10722, #4917 ),
 ( #18003, #21225, #1356, #8581, #3487, #1714 ),
 ( #1476, #21579, #15855, #12511, #5260, #23120 ),
 ( #17885, #10371, #17647, #19907, #3605, #14430 ),
 ( #12636, #19793, #10835, #21459, #23469, #7164 ),
 ( #21702, #16099, #5389, #12165, #3141, #1829 ) ),
 .UNSPECIFIED., .F., .F., .F. ) 
 B_SPLINE_SURFACE_WITH_KNOTS ( ( 6, 3, 3, 6 ),
 ( 6, 6 ),
 ( 0.000000000000000000, 4.371092480729999785, 8.745625541600000830, 13.12578902609999965 ),
 ( 0.000000000000000000, 1.570796326891464867 ),
 .UNSPECIFIED. ) 
 GEOMETRIC_REPRESENTATION_ITEM ( )  RATIONAL_B_SPLINE_SURFACE ( (
 ( 1.000000000000000000, 0.5999999999754349611, 0.3999999999754355051, 0.2999999999815765039, 0.2499999999877174917, 0.2500000000000000000),
 ( 1.000000000000000000, 0.5999999999754349611, 0.3999999999754355051, 0.2999999999815765039, 0.2499999999877174917, 0.2500000000000000000),
 ( 1.000000000000000000, 0.5999999999754349611, 0.3999999999754355051, 0.2999999999815765039, 0.2499999999877174917, 0.2500000000000000000),
 ( 1.000000000000000000, 0.5999999999754349611, 0.3999999999754355051, 0.2999999999815765039, 0.2499999999877174917, 0.2500000000000000000),
 ( 1.000000000000000000, 0.5999999999754349611, 0.3999999999754355051, 0.2999999999815765039, 0.2499999999877174917, 0.2500000000000000000),
 ( 1.000000000000000000, 0.5999999999754349611, 0.3999999999754355051, 0.2999999999815765039, 0.2499999999877174917, 0.2500000000000000000),
 ( 1.000000000000000000, 0.5999999999754349611, 0.3999999999754355051, 0.2999999999815765039, 0.2499999999877174917, 0.2500000000000000000),
 ( 1.000000000000000000, 0.5999999999754349611, 0.3999999999754355051, 0.2999999999815765039, 0.2499999999877174917, 0.2500000000000000000),
 ( 1.000000000000000000, 0.5999999999754349611, 0.3999999999754355051, 0.2999999999815765039, 0.2499999999877174917, 0.2500000000000000000),
 ( 1.000000000000000000, 0.5999999999754349611, 0.3999999999754355051, 0.2999999999815765039, 0.2499999999877174917, 0.2500000000000000000),
 ( 1.000000000000000000, 0.5999999999754349611, 0.3999999999754355051, 0.2999999999815765039, 0.2499999999877174917, 0.2500000000000000000),
 ( 1.000000000000000000, 0.5999999999754349611, 0.3999999999754355051, 0.2999999999815765039, 0.2499999999877174917, 0.2500000000000000000) ) ) 
 REPRESENTATION_ITEM ( '' )  SURFACE ( )  );
#21817=CARTESIAN_POINT ( 'NONE',  ( -11.17931034166987203, 33.41890892721424677, -141.8539557988947877 ) ) ;
#21818=CARTESIAN_POINT ( 'NONE',  ( -19.82031220496693180, 35.98978369854768289, -139.3867682255206262 ) ) ;
#21837=CARTESIAN_POINT ( 'NONE',  ( -24.63187620837634739, 37.01311550627328018, -148.7335123084583302 ) ) ;
#21851=CARTESIAN_POINT ( 'NONE',  ( -16.90886450125455198, 35.01031021513652775, -141.1892970147640085 ) ) ;
#21854=CARTESIAN_POINT ( 'NONE',  ( -18.18930989820000121, 36.96028804430000037, -147.6841622079999752 ) ) ;
#21857=CARTESIAN_POINT ( 'NONE',  ( -19.49544947696901787, 34.86113041125985745, -141.2543152433912041 ) ) ;
#21876=CARTESIAN_POINT ( 'NONE',  ( -22.36496694526604756, 35.22036549038422493, -139.8269661872139409 ) ) ;
#21882=CARTESIAN_POINT ( 'NONE',  ( -26.33255611194164558, 36.96293009473756541, -139.4434112040622153 ) ) ;
#21898=CARTESIAN_POINT ( 'NONE',  ( -23.02519999780000148, 33.35976406540000028, -141.9520978260000277 ) ) ;
#21909=CARTESIAN_POINT ( 'NONE',  ( -27.44856507211657615, 33.04311423941999948, -146.2071622461182017 ) ) ;
#21913=ADVANCED_FACE ( 'NONE', ( #12244 ), #3595, .F. ) ;
#21914=CARTESIAN_POINT ( 'NONE',  ( -5.385270659705732044, 41.64123329751902958, -144.5533759557629310 ) ) ;
#21924=CARTESIAN_POINT ( 'NONE',  ( -22.60318121862521323, 35.64391590581870162, -140.8717365814055995 ) ) ;
#21928=CARTESIAN_POINT ( 'NONE',  ( -11.40196181638443207, 35.19900947717987805, -139.9192633046721994 ) ) ;
#21929=CARTESIAN_POINT ( 'NONE',  ( -18.46643761655235849, 34.84883242740267661, -147.1252693406791821 ) ) ;
#21941=CARTESIAN_POINT ( 'NONE',  ( -5.366752052302948606, 40.61197287204888084, -143.6738006028257928 ) ) ;
#21943=( BOUNDED_SURFACE ( )  B_SPLINE_SURFACE ( 5, 5, ( 
 ( #10614, #17770, #7175, #1487, #17895, #1727 ),
 ( #5272, #8947, #6945, #14208, #10847, #19918 ),
 ( #4076, #2428, #3966, #5972, #20500, #11198 ),
 ( #3730, #9408, #11437, #18471, #2186, #18253 ),
 ( #7865, #5853, #14791, #22281, #16686, #18590 ),
 ( #9645, #21941, #630, #16919, #5741, #15018 ),
 ( #12999, #15136, #13110, #22057, #11311, #22168 ),
 ( #18720, #20272, #403, #20035, #5513, #20382 ),
 ( #12760, #4202, #9184, #7753, #13224, #10968 ),
 ( #7636, #14909, #2314, #1962, #9537, #16461 ),
 ( #166, #7408, #14671, #5625, #12877, #16807 ),
 ( #20159, #3851, #11086, #18366, #519, #2077 ) ),
 .UNSPECIFIED., .F., .F., .F. ) 
 B_SPLINE_SURFACE_WITH_KNOTS ( ( 6, 3, 3, 6 ),
 ( 6, 6 ),
 ( 0.000000000000000000, 4.445608688430000122, 8.917804078430000558, 13.41780914199999941 ),
 ( 0.000000000000000000, 1.570796326505564888 ),
 .UNSPECIFIED. ) 
 GEOMETRIC_REPRESENTATION_ITEM ( )  RATIONAL_B_SPLINE_SURFACE ( (
 ( 1.000000000000000000, 0.6000000000737040207, 0.4000000000737040096, 0.3000000000552779933, 0.2500000000368520214, 0.2500000000000000000),
 ( 1.000000000000000000, 0.6000000000737040207, 0.4000000000737040096, 0.3000000000552779933, 0.2500000000368520214, 0.2500000000000000000),
 ( 1.000000000000000000, 0.6000000000737040207, 0.4000000000737040096, 0.3000000000552779933, 0.2500000000368520214, 0.2500000000000000000),
 ( 1.000000000000000000, 0.6000000000737040207, 0.4000000000737040096, 0.3000000000552779933, 0.2500000000368520214, 0.2500000000000000000),
 ( 1.000000000000000000, 0.6000000000737040207, 0.4000000000737040096, 0.3000000000552779933, 0.2500000000368520214, 0.2500000000000000000),
 ( 1.000000000000000000, 0.6000000000737040207, 0.4000000000737040096, 0.3000000000552779933, 0.2500000000368520214, 0.2500000000000000000),
 ( 1.000000000000000000, 0.6000000000737040207, 0.4000000000737040096, 0.3000000000552779933, 0.2500000000368520214, 0.2500000000000000000),
 ( 1.000000000000000000, 0.6000000000737040207, 0.4000000000737040096, 0.3000000000552779933, 0.2500000000368520214, 0.2500000000000000000),
 ( 1.000000000000000000, 0.6000000000737040207, 0.4000000000737040096, 0.3000000000552779933, 0.2500000000368520214, 0.2500000000000000000),
 ( 1.000000000000000000, 0.6000000000737040207, 0.4000000000737040096, 0.3000000000552779933, 0.2500000000368520214, 0.2500000000000000000),
 ( 1.000000000000000000, 0.6000000000737040207, 0.4000000000737040096, 0.3000000000552779933, 0.2500000000368520214, 0.2500000000000000000),
 ( 1.000000000000000000, 0.6000000000737040207, 0.4000000000737040096, 0.3000000000552779933, 0.2500000000368520214, 0.2500000000000000000) ) ) 
 REPRESENTATION_ITEM ( '' )  SURFACE ( )  );
#21965=CARTESIAN_POINT ( 'NONE',  ( -20.40880337526489186, 35.19740419381395213, -140.3550962540792000 ) ) ;
#21970=CARTESIAN_POINT ( 'NONE',  ( -18.18930989820000121, 36.96028804430000037, -147.6841622079999752 ) ) ;
#21979=CARTESIAN_POINT ( 'NONE',  ( -25.38678224704220199, 37.07582353397776131, -140.0279244688226754 ) ) ;
#21985=EDGE_CURVE ( 'NONE', #11114, #8868, #3610, .T. ) ;
#21988=CARTESIAN_POINT ( 'NONE',  ( -27.38907315503255191, 40.93772549015603346, -144.3834931736647889 ) ) ;
#21995=CARTESIAN_POINT ( 'NONE',  ( -9.085559744729581055, 40.87064354070782457, -141.7118699073245978 ) ) ;
#22006=CARTESIAN_POINT ( 'NONE',  ( -11.80429832671256563, 38.82045246462196531, -139.9120858938445338 ) ) ;
#22014=CARTESIAN_POINT ( 'NONE',  ( -28.25100290369999811, 33.74243115720000219, -145.9160084049999853 ) ) ;
#22017=CARTESIAN_POINT ( 'NONE',  ( -19.39325354300846271, 37.07505107992977855, -139.9601895477372011 ) ) ;
#22024=ORIENTED_EDGE ( 'NONE', *, *, #22815, .T. ) ;
#22027=CARTESIAN_POINT ( 'NONE',  ( -15.90674982584208230, 37.04592612750105474, -148.5146100863323113 ) ) ;
#22035=CARTESIAN_POINT ( 'NONE',  ( -29.13601448249999848, 36.98639052360000079, -140.5419328609999923 ) ) ;
#22039=CARTESIAN_POINT ( 'NONE',  ( -21.03694116389999635, 36.94210036639999828, -147.9486865819999935 ) ) ;
#22048=CARTESIAN_POINT ( 'NONE',  ( -24.81028755636832273, 39.53448486588602151, -147.4801103133366382 ) ) ;
#22049=CARTESIAN_POINT ( 'NONE',  ( -16.37184312240000139, 32.37338091950000063, -144.3414871020000021 ) ) ;
#22057=CARTESIAN_POINT ( 'NONE',  ( -6.183746982877465825, 40.52362886641058282, -144.3549557629433195 ) ) ;
#22063=CARTESIAN_POINT ( 'NONE',  ( -13.71246964740000074, 35.06639867129999999, -139.8243480419999685 ) ) ;
#22074=CARTESIAN_POINT ( 'NONE',  ( -27.60583033829190924, 37.01000650954619431, -148.6900182103307486 ) ) ;
#22077=CARTESIAN_POINT ( 'NONE',  ( -12.28014746100000032, 36.97113097969999984, -148.4919582129999753 ) ) ;
#22086=CARTESIAN_POINT ( 'NONE',  ( -19.79184979336553241, 37.02747215728108188, -140.6521846888477114 ) ) ;
#22099=FACE_OUTER_BOUND ( 'NONE', #3224, .T. ) ;
#22101=CARTESIAN_POINT ( 'NONE',  ( -23.31991597950000283, 35.31558869410000057, -140.3324749399999973 ) ) ;
#22106=CARTESIAN_POINT ( 'NONE',  ( -27.86298653490555566, 38.63966099682678390, -147.5694018320387499 ) ) ;
#22108=CARTESIAN_POINT ( 'NONE',  ( -14.11967125440000004, 36.98834135279999913, -140.5455248810000057 ) ) ;
#22111=CARTESIAN_POINT ( 'NONE',  ( -6.033650297970000409, 36.94170754819999303, -147.9652040070000112 ) ) ;
#22123=CARTESIAN_POINT ( 'NONE',  ( -10.98828237508949002, 38.00460691268780522, -139.4738624127897992 ) ) ;
#22124=CARTESIAN_POINT ( 'NONE',  ( -17.32451618079999633, 37.89224186959999940, -139.5945780149999962 ) ) ;
#22125=CARTESIAN_POINT ( 'NONE',  ( -29.78377644610135988, 41.56884167520560425, -144.3599435678619898 ) ) ;
#22131=CARTESIAN_POINT ( 'NONE',  ( -28.85277900879999891, 34.87340808660000135, -141.1101275619999740 ) ) ;
#22133=CARTESIAN_POINT ( 'NONE',  ( -20.44591902742020295, 41.68207087135139943, -144.6720133961590591 ) ) ;
#22150=CARTESIAN_POINT ( 'NONE',  ( -22.33063748470679855, 35.38828378189443669, -140.2025093957771844 ) ) ;
#22151=CARTESIAN_POINT ( 'NONE',  ( -29.78377644595123996, 41.56884167519815776, -144.3599435678792133 ) ) ;
#22155=CARTESIAN_POINT ( 'NONE',  ( -18.64600821076795967, 33.72696025766887828, -146.0724859999091905 ) ) ;
#22159=CARTESIAN_POINT ( 'NONE',  ( -24.49703822390000241, 40.50511125069999707, -146.0729279460000214 ) ) ;
#22161=CARTESIAN_POINT ( 'NONE',  ( -16.11775386688182010, 33.36946837796644161, -144.2542744048722057 ) ) ;
#22168=CARTESIAN_POINT ( 'NONE',  ( -6.288682382015720052, 41.28368337086639173, -144.4167712528271750 ) ) ;
#22177=CARTESIAN_POINT ( 'NONE',  ( -11.99109128265850543, 36.93662743998236664, -148.3295785879953712 ) ) ;
#22190=CARTESIAN_POINT ( 'NONE',  ( -13.98445131495799387, 32.80079897227977881, -143.8357661806866474 ) ) ;
#22199=CARTESIAN_POINT ( 'NONE',  ( -19.98913152175602903, 38.47389702338594475, -140.8539614082147295 ) ) ;
#22210=ORIENTED_EDGE ( 'NONE', *, *, #19867, .F. ) ;
#22214=CARTESIAN_POINT ( 'NONE',  ( -21.83347610790112014, 32.92361448676648195, -143.4947777357538143 ) ) ;
#22220=CARTESIAN_POINT ( 'NONE',  ( -27.76683509697144459, 39.35409722523485243, -147.1504185288667941 ) ) ;
#22226=CARTESIAN_POINT ( 'NONE',  ( -8.810109936695118549, 39.32487244769719581, -140.7337397747917862 ) ) ;
#22233=CARTESIAN_POINT ( 'NONE',  ( -11.68432188606179700, 41.73979788245389244, -143.7054085318254693 ) ) ;
#22237=CARTESIAN_POINT ( 'NONE',  ( -8.514310886080000529, 36.94123471670000214, -140.1199228270000106 ) ) ;
#22244=CARTESIAN_POINT ( 'NONE',  ( -21.62977836625777073, 39.70709670999821128, -147.7621909749726683 ) ) ;
#22245=ORIENTED_EDGE ( 'NONE', *, *, #21985, .F. ) ;
#22247=CARTESIAN_POINT ( 'NONE',  ( -27.47244207678307859, 35.09215423527204791, -148.2237751110660327 ) ) ;
#22272=FACE_OUTER_BOUND ( 'NONE', #14172, .T. ) ;
#22274=CARTESIAN_POINT ( 'NONE',  ( -17.40421240568337069, 34.61091079777447987, -140.7087267687066401 ) ) ;
#22279=( BOUNDED_SURFACE ( )  B_SPLINE_SURFACE ( 5, 5, ( 
 ( #17672, #10959, #10398, #9288, #19581, #1382 ),
 ( #18243, #17786, #1508, #16453, #159, #7511 ),
 ( #8731, #6961, #16561, #21135, #269, #7402 ),
 ( #4826, #4192, #20492, #18465, #510, #11426 ),
 ( #11652, #4068, #16909, #20265, #18930, #7629 ),
 ( #2178, #18710, #2643, #20613, #9525, #9873 ),
 ( #20375, #17146, #868, #9400, #11304, #7976 ),
 ( #22159, #14781, #15252, #5962, #2420, #14901 ),
 ( #17023, #22048, #4414, #22512, #16677, #13216 ),
 ( #4307, #12991, #743, #5732, #20719, #18581 ),
 ( #11537, #15010, #3957, #11190, #390, #5845 ),
 ( #13101, #6204, #2303, #7854, #15127, #22391 ) ),
 .UNSPECIFIED., .F., .F., .F. ) 
 B_SPLINE_SURFACE_WITH_KNOTS ( ( 6, 3, 3, 6 ),
 ( 6, 6 ),
 ( 0.000000000000000000, 4.509114667229999540, 8.972055907920001516, 13.39149027790000090 ),
 ( 0.000000000000000000, 1.570796326807959886 ),
 .UNSPECIFIED. ) 
 GEOMETRIC_REPRESENTATION_ITEM ( )  RATIONAL_B_SPLINE_SURFACE ( (
 ( 1.000000000000000000, 0.5999999999966999509, 0.3999999999966994957, 0.2999999999975245246, 0.2499999999983500143, 0.2500000000000000000),
 ( 1.000000000000000000, 0.5999999999966999509, 0.3999999999966994957, 0.2999999999975245246, 0.2499999999983500143, 0.2500000000000000000),
 ( 1.000000000000000000, 0.5999999999966999509, 0.3999999999966994957, 0.2999999999975245246, 0.2499999999983500143, 0.2500000000000000000),
 ( 1.000000000000000000, 0.5999999999966999509, 0.3999999999966994957, 0.2999999999975245246, 0.2499999999983500143, 0.2500000000000000000),
 ( 1.000000000000000000, 0.5999999999966999509, 0.3999999999966994957, 0.2999999999975245246, 0.2499999999983500143, 0.2500000000000000000),
 ( 1.000000000000000000, 0.5999999999966999509, 0.3999999999966994957, 0.2999999999975245246, 0.2499999999983500143, 0.2500000000000000000),
 ( 1.000000000000000000, 0.5999999999966999509, 0.3999999999966994957, 0.2999999999975245246, 0.2499999999983500143, 0.2500000000000000000),
 ( 1.000000000000000000, 0.5999999999966999509, 0.3999999999966994957, 0.2999999999975245246, 0.2499999999983500143, 0.2500000000000000000),
 ( 1.000000000000000000, 0.5999999999966999509, 0.3999999999966994957, 0.2999999999975245246, 0.2499999999983500143, 0.2500000000000000000),
 ( 1.000000000000000000, 0.5999999999966999509, 0.3999999999966994957, 0.2999999999975245246, 0.2499999999983500143, 0.2500000000000000000),
 ( 1.000000000000000000, 0.5999999999966999509, 0.3999999999966994957, 0.2999999999975245246, 0.2499999999983500143, 0.2500000000000000000),
 ( 1.000000000000000000, 0.5999999999966999509, 0.3999999999966994957, 0.2999999999975245246, 0.2499999999983500143, 0.2500000000000000000) ) ) 
 REPRESENTATION_ITEM ( '' )  SURFACE ( )  );
#22281=CARTESIAN_POINT ( 'NONE',  ( -5.939134658313754755, 40.12020460348677631, -142.1663841678295910 ) ) ;
#22286=CARTESIAN_POINT ( 'NONE',  ( -22.83975120143743709, 33.21124457260541618, -143.6444256086801943 ) ) ;
#22289=CARTESIAN_POINT ( 'NONE',  ( -12.12080053524453760, 36.22692207383995822, -147.5732363758075394 ) ) ;
#22298=CARTESIAN_POINT ( 'NONE',  ( -28.89753534828613724, 32.87340430931627822, -144.5128512668707401 ) ) ;
#22301=CARTESIAN_POINT ( 'NONE',  ( -6.093288228389445393, 36.94882630176741856, -147.6373263596331924 ) ) ;
#22302=CARTESIAN_POINT ( 'NONE',  ( -10.15741051819999896, 33.19655140199999721, -141.5761258080000005 ) ) ;
#22308=CARTESIAN_POINT ( 'NONE',  ( -20.64942635760176159, 37.69947397057557481, -140.4574076963200184 ) ) ;
#22333=CARTESIAN_POINT ( 'NONE',  ( -27.45733976771897744, 41.32706283359203780, -144.4146484396392225 ) ) ;
#22338=CARTESIAN_POINT ( 'NONE',  ( -8.565647946481169228, 36.93510680651066025, -139.7232782068570032 ) ) ;
#22348=CARTESIAN_POINT ( 'NONE',  ( -11.47619453871935313, 38.96689531369231219, -139.6865868919825004 ) ) ;
#22353=CARTESIAN_POINT ( 'NONE',  ( -7.529689113779999943, 37.05876528330000497, -139.9906690790000141 ) ) ;
#22360=CARTESIAN_POINT ( 'NONE',  ( -21.01649482008910752, 38.86873054228240676, -148.4377912740901593 ) ) ;
#22363=CARTESIAN_POINT ( 'NONE',  ( -27.36723106715751896, 36.02973761862399726, -148.4771530685680148 ) ) ;
#22370=CARTESIAN_POINT ( 'NONE',  ( -10.28060652870000169, 34.62853500599999990, -147.1732277810000085 ) ) ;
#22377=CARTESIAN_POINT ( 'NONE',  ( -22.52780672254771943, 37.05898997718328047, -140.0074087190062073 ) ) ;
#22380=CARTESIAN_POINT ( 'NONE',  ( -30.02199999990120105, 40.89711431701032041, -146.3052959530037924 ) ) ;
#22386=CARTESIAN_POINT ( 'NONE',  ( -8.554523812450000264, 40.80811760249999764, -146.2789059460000090 ) ) ;
#22391=CARTESIAN_POINT ( 'NONE',  ( -24.06602356364351891, 36.94557182216171753, -148.2530914609847912 ) ) ;
#22392=CARTESIAN_POINT ( 'NONE',  ( -15.79202522179999946, 35.03772048769999969, -148.2850092029999871 ) ) ;
#22393=CARTESIAN_POINT ( 'NONE',  ( -17.46227293580260920, 36.22162391660916114, -140.4936808527247649 ) ) ;
#22397=VERTEX_POINT ( 'NONE', #3896 ) ;
#22398=CARTESIAN_POINT ( 'NONE',  ( -9.032885736888680128, 36.94161628545133169, -147.5965110584589013 ) ) ;
#22399=CARTESIAN_POINT ( 'NONE',  ( -29.69101630271008219, 40.01133477890059709, -145.8395111173322789 ) ) ;
#22406=CARTESIAN_POINT ( 'NONE',  ( -21.95610187424196269, 33.93983213285952871, -145.7584130793499355 ) ) ;
#22408=VERTEX_POINT ( 'NONE', #5443 ) ;
#22409=CARTESIAN_POINT ( 'NONE',  ( -13.13790626639999992, 32.38985286280000508, -143.7114742199999853 ) ) ;
#22415=CARTESIAN_POINT ( 'NONE',  ( -9.971101149720000834, 37.05360750090000721, -147.8421425029999909 ) ) ;
#22420=CARTESIAN_POINT ( 'NONE',  ( -27.26567793384627691, 36.96940380711799889, -148.4835048637780233 ) ) ;
#22423=CARTESIAN_POINT ( 'NONE',  ( -14.24884431179002853, 36.97292245484321427, -139.4994906131552739 ) ) ;
#22430=CARTESIAN_POINT ( 'NONE',  ( -21.05710980616944283, 40.00468299078687551, -145.8366455853836499 ) ) ;
#22436=CARTESIAN_POINT ( 'NONE',  ( -25.34637217103697182, 33.93854440830394026, -142.2873866648762373 ) ) ;
#22443=CARTESIAN_POINT ( 'NONE',  ( -27.16475626505743790, 37.90277890285160112, -148.4897851380626150 ) ) ;
#22452=CARTESIAN_POINT ( 'NONE',  ( -26.50527565025032217, 41.51083911086064404, -144.5405030845066108 ) ) ;
#22458=CARTESIAN_POINT ( 'NONE',  ( -8.031950161270000166, 40.75709267670000457, -141.9144354160000034 ) ) ;
#22463=CARTESIAN_POINT ( 'NONE',  ( -14.50908993389082724, 36.94185792195812468, -140.4668331869691826 ) ) ;
#22469=CARTESIAN_POINT ( 'NONE',  ( -11.86129685666417544, 38.63195145382516671, -140.3074378722488689 ) ) ;
#22470=CARTESIAN_POINT ( 'NONE',  ( -17.89449017619289961, 39.21037955095951588, -147.0820833684587967 ) ) ;
#22480=CARTESIAN_POINT ( 'NONE',  ( -21.29590688489999906, 41.28591597809999314, -144.5271551099999954 ) ) ;
#22484=CARTESIAN_POINT ( 'NONE',  ( -28.71558688633279743, 36.31472216850572465, -140.6134838335071890 ) ) ;
#22487=CARTESIAN_POINT ( 'NONE',  ( -13.92432874550000044, 37.01165864720000087, -139.5650670249999905 ) ) ;
#22512=CARTESIAN_POINT ( 'NONE',  ( -24.31845739552116825, 39.82285914874432819, -147.9810288385895944 ) ) ;
#22513=CARTESIAN_POINT ( 'NONE',  ( -15.76532943048110091, 34.76918918228179933, -146.9254579970016152 ) ) ;
#22514=CARTESIAN_POINT ( 'NONE',  ( -16.90879464662080878, 32.79049683898814749, -144.3773178752514355 ) ) ;
#22519=CARTESIAN_POINT ( 'NONE',  ( -10.01905152896493512, 33.53823069094890741, -144.2070255763365765 ) ) ;
#22526=CARTESIAN_POINT ( 'NONE',  ( -21.41277927229678824, 34.79026080032429746, -146.9436551339746302 ) ) ;
#22535=CARTESIAN_POINT ( 'NONE',  ( -10.14042191033887086, 37.07381867794360630, -148.2039739395296749 ) ) ;
#22536=CARTESIAN_POINT ( 'NONE',  ( -7.728596210859999260, 38.74386132360000090, -140.2295773360000055 ) ) ;
#22540=CARTESIAN_POINT ( 'NONE',  ( -13.46508678921569313, 33.00136909151063236, -146.5816114374932226 ) ) ;
#22551=CARTESIAN_POINT ( 'NONE',  ( -21.19302672506264429, 40.61567049807046459, -143.6742535173994781 ) ) ;
#22552=CARTESIAN_POINT ( 'NONE',  ( -17.27864984443349883, 40.23496799371888244, -142.1532139957071763 ) ) ;
#22557=CARTESIAN_POINT ( 'NONE',  ( -26.29566636579999894, 36.18167175180000328, -140.3932108110000172 ) ) ;
#22559=( BOUNDED_CURVE ( )  B_SPLINE_CURVE ( 5, ( #17720, #17609, #19514, #14031, #15584, #4752, #15815, #10088, #8541, #22966, #1431, #8653 ),
 .UNSPECIFIED., .F., .F. ) 
 B_SPLINE_CURVE_WITH_KNOTS ( ( 6, 3, 3, 6 ),
 ( 0.000000000000000000, 4.454241660750000165, 8.943513424000000711, 13.47090878500000066 ),
 .UNSPECIFIED. ) 
 CURVE ( )  GEOMETRIC_REPRESENTATION_ITEM ( )  RATIONAL_B_SPLINE_CURVE ( ( 0.2500000000000000000, 0.2500000000000000000, 0.2500000000000000000, 0.2500000000000000000, 0.2500000000000000000, 0.2500000000000000000, 0.2500000000000000000, 0.2500000000000000000, 0.2500000000000000000, 0.2500000000000000000, 0.2500000000000000000, 0.2500000000000000000 ) ) 
 REPRESENTATION_ITEM ( '' )  );
#22578=CARTESIAN_POINT ( 'NONE',  ( -9.112817567394211338, 37.91675322417339089, -148.5775373212531463 ) ) ;
#22580=CARTESIAN_POINT ( 'NONE',  ( -27.26567793380000282, 36.96940380710000085, -148.4835048639999968 ) ) ;
#22585=CARTESIAN_POINT ( 'NONE',  ( -17.53569647182064273, 40.68917497046800236, -144.4123951040203906 ) ) ;
#22594=CARTESIAN_POINT ( 'NONE',  ( -14.40511015809376083, 39.11695720674963894, -141.1121292871317792 ) ) ;
#22595=CARTESIAN_POINT ( 'NONE',  ( -25.11959125024334227, 32.26208325171451463, -143.5588604866181015 ) ) ;
#22614=EDGE_LOOP ( 'NONE', ( #6175, #18516, #22678, #996 ) ) ;
#22623=CARTESIAN_POINT ( 'NONE',  ( -16.06125683602935084, 34.67123563680174669, -140.5203502863974165 ) ) ;
#22625=CARTESIAN_POINT ( 'NONE',  ( -17.01097330534292240, 32.84288031327549362, -143.4865848381450348 ) ) ;
#22627=CARTESIAN_POINT ( 'NONE',  ( -4.428060343052305114, 37.07089632425688563, -139.9976721173915450 ) ) ;
#22641=CARTESIAN_POINT ( 'NONE',  ( -22.52780672254944250, 37.05898997718308152, -140.0074087189881880 ) ) ;
#22642=CARTESIAN_POINT ( 'NONE',  ( -16.81794493339999619, 37.02435727940000731, -140.5111119820000170 ) ) ;
#22645=CARTESIAN_POINT ( 'NONE',  ( -5.733381482170000432, 39.34803470290000149, -147.3316303149999840 ) ) ;
#22647=CARTESIAN_POINT ( 'NONE',  ( -8.238646733050000392, 41.24792906369999912, -143.6196368420000056 ) ) ;
#22653=CARTESIAN_POINT ( 'NONE',  ( -13.44992991213783995, 32.27235479864616963, -143.7382959716714481 ) ) ;
#22659=CARTESIAN_POINT ( 'NONE',  ( -14.68945449529999969, 41.62249060810000145, -143.5408288559999903 ) ) ;
#22662=CARTESIAN_POINT ( 'NONE',  ( -19.04747499291816482, 37.87694391812206618, -147.8065290023580189 ) ) ;
#22666=CARTESIAN_POINT ( 'NONE',  ( -25.30721887416896010, 33.85380199680784585, -145.9318938156505965 ) ) ;
#22673=CARTESIAN_POINT ( 'NONE',  ( -27.39460866327015864, 37.71341861930930150, -147.4556575159825229 ) ) ;
#22678=ORIENTED_EDGE ( 'NONE', *, *, #5211, .T. ) ;
#22685=CARTESIAN_POINT ( 'NONE',  ( -7.469704578253070437, 36.11012087976002505, -139.6489141305654584 ) ) ;
#22686=CARTESIAN_POINT ( 'NONE',  ( -8.764836022000000781, 39.53398178709999655, -147.5842891229999907 ) ) ;
#22689=( BOUNDED_CURVE ( )  B_SPLINE_CURVE ( 5, ( #22108, #14960, #9587, #5795, #13055, #20327, #2476, #15074, #6027, #17326, #17799, #3066 ),
 .UNSPECIFIED., .F., .F. ) 
 B_SPLINE_CURVE_WITH_KNOTS ( ( 6, 3, 3, 6 ),
 ( 0.000000000000000000, 4.151671928079999851, 8.316542232069998875, 12.50501063799999990 ),
 .UNSPECIFIED. ) 
 CURVE ( )  GEOMETRIC_REPRESENTATION_ITEM ( )  RATIONAL_B_SPLINE_CURVE ( ( 0.2500000000000000000, 0.2500000000000000000, 0.2500000000000000000, 0.2500000000000000000, 0.2500000000000000000, 0.2500000000000000000, 0.2500000000000000000, 0.2500000000000000000, 0.2500000000000000000, 0.2500000000000000000, 0.2500000000000000000, 0.2500000000000000000 ) ) 
 REPRESENTATION_ITEM ( '' )  );
#22695=CARTESIAN_POINT ( 'NONE',  ( -18.50695094929572804, 37.98868281441455252, -148.6476439268063245 ) ) ;
#22701=CARTESIAN_POINT ( 'NONE',  ( -30.02199999990000023, 40.89711431700000333, -146.3052959529999839 ) ) ;
#22706=CARTESIAN_POINT ( 'NONE',  ( -14.45813593939999997, 41.09907220950000095, -141.6721478100000127 ) ) ;
#22707=CARTESIAN_POINT ( 'NONE',  ( -25.52669956779758209, 32.98784426750318488, -146.4664506488380198 ) ) ;
#22729=CARTESIAN_POINT ( 'NONE',  ( -8.971913342289999704, 37.83624783359999810, -148.2794752869999968 ) ) ;
#22740=CARTESIAN_POINT ( 'NONE',  ( -4.740745377972312546, 37.03357229754023194, -140.5852769423916300 ) ) ;
#22742=EDGE_LOOP ( 'NONE', ( #15603, #3086, #11174, #12641 ) ) ;
#22743=CARTESIAN_POINT ( 'NONE',  ( -9.178237216079999428, 36.01795878010000251, -148.2568923610000127 ) ) ;
#22749=EDGE_CURVE ( 'NONE', #7827, #6123, #4347, .T. ) ;
#22752=CARTESIAN_POINT ( 'NONE',  ( -28.59946202390224101, 34.31616424881172378, -140.2812573677418015 ) ) ;
#22756=CARTESIAN_POINT ( 'NONE',  ( -24.01715389780000010, 40.57582142210000598, -141.9832779239999923 ) ) ;
#22763=CARTESIAN_POINT ( 'NONE',  ( -10.13646216689614299, 32.62416684293538083, -146.3387243813236296 ) ) ;
#22765=CARTESIAN_POINT ( 'NONE',  ( -7.777479512046423515, 39.31680732581353510, -140.9495105956953864 ) ) ;
#22771=CARTESIAN_POINT ( 'NONE',  ( -7.069412601425229425, 33.52643604124185828, -143.7480921736344897 ) ) ;
#22772=CARTESIAN_POINT ( 'NONE',  ( -27.26567793380000282, 36.96940380710000085, -148.4835048639999968 ) ) ;
#22779=CARTESIAN_POINT ( 'NONE',  ( -15.57786843150000067, 37.00666880280000726, -148.5521201120000114 ) ) ;
#22781=CARTESIAN_POINT ( 'NONE',  ( -21.80913741070000000, 38.74859698539999897, -147.9243209519999880 ) ) ;
#22783=CARTESIAN_POINT ( 'NONE',  ( -18.80116448531132889, 37.77574032756653821, -147.4754319351692402 ) ) ;
#22791=CARTESIAN_POINT ( 'NONE',  ( -24.10609388846707191, 35.33584289672160850, -147.6535802351943971 ) ) ;
#22809=CARTESIAN_POINT ( 'NONE',  ( -18.37691940361212062, 35.51168060177987940, -147.4900940512081888 ) ) ;
#22810=CARTESIAN_POINT ( 'NONE',  ( -11.38486064716495960, 36.95668670071903961, -140.3965526140712257 ) ) ;
#22815=EDGE_CURVE ( 'NONE', #2118, #16530, #19989, .T. ) ;
#22834=CARTESIAN_POINT ( 'NONE',  ( -14.68128999515341704, 37.84311035093374898, -139.6736120657584479 ) ) ;
#22835=CARTESIAN_POINT ( 'NONE',  ( -26.51626171185139924, 36.02146533797493078, -139.7633415074477057 ) ) ;
#22856=CARTESIAN_POINT ( 'NONE',  ( -14.43541547443227557, 40.58553253640290137, -144.4623272911945833 ) ) ;
#22864=CARTESIAN_POINT ( 'NONE',  ( -11.59475511470959752, 36.93163239418914401, -139.6817994051292260 ) ) ;
#22881=FACE_OUTER_BOUND ( 'NONE', #11752, .T. ) ;
#22888=CARTESIAN_POINT ( 'NONE',  ( -14.01657753872050094, 36.22806874875712424, -140.5479840251192059 ) ) ;
#22897=CARTESIAN_POINT ( 'NONE',  ( -22.00705883600000234, 37.05789963359999462, -148.1619053240000028 ) ) ;
#22900=CARTESIAN_POINT ( 'NONE',  ( -7.496535154942796986, 35.57088646773350860, -140.8259703478072993 ) ) ;
#22908=CARTESIAN_POINT ( 'NONE',  ( -20.93854596060227635, 37.74500530013531829, -147.9603137873362186 ) ) ;
#22909=CARTESIAN_POINT ( 'NONE',  ( -17.27792307866062060, 37.67644708809300624, -140.6717186866207783 ) ) ;
#22914=CARTESIAN_POINT ( 'NONE',  ( -24.95294881421506261, 33.96416018870619524, -145.8216992312312641 ) ) ;
#22936=CARTESIAN_POINT ( 'NONE',  ( -18.64600821080000159, 33.72696025770000006, -146.0724859999999978 ) ) ;
#22937=CARTESIAN_POINT ( 'NONE',  ( -10.97748938910000049, 39.75689975739999937, -140.4868351200000234 ) ) ;
#22940=CARTESIAN_POINT ( 'NONE',  ( -7.801194085041059267, 32.45455882765661926, -143.7439339061524493 ) ) ;
#22944=CARTESIAN_POINT ( 'NONE',  ( -7.486908230310619139, 37.06387187510053138, -140.3212062627005707 ) ) ;
#22946=ORIENTED_EDGE ( 'NONE', *, *, #10115, .T. ) ;
#22955=CARTESIAN_POINT ( 'NONE',  ( -15.48617276601169834, 40.96818823142278632, -144.3825155029135772 ) ) ;
#22957=CARTESIAN_POINT ( 'NONE',  ( -26.51312621108908019, 36.10278884006311273, -140.1473911447703529 ) ) ;
#22960=CARTESIAN_POINT ( 'NONE',  ( -11.48759298129999884, 37.74537190000000209, -140.3874188149999895 ) ) ;
#22966=CARTESIAN_POINT ( 'NONE',  ( -25.44349950029999974, 35.21826511839999796, -139.9516901549999943 ) ) ;
#22971=CARTESIAN_POINT ( 'NONE',  ( -13.60171424471084478, 38.61389101324630246, -140.5757119291933748 ) ) ;
#22982=CARTESIAN_POINT ( 'NONE',  ( -16.81794493339610241, 37.02435727936596521, -140.5111119823619958 ) ) ;
#22986=FACE_OUTER_BOUND ( 'NONE', #18459, .T. ) ;
#22990=CARTESIAN_POINT ( 'NONE',  ( -25.46021907539999773, 33.59345108530000346, -146.1038275270000213 ) ) ;
#22992=CARTESIAN_POINT ( 'NONE',  ( -28.03429568396224170, 32.40695676819103710, -144.4586890253826255 ) ) ;
#22995=CARTESIAN_POINT ( 'NONE',  ( -24.21925763020469802, 40.64313348517629265, -144.4529654621569819 ) ) ;
#23001=CARTESIAN_POINT ( 'NONE',  ( -5.932764524189999555, 37.76833845600000217, -147.9772051180000005 ) ) ;
#23003=CARTESIAN_POINT ( 'NONE',  ( -9.092633533251282429, 40.57158656394992846, -143.6010347923813129 ) ) ;
#23012=CARTESIAN_POINT ( 'NONE',  ( -7.206173031900359405, 35.38491483727327847, -147.9515367338636054 ) ) ;
#23013=CARTESIAN_POINT ( 'NONE',  ( -27.06022691649999956, 38.83733237969999408, -148.2479545119999784 ) ) ;
#23022=CARTESIAN_POINT ( 'NONE',  ( -18.65864117670379585, 40.55340188292282022, -145.9561081538003862 ) ) ;
#23027=CARTESIAN_POINT ( 'NONE',  ( -17.52779041586177300, 36.93962571632795999, -139.7364823516871581 ) ) ;
#23029=CARTESIAN_POINT ( 'NONE',  ( -12.56920363940049512, 37.00563451942266369, -148.6543378380284821 ) ) ;
#23033=EDGE_CURVE ( 'NONE', #16183, #17995, #14222, .T. ) ;
#23039=CARTESIAN_POINT ( 'NONE',  ( -28.81387671664944250, 37.02484288695405468, -140.6184821045081037 ) ) ;
#23045=CARTESIAN_POINT ( 'NONE',  ( -11.79464594726566062, 38.67573169081060058, -148.1300312029912050 ) ) ;
#23047=( BOUNDED_CURVE ( )  B_SPLINE_CURVE ( 5, ( #11795, #13236, #7993, #15276, #20512, #22642 ),
 .UNSPECIFIED., .F., .F. ) 
 B_SPLINE_CURVE_WITH_KNOTS ( ( 6, 6 ),
 ( 0.000000000000000000, 1.570796326654103181 ),
 .UNSPECIFIED. ) 
 CURVE ( )  GEOMETRIC_REPRESENTATION_ITEM ( )  RATIONAL_B_SPLINE_CURVE ( ( 1.000000000000000000, 0.6000000000358791663, 0.4000000000358792107, 0.3000000000269094080, 0.2500000000179396498, 0.2500000000000000555 ) ) 
 REPRESENTATION_ITEM ( '' )  );
#23048=CARTESIAN_POINT ( 'NONE',  ( -7.572469997258134633, 37.05365869149841984, -139.6601318950651773 ) ) ;
#23061=CARTESIAN_POINT ( 'NONE',  ( -20.26899604980000191, 40.93030953040000242, -143.7497896410000067 ) ) ;
#23067=CARTESIAN_POINT ( 'NONE',  ( -14.79658270967934008, 39.12156175677914405, -141.0283858338752339 ) ) ;
#23069=CARTESIAN_POINT ( 'NONE',  ( -26.61707828802655484, 36.92896776167479089, -139.7487649555727103 ) ) ;
#23073=CARTESIAN_POINT ( 'NONE',  ( -12.76385253890000016, 37.02886902030000016, -147.6186336929999925 ) ) ;
#23086=CARTESIAN_POINT ( 'NONE',  ( -13.90907534077411434, 39.72570884558322746, -140.3685967658352638 ) ) ;
#23092=CARTESIAN_POINT ( 'NONE',  ( -28.81387671665526895, 37.02484288695334413, -140.6184821045066826 ) ) ;
#23094=EDGE_LOOP ( 'NONE', ( #12126, #22946, #8992, #16765 ) ) ;
#23095=CARTESIAN_POINT ( 'NONE',  ( -16.26754611222665048, 35.58143005778827472, -140.5099932849695961 ) ) ;
#23104=CARTESIAN_POINT ( 'NONE',  ( -25.91744746520000220, 33.58572460659999592, -142.1592104600000255 ) ) ;
#23106=EDGE_CURVE ( 'NONE', #9000, #20464, #6971, .T. ) ;
#23118=CARTESIAN_POINT ( 'NONE',  ( -10.01829490536019662, 32.29821814703051075, -144.2706886520148828 ) ) ;
#23120=CARTESIAN_POINT ( 'NONE',  ( -9.674592407298980845, 39.37273218293604060, -147.1879168912154228 ) ) ;
#23124=( NAMED_UNIT ( * ) PLANE_ANGLE_UNIT ( ) SI_UNIT ( $, .RADIAN. ) );
#23126=CARTESIAN_POINT ( 'NONE',  ( -8.008464111606381053, 33.29536412533623491, -142.0809313903132249 ) ) ;
#23136=CARTESIAN_POINT ( 'NONE',  ( -17.53569647200000148, 40.68917497039999631, -144.4123951040000122 ) ) ;
#23154=CARTESIAN_POINT ( 'NONE',  ( -28.47499893024826889, 37.06529344307018192, -140.4421442387167360 ) ) ;
#23158=CARTESIAN_POINT ( 'NONE',  ( -8.514310886080000529, 36.94123471670000214, -140.1199228270000106 ) ) ;
#23161=CARTESIAN_POINT ( 'NONE',  ( -7.363485702945446576, 35.16406626390504897, -139.8948755779048270 ) ) ;
#23179=CARTESIAN_POINT ( 'NONE',  ( -12.18289575740000075, 37.87223172089999679, -148.4976681630000144 ) ) ;
#23181=CARTESIAN_POINT ( 'NONE',  ( -22.03835531321502117, 36.10604702353144546, -148.4978763513408921 ) ) ;
#23202=CARTESIAN_POINT ( 'NONE',  ( -21.03694116389999635, 36.94210036639999828, -147.9486865819999935 ) ) ;
#23204=CARTESIAN_POINT ( 'NONE',  ( -14.23530246729999860, 39.72954597060000026, -140.2988105550000171 ) ) ;
#23205=CARTESIAN_POINT ( 'NONE',  ( -28.59540039647975718, 38.02976288075254274, -140.4496050658455886 ) ) ;
#23207=CARTESIAN_POINT ( 'NONE',  ( -9.072898850179999641, 36.94639249900000522, -148.2684494029999769 ) ) ;
#23219=CARTESIAN_POINT ( 'NONE',  ( -6.938784185830692230, 37.04974994751732709, -148.5388410750851165 ) ) ;
#23226=EDGE_CURVE ( 'NONE', #19149, #7237, #448, .T. ) ;
#23236=CARTESIAN_POINT ( 'NONE',  ( -10.92854443021380106, 33.70908472083943508, -142.0058283514407833 ) ) ;
#23247=CARTESIAN_POINT ( 'NONE',  ( -6.375405121820262089, 34.81974364058724802, -147.0569159591387631 ) ) ;
#23260=CARTESIAN_POINT ( 'NONE',  ( -12.56920363940050223, 37.00563451942269921, -148.6543378380283684 ) ) ;
#23262=CARTESIAN_POINT ( 'NONE',  ( -28.90798551740000022, 37.01360947639999921, -139.5686590450000040 ) ) ;
#23268=CARTESIAN_POINT ( 'NONE',  ( -15.57786843150000067, 37.00666880280000726, -148.5521201120000114 ) ) ;
#23275=CARTESIAN_POINT ( 'NONE',  ( -16.27122798455739527, 36.16215725498741307, -148.2498576458012849 ) ) ;
#23276=CARTESIAN_POINT ( 'NONE',  ( -28.21528208400208726, 34.41375009921395645, -140.3410504852042777 ) ) ;
#23282=CARTESIAN_POINT ( 'NONE',  ( -20.24645939794500293, 34.66320656008903711, -141.1397956616578426 ) ) ;
#23283=CARTESIAN_POINT ( 'NONE',  ( -11.37826538047574765, 40.43565427802512602, -146.2436245357287703 ) ) ;
#23287=( BOUNDED_CURVE ( )  B_SPLINE_CURVE ( 5, ( #4856, #19377, #19499, #10192, #3193, #3084 ),
 .UNSPECIFIED., .F., .F. ) 
 B_SPLINE_CURVE_WITH_KNOTS ( ( 6, 6 ),
 ( 0.000000000000000000, 1.570796326503991924 ),
 .UNSPECIFIED. ) 
 CURVE ( )  GEOMETRIC_REPRESENTATION_ITEM ( )  RATIONAL_B_SPLINE_CURVE ( ( 1.000000000000000000, 0.6000000000741045891, 0.4000000000741046335, 0.3000000000555784752, 0.2500000000370523612, 0.2500000000000000555 ) ) 
 REPRESENTATION_ITEM ( '' )  );
#23290=CARTESIAN_POINT ( 'NONE',  ( -8.100541861814507527, 36.99062475582145737, -140.7379126119400610 ) ) ;
#23301=CARTESIAN_POINT ( 'NONE',  ( -15.80598957920876302, 37.98416398598419619, -148.5052001024989181 ) ) ;
#23307=CARTESIAN_POINT ( 'NONE',  ( -26.64637222122986771, 39.75485585484910445, -140.1771219359338829 ) ) ;
#23313=CARTESIAN_POINT ( 'NONE',  ( -12.76385253890000016, 37.02886902030000016, -147.6186336929999925 ) ) ;
#23319=APPLICATION_CONTEXT ( 'automotive_design' ) ;
#23320=CARTESIAN_POINT ( 'NONE',  ( -13.87262227687442540, 40.83548773877500793, -141.9013165816338073 ) ) ;
#23321=CARTESIAN_POINT ( 'NONE',  ( -28.81387671665254757, 37.02484288695368519, -140.6184821045073647 ) ) ;
#23325=( BOUNDED_SURFACE ( )  B_SPLINE_SURFACE ( 5, 5, ( 
 ( #3805, #3570, #18082, #11267, #8901, #348 ),
 ( #22124, #7474, #16181, #14629, #9363, #7590 ),
 ( #16300, #235, #9014, #11156, #9257, #10918 ),
 ( #2144, #5, #12602, #7254, #14521, #21787 ),
 ( #5472, #12715, #12831, #19984, #11044, #3684 ),
 ( #14865, #9138, #16636, #16418, #128, #18322 ),
 ( #16528, #14738, #12952, #20229, #3922, #22585 ),
 ( #20681, #13527, #7819, #4493, #2380, #11860 ),
 ( #11385, #9601, #18667, #16875, #4147, #22470 ),
 ( #7933, #5924, #583, #937, #8163, #11732 ),
 ( #13179, #22695, #2725, #700, #471, #6391 ),
 ( #13651, #18889, #15087, #20453, #4375, #15328 ) ),
 .UNSPECIFIED., .F., .F., .F. ) 
 B_SPLINE_SURFACE_WITH_KNOTS ( ( 6, 3, 3, 6 ),
 ( 6, 6 ),
 ( 0.000000000000000000, 4.124045064660000648, 8.344666563069999654, 12.67057240369999960 ),
 ( 0.000000000000000000, 1.570796326683649990 ),
 .UNSPECIFIED. ) 
 GEOMETRIC_REPRESENTATION_ITEM ( )  RATIONAL_B_SPLINE_SURFACE ( (
 ( 1.000000000000000000, 0.6000000000283549628, 0.4000000000283550072, 0.3000000000212664775, 0.2500000000141774925, 0.2500000000000000000),
 ( 1.000000000000000000, 0.6000000000283549628, 0.4000000000283550072, 0.3000000000212664775, 0.2500000000141774925, 0.2500000000000000000),
 ( 1.000000000000000000, 0.6000000000283549628, 0.4000000000283550072, 0.3000000000212664775, 0.2500000000141774925, 0.2500000000000000000),
 ( 1.000000000000000000, 0.6000000000283549628, 0.4000000000283550072, 0.3000000000212664775, 0.2500000000141774925, 0.2500000000000000000),
 ( 1.000000000000000000, 0.6000000000283549628, 0.4000000000283550072, 0.3000000000212664775, 0.2500000000141774925, 0.2500000000000000000),
 ( 1.000000000000000000, 0.6000000000283549628, 0.4000000000283550072, 0.3000000000212664775, 0.2500000000141774925, 0.2500000000000000000),
 ( 1.000000000000000000, 0.6000000000283549628, 0.4000000000283550072, 0.3000000000212664775, 0.2500000000141774925, 0.2500000000000000000),
 ( 1.000000000000000000, 0.6000000000283549628, 0.4000000000283550072, 0.3000000000212664775, 0.2500000000141774925, 0.2500000000000000000),
 ( 1.000000000000000000, 0.6000000000283549628, 0.4000000000283550072, 0.3000000000212664775, 0.2500000000141774925, 0.2500000000000000000),
 ( 1.000000000000000000, 0.6000000000283549628, 0.4000000000283550072, 0.3000000000212664775, 0.2500000000141774925, 0.2500000000000000000),
 ( 1.000000000000000000, 0.6000000000283549628, 0.4000000000283550072, 0.3000000000212664775, 0.2500000000141774925, 0.2500000000000000000),
 ( 1.000000000000000000, 0.6000000000283549628, 0.4000000000283550072, 0.3000000000212664775, 0.2500000000141774925, 0.2500000000000000000) ) ) 
 REPRESENTATION_ITEM ( '' )  SURFACE ( )  );
#23327=CARTESIAN_POINT ( 'NONE',  ( -29.13601448249999848, 36.98639052360000079, -140.5419328609999923 ) ) ;
#23335=CARTESIAN_POINT ( 'NONE',  ( -5.847812726100290348, 39.76587201757381962, -147.8755786061779816 ) ) ;
#23336=CARTESIAN_POINT ( 'NONE',  ( -7.806459626920000616, 32.86659014889999497, -143.7778124400000195 ) ) ;
#23348=CARTESIAN_POINT ( 'NONE',  ( -29.04405754842699849, 38.20917013907699555, -139.5702141476339762 ) ) ;
#23353=CARTESIAN_POINT ( 'NONE',  ( -11.59475511509054257, 36.93163239414370480, -139.6817994054218559 ) ) ;
#23362=PRESENTATION_STYLE_ASSIGNMENT (( #5264 ) ) ;
#23371=CARTESIAN_POINT ( 'NONE',  ( -17.27864984460000031, 40.23496799359999443, -142.1532139960000052 ) ) ;
#23378=CARTESIAN_POINT ( 'NONE',  ( -16.81794493339999619, 37.02435727940000731, -140.5111119820000170 ) ) ;
#23388=CARTESIAN_POINT ( 'NONE',  ( -15.68268784160000173, 36.02211616019999951, -148.5535485649999998 ) ) ;
#23395=CARTESIAN_POINT ( 'NONE',  ( -20.44384907338949375, 36.15213303015924851, -140.4838640016932629 ) ) ;
#23396=CARTESIAN_POINT ( 'NONE',  ( -11.97376781498133447, 40.01783495556804837, -145.9099724590802225 ) ) ;
#23426=CARTESIAN_POINT ( 'NONE',  ( -10.36675979729999852, 34.52853970540000006, -140.3392284379999921 ) ) ;
#23442=CARTESIAN_POINT ( 'NONE',  ( -28.33971964075504957, 37.08144121879503530, -140.0461821376672162 ) ) ;
#23448=CARTESIAN_POINT ( 'NONE',  ( -13.37265858230000148, 32.83955069500000690, -141.7941727500000013 ) ) ;
#23453=CARTESIAN_POINT ( 'NONE',  ( -26.59168384020000175, 38.48554521319999822, -140.5676127940000129 ) ) ;
#23460=( BOUNDED_SURFACE ( )  B_SPLINE_SURFACE ( 5, 5, ( 
 ( #18466, #20377, #16912, #2179, #20493, #511 ),
 ( #7745, #5964, #14783, #17025, #18359, #15130 ),
 ( #22392, #4193, #13218, #6090, #11306, #13342 ),
 ( #9402, #18582, #4309, #20614, #2304, #22513 ),
 ( #4069, #11539, #9749, #14902, #6205, #9530 ),
 ( #22049, #2071, #745, #12993, #7631, #22161 ),
 ( #5846, #13103, #14052, #1099, #8329, #12138 ),
 ( #13567, #8559, #10350, #15719, #17149, #15478 ),
 ( #869, #4536, #15831, #22623, #1334, #2644 ),
 ( #8452, #19285, #3118, #4890, #23095, #10233 ),
 ( #19168, #11776, #13696, #12020, #20841, #13822 ),
 ( #6786, #21320, #9875, #11653, #17502, #22982 ) ),
 .UNSPECIFIED., .F., .F., .F. ) 
 B_SPLINE_SURFACE_WITH_KNOTS ( ( 6, 3, 3, 6 ),
 ( 6, 6 ),
 ( 0.000000000000000000, 4.358589029760000066, 8.533830367689999363, 12.54112731390000057 ),
 ( 0.000000000000000000, 1.570796326769924978 ),
 .UNSPECIFIED. ) 
 GEOMETRIC_REPRESENTATION_ITEM ( )  RATIONAL_B_SPLINE_SURFACE ( (
 ( 1.000000000000000000, 0.6000000000063859806, 0.4000000000063860250, 0.3000000000047894910, 0.2500000000031930014, 0.2500000000000000000),
 ( 1.000000000000000000, 0.6000000000063859806, 0.4000000000063860250, 0.3000000000047894910, 0.2500000000031930014, 0.2500000000000000000),
 ( 1.000000000000000000, 0.6000000000063859806, 0.4000000000063860250, 0.3000000000047894910, 0.2500000000031930014, 0.2500000000000000000),
 ( 1.000000000000000000, 0.6000000000063859806, 0.4000000000063860250, 0.3000000000047894910, 0.2500000000031930014, 0.2500000000000000000),
 ( 1.000000000000000000, 0.6000000000063859806, 0.4000000000063860250, 0.3000000000047894910, 0.2500000000031930014, 0.2500000000000000000),
 ( 1.000000000000000000, 0.6000000000063859806, 0.4000000000063860250, 0.3000000000047894910, 0.2500000000031930014, 0.2500000000000000000),
 ( 1.000000000000000000, 0.6000000000063859806, 0.4000000000063860250, 0.3000000000047894910, 0.2500000000031930014, 0.2500000000000000000),
 ( 1.000000000000000000, 0.6000000000063859806, 0.4000000000063860250, 0.3000000000047894910, 0.2500000000031930014, 0.2500000000000000000),
 ( 1.000000000000000000, 0.6000000000063859806, 0.4000000000063860250, 0.3000000000047894910, 0.2500000000031930014, 0.2500000000000000000),
 ( 1.000000000000000000, 0.6000000000063859806, 0.4000000000063860250, 0.3000000000047894910, 0.2500000000031930014, 0.2500000000000000000),
 ( 1.000000000000000000, 0.6000000000063859806, 0.4000000000063860250, 0.3000000000047894910, 0.2500000000031930014, 0.2500000000000000000),
 ( 1.000000000000000000, 0.6000000000063859806, 0.4000000000063860250, 0.3000000000047894910, 0.2500000000031930014, 0.2500000000000000000) ) ) 
 REPRESENTATION_ITEM ( '' )  SURFACE ( )  );
#23461=CARTESIAN_POINT ( 'NONE',  ( -24.49703822390000241, 40.50511125069999707, -146.0729279460000214 ) ) ;
#23466=CARTESIAN_POINT ( 'NONE',  ( -11.38486064677451992, 36.95668670076564410, -140.3965526144922080 ) ) ;
#23467=CARTESIAN_POINT ( 'NONE',  ( -18.75102069614494837, 32.86990036210830368, -146.6269676767523720 ) ) ;
#23469=CARTESIAN_POINT ( 'NONE',  ( -9.701308260419525098, 37.75684802965571407, -147.4734421784763754 ) ) ;
#23482=EDGE_CURVE ( 'NONE', #16530, #4528, #4422, .T. ) ;
#23509=ADVANCED_FACE ( 'NONE', ( #22099 ), #11619, .F. ) ;
#23515=CARTESIAN_POINT ( 'NONE',  ( -11.40579923052419176, 40.54540395906296624, -144.5952108064055608 ) ) ;
#23535=CARTESIAN_POINT ( 'NONE',  ( -22.25292207123187893, 34.30819563794508298, -147.7538981111728731 ) ) ;
#23540=CARTESIAN_POINT ( 'NONE',  ( -29.13601448249999848, 36.98639052360000079, -140.5419328609999923 ) ) ;
ENDSEC;
END-ISO-10303-21;
